ISO-10303-21;
HEADER;
FILE_DESCRIPTION (('STEP AP214'),
    '1' );
FILE_NAME ('positive pin.step',
    '2026-10-05T20:10:51',
    ( '' ),
    ( '' ),
    'SwSTEP 2.0',
    'SolidWorks 2020',
    '' );
FILE_SCHEMA (( 'AUTOMOTIVE_DESIGN' ));
ENDSEC;

DATA;
#66=CARTESIAN_POINT ( 'NONE',  ( -8.012344526598182026E-15, 11.29687500034139980, -1.575800808251669460 ) ) ;
#212=CARTESIAN_POINT ( 'NONE',  ( -0.6823417656250003738, 12.71354166700806942, 1.181850606188754593 ) ) ;
#241=CARTESIAN_POINT ( 'NONE',  ( -2.788906526875773208E-15, 11.93750000000000000, -1.499999999999998446 ) ) ;
#278=CARTESIAN_POINT ( 'NONE',  ( 0.6823417656249934904, 10.75520833367472839, 1.181850606188764807 ) ) ;
#292=CARTESIAN_POINT ( 'NONE',  ( 0.7500000000000006661, 9.614583334016129967, 1.299038105676657340 ) ) ;
#320=CARTESIAN_POINT ( 'NONE',  ( -1.500000000000001110, 9.302083334016128191, 0.8660254037844419273 ) ) ;
#355=ORIENTED_EDGE ( 'NONE', *, *, #112300, .T. ) ;
#458=CARTESIAN_POINT ( 'NONE',  ( -1.364683531250014514, 8.588541667008065872, -0.7879004041258335089 ) ) ;
#503=ORIENTED_EDGE ( 'NONE', *, *, #67371, .T. ) ;
#525=CARTESIAN_POINT ( 'NONE',  ( 1.364683531249996529, 14.02604166700806942, 0.7879004041258405033 ) ) ;
#645=ORIENTED_EDGE ( 'NONE', *, *, #104314, .F. ) ;
#719=CARTESIAN_POINT ( 'NONE',  ( 1.499999999999993117, 11.35416666666667140, 0.8660254037844409281 ) ) ;
#723=CARTESIAN_POINT ( 'NONE',  ( -8.012344526598182026E-15, 15.35937500034140513, -1.575800808251669460 ) ) ;
#724=ORIENTED_EDGE ( 'NONE', *, *, #115096, .T. ) ;
#730=CARTESIAN_POINT ( 'NONE',  ( -0.5773502691896261751, -4.295408888568413630, -0.9999999999999991118 ) ) ;
#762=CARTESIAN_POINT ( 'NONE',  ( -1.364683531250010740, 11.19270833367473550, 0.7879004041258445001 ) ) ;
#784=CARTESIAN_POINT ( 'NONE',  ( -1.115562610750309283E-14, 11.31249999999999822, 1.500000000000001554 ) ) ;
#839=CARTESIAN_POINT ( 'NONE',  ( 0.7500000000000006661, 12.44791666734946389, -1.299038105676657340 ) ) ;
#934=CARTESIAN_POINT ( 'NONE',  ( -8.012344526598182026E-15, 13.04687500034139980, -1.575800808251669460 ) ) ;
#976=CARTESIAN_POINT ( 'NONE',  ( 3.834746474454188013E-15, 8.812500000000000000, 1.500000000000001554 ) ) ;
#988=CARTESIAN_POINT ( 'NONE',  ( -1.364683531250014514, 12.08854166700806765, -0.7879004041258335089 ) ) ;
#1036=CARTESIAN_POINT ( 'NONE',  ( -0.7500000000000179856, 9.541666666666671404, 1.299038105676658228 ) ) ;
#1045=LINE ( 'NONE', #164649, #45487 ) ;
#1073=ORIENTED_EDGE ( 'NONE', *, *, #78717, .T. ) ;
#1134=CYLINDRICAL_SURFACE ( 'NONE', #80203, 1.500000000000000222 ) ;
#1140=CARTESIAN_POINT ( 'NONE',  ( -0.6823417656250003738, 11.40104166700806765, 1.181850606188754593 ) ) ;
#1193=EDGE_LOOP ( 'NONE', ( #146802, #196436, #20921, #16035 ) ) ;
#1221=CYLINDRICAL_SURFACE ( 'NONE', #40355, 1.500000000000000222 ) ;
#1289=CARTESIAN_POINT ( 'NONE',  ( -8.012344526598182026E-15, 11.85937500034140157, -1.575800808251669460 ) ) ;
#1344=CYLINDRICAL_SURFACE ( 'NONE', #14413, 0.6500000000000000222 ) ;
#1351=EDGE_CURVE ( 'NONE', #113572, #84297, #191408, .T. ) ;
#1353=CARTESIAN_POINT ( 'NONE',  ( -0.6823417656250039265, 9.880208333674728394, -1.181850606188755259 ) ) ;
#1394=CARTESIAN_POINT ( 'NONE',  ( 1.499999999999997113, 8.927083334016126415, -0.8660254037844378194 ) ) ;
#1396=EDGE_LOOP ( 'NONE', ( #3690, #54781, #30008, #199049 ) ) ;
#1432=VERTEX_POINT ( 'NONE', #200449 ) ;
#1457=FACE_OUTER_BOUND ( 'NONE', #169413, .T. ) ;
#1531=CARTESIAN_POINT ( 'NONE',  ( 1.364683531249996529, 8.463541667008065872, 0.7879004041258403923 ) ) ;
#1547=ORIENTED_EDGE ( 'NONE', *, *, #172795, .T. ) ;
#1571=EDGE_LOOP ( 'NONE', ( #141077, #205442 ) ) ;
#1588=CARTESIAN_POINT ( 'NONE',  ( 0.000000000000000000, 13.49999999999999822, -1.500000000000000222 ) ) ;
#1600=CARTESIAN_POINT ( 'NONE',  ( -1.402160292154681736E-14, 14.73437500034139980, 1.575800808251682339 ) ) ;
#1738=VERTEX_POINT ( 'NONE', #78731 ) ;
#1784=DIRECTION ( 'NONE',  ( -1.665334536937734811E-16, 0.000000000000000000, -1.000000000000000000 ) ) ;
#1791=CARTESIAN_POINT ( 'NONE',  ( -1.364683531250000748, 11.85937500034139802, 0.000000000000000000 ) ) ;
#1796=CARTESIAN_POINT ( 'NONE',  ( 1.499999999999993117, 10.60416666666666607, 0.8660254037844409281 ) ) ;
#1809=CARTESIAN_POINT ( 'NONE',  ( 1.499999999999996891, 9.645833333333333925, -0.8660254037844378194 ) ) ;
#1837=ORIENTED_EDGE ( 'NONE', *, *, #166482, .F. ) ;
#1842=CARTESIAN_POINT ( 'NONE',  ( -0.6823417656250039265, 8.880208333674733723, -1.181850606188755259 ) ) ;
#1855=CARTESIAN_POINT ( 'NONE',  ( -1.500000000000015099, 12.51041666734946389, -0.8660254037844309360 ) ) ;
#1912=FACE_OUTER_BOUND ( 'NONE', #168026, .T. ) ;
#1913=CARTESIAN_POINT ( 'NONE',  ( -6.009258394948636914E-15, 13.21875000068279427, -1.732050807568875195 ) ) ;
#1949=VECTOR ( 'NONE', #166204, 1000.000000000000000 ) ;
#1960=CARTESIAN_POINT ( 'NONE',  ( -0.4153311931458959494, 3.850000000000006306, 0.5000000000000064393 ) ) ;
#1987=DIRECTION ( 'NONE',  ( 0.000000000000000000, 0.000000000000000000, -1.000000000000000000 ) ) ;
#2000=CARTESIAN_POINT ( 'NONE',  ( 1.364683531249996529, 13.71354166700806765, 0.7879004041258405033 ) ) ;
#2049=CARTESIAN_POINT ( 'NONE',  ( 1.364683531249997417, 12.23437500034139980, 2.602085213965210642E-15 ) ) ;
#2131=CARTESIAN_POINT ( 'NONE',  ( 1.500000000000001332, 10.65625000068279249, 0.000000000000000000 ) ) ;
#2145=CARTESIAN_POINT ( 'NONE',  ( -0.5368768833858145184, 13.37576698399828246, -1.254641125003840507 ) ) ;
#2189=DIRECTION ( 'NONE',  ( -0.8660254037844387076, 0.000000000000000000, -0.4999999999999999445 ) ) ;
#2197=CARTESIAN_POINT ( 'NONE',  ( 0.6823417656249969321, 11.02604166700806765, -1.181850606188757036 ) ) ;
#2350=CARTESIAN_POINT ( 'NONE',  ( -1.364683531250010295, 10.94270833367473372, 0.7879004041258445001 ) ) ;
#2416=CARTESIAN_POINT ( 'NONE',  ( 1.364683531250000303, 9.317708333674735499, -0.7879004041258355073 ) ) ;
#2434=EDGE_LOOP ( 'NONE', ( #151749, #136029 ) ) ;
#2436=ADVANCED_FACE ( 'NONE', ( #136210 ), #138343, .T. ) ;
#2456=CARTESIAN_POINT ( 'NONE',  ( 0.6823417656249969321, 15.02604166700806410, -1.181850606188757036 ) ) ;
#2477=B_SPLINE_CURVE_WITH_KNOTS ( 'NONE', 3,
 ( #116896, #51849, #151485, #213248 ),
 .UNSPECIFIED., .F., .F.,
 ( 4, 4 ),
 ( 0.001076902096689604481, 0.001673025196799804177 ),
 .UNSPECIFIED. ) ;
#2493=VECTOR ( 'NONE', #161029, 1000.000000000000000 ) ;
#2563=CARTESIAN_POINT ( 'NONE',  ( 0.4019237886466884846, 9.457585450998170273, -1.499999999999994449 ) ) ;
#2667=CARTESIAN_POINT ( 'NONE',  ( -1.364683531250010295, 13.44270833367473017, 0.7879004041258445001 ) ) ;
#2752=CARTESIAN_POINT ( 'NONE',  ( -0.4019237886467001974, 11.08258545099816494, 1.500000000000001998 ) ) ;
#2779=CARTESIAN_POINT ( 'NONE',  ( 0.4019237886466816012, 12.95758545099816850, -1.499999999999998668 ) ) ;
#2854=CARTESIAN_POINT ( 'NONE',  ( -1.364683531250014514, 11.58854166700806410, -0.7879004041258335089 ) ) ;
#2859=CARTESIAN_POINT ( 'NONE',  ( -1.500000000000015099, 10.22916666666667318, -0.8660254037844309360 ) ) ;
#2906=CARTESIAN_POINT ( 'NONE',  ( -1.402160292154681736E-14, 9.984375000341401574, 1.575800808251682339 ) ) ;
#2959=CARTESIAN_POINT ( 'NONE',  ( 1.220146605508150803E-14, 11.46875000068279604, -1.499999999999998446 ) ) ;
#2965=CARTESIAN_POINT ( 'NONE',  ( 1.499999999999996891, 8.645833333333337478, -0.8660254037844378194 ) ) ;
#2984=CARTESIAN_POINT ( 'NONE',  ( 1.500000000000001332, 13.15625000068279604, 0.000000000000000000 ) ) ;
#3016=( BOUNDED_CURVE ( )  B_SPLINE_CURVE ( 2, ( #161431, #140943, #193908, #209072, #208021, #73765, #108473, #206957, #124741 ),
 .UNSPECIFIED., .F., .T. ) 
 B_SPLINE_CURVE_WITH_KNOTS ( ( 3, 2, 2, 2, 3 ),
 ( 0.6875000000000000000, 0.6904761904761904656, 0.6964285714285713969, 0.7023809523809523281, 0.7053571428571427937 ),
 .UNSPECIFIED. ) 
 CURVE ( )  GEOMETRIC_REPRESENTATION_ITEM ( )  RATIONAL_B_SPLINE_CURVE ( ( 0.9330127018922194093, 0.9330127018922194093, 1.000000000000000000, 0.8660254037844387076, 1.000000000000000000, 0.8660254037844387076, 1.000000000000000000, 0.9330127018922206306, 0.9330127018922194093 ) ) 
 REPRESENTATION_ITEM ( '' )  );
#3030=CARTESIAN_POINT ( 'NONE',  ( 1.220146605508150803E-14, 11.21875000068279249, -1.499999999999998446 ) ) ;
#3068=CARTESIAN_POINT ( 'NONE',  ( 1.364683531250000303, 12.75520833367473550, -0.7879004041258355073 ) ) ;
#3077=EDGE_CURVE ( 'NONE', #80044, #196686, #78774, .T. ) ;
#3111=CARTESIAN_POINT ( 'NONE',  ( -0.7500000000000179856, 14.29166666666666785, 1.299038105676658228 ) ) ;
#3119=CARTESIAN_POINT ( 'NONE',  ( -0.6823417656250003738, 11.90104166700806054, 1.181850606188754593 ) ) ;
#3259=CARTESIAN_POINT ( 'NONE',  ( 0.4842345852037197029, 4.104600205398202917, 0.4350569428522614857 ) ) ;
#3269=CARTESIAN_POINT ( 'NONE',  ( -1.364683531250000748, 11.60937500034139802, 0.000000000000000000 ) ) ;
#3423=CARTESIAN_POINT ( 'NONE',  ( 0.6823417656249934904, 11.50520833367473017, 1.181850606188764807 ) ) ;
#3477=DIRECTION ( 'NONE',  ( 0.000000000000000000, -1.000000000000000000, 0.000000000000000000 ) ) ;
#3485=CARTESIAN_POINT ( 'NONE',  ( -1.364683531250010295, 9.192708333674733723, 0.7879004041258445001 ) ) ;
#3524=CARTESIAN_POINT ( 'NONE',  ( 1.499999999999997113, 8.677083334016131744, -0.8660254037844378194 ) ) ;
#3596=CARTESIAN_POINT ( 'NONE',  ( 1.500000000000001332, 10.62499999999999645, 0.000000000000000000 ) ) ;
#3624=ORIENTED_EDGE ( 'NONE', *, *, #28439, .T. ) ;
#3690=ORIENTED_EDGE ( 'NONE', *, *, #95199, .F. ) ;
#3711=CARTESIAN_POINT ( 'NONE',  ( 0.000000000000000000, 13.24045051524828231, 0.000000000000000000 ) ) ;
#3727=CARTESIAN_POINT ( 'NONE',  ( 1.499999999999993117, 12.85416666666666785, 0.8660254037844408170 ) ) ;
#3728=CARTESIAN_POINT ( 'NONE',  ( 1.364683531249997417, 13.29687500034139980, 2.602085213965210642E-15 ) ) ;
#3811=CARTESIAN_POINT ( 'NONE',  ( -0.7500000000000179856, 9.572916667349467446, 1.299038105676658228 ) ) ;
#3918=CARTESIAN_POINT ( 'NONE',  ( 0.6823417656249934904, 11.44270833367473728, 1.181850606188764807 ) ) ;
#3923=CARTESIAN_POINT ( 'NONE',  ( -1.500000000000001110, 9.770833333333333925, 0.8660254037844419273 ) ) ;
#3941=CARTESIAN_POINT ( 'NONE',  ( 0.4019237886466884846, 9.676335450315368902, -1.499999999999994449 ) ) ;
#3974=CARTESIAN_POINT ( 'NONE',  ( -8.012344526598182026E-15, 8.859375000341405126, -1.575800808251669460 ) ) ;
#4046=CARTESIAN_POINT ( 'NONE',  ( -5.000000000000009770, 3.850000000000006306, 6.071532165918824830E-15 ) ) ;
#4047=CARTESIAN_POINT ( 'NONE',  ( 0.7500000000000006661, 11.69791666734946389, -1.299038105676657340 ) ) ;
#4137=CARTESIAN_POINT ( 'NONE',  ( -1.364683531250000748, 13.35937500034139980, 0.000000000000000000 ) ) ;
#4158=CARTESIAN_POINT ( 'NONE',  ( 1.264911064067342217, 3.850000000000006306, -0.4999999999999987232 ) ) ;
#4180=CARTESIAN_POINT ( 'NONE',  ( -0.7500000000000179856, 13.79166666666666785, 1.299038105676658228 ) ) ;
#4187=CARTESIAN_POINT ( 'NONE',  ( -8.012344526598182026E-15, 11.29687500034139980, -1.575800808251669460 ) ) ;
#4233=CARTESIAN_POINT ( 'NONE',  ( -0.6823417656250039265, 13.13020833367473017, -1.181850606188755259 ) ) ;
#4330=CARTESIAN_POINT ( 'NONE',  ( -1.402160292154681736E-14, 11.67187500034140157, 1.575800808251682339 ) ) ;
#4477=CARTESIAN_POINT ( 'NONE',  ( -0.6823417656250003738, 10.96354166700806765, 1.181850606188754593 ) ) ;
#4503=CARTESIAN_POINT ( 'NONE',  ( -1.364683531250014514, 15.08854166700806587, -0.7879004041258335089 ) ) ;
#4544=CARTESIAN_POINT ( 'NONE',  ( -1.364683531250014514, 8.901041667008069425, -0.7879004041258335089 ) ) ;
#4549=AXIS2_PLACEMENT_3D ( 'NONE', #87469, #133041, #103722 ) ;
#4552=CARTESIAN_POINT ( 'NONE',  ( -1.355131232792150309, 3.768605237513072304, -0.6431325189496899242 ) ) ;
#4588=CARTESIAN_POINT ( 'NONE',  ( -1.402160292154681736E-14, 9.093750000682799595, 1.732050807568881190 ) ) ;
#4642=CONICAL_SURFACE ( 'NONE', #35902, 1.376945625684933061, 0.7853981633974491672 ) ;
#4729=CARTESIAN_POINT ( 'NONE',  ( -1.364683531250010295, 14.69270833367472839, 0.7879004041258445001 ) ) ;
#4762=CARTESIAN_POINT ( 'NONE',  ( 0.000000000000000000, 13.49999999999999822, -1.500000000000000222 ) ) ;
#4787=CARTESIAN_POINT ( 'NONE',  ( -1.364683531250010295, 13.69270833367473195, 0.7879004041258445001 ) ) ;
#4896=CARTESIAN_POINT ( 'NONE',  ( -1.280216254274686216, 4.017177813915858486, 0.4723901200327987882 ) ) ;
#4904=VECTOR ( 'NONE', #61668, 1000.000000000000000 ) ;
#4966=ORIENTED_EDGE ( 'NONE', *, *, #114112, .F. ) ;
#4978=CARTESIAN_POINT ( 'NONE',  ( -1.364683531250010740, 12.13020833367473195, 0.7879004041258445001 ) ) ;
#4985=CARTESIAN_POINT ( 'NONE',  ( -1.402160292154681736E-14, 9.562499999999998224, 1.732050807568881190 ) ) ;
#5038=CARTESIAN_POINT ( 'NONE',  ( -1.364683531250010740, 9.692708333674737275, 0.7879004041258445001 ) ) ;
#5069=ORIENTED_EDGE ( 'NONE', *, *, #8140, .T. ) ;
#5165=EDGE_CURVE ( 'NONE', #213528, #98728, #14689, .T. ) ;
#5198=CARTESIAN_POINT ( 'NONE',  ( 3.834746474454188013E-15, 12.56250000000000178, 1.500000000000001554 ) ) ;
#5199=CARTESIAN_POINT ( 'NONE',  ( 1.364683531249996529, 12.71354166700806232, 0.7879004041258405033 ) ) ;
#5220=CARTESIAN_POINT ( 'NONE',  ( 0.5773502691896124084, -2.500000000000002220, -0.9999999999999991118 ) ) ;
#5242=CARTESIAN_POINT ( 'NONE',  ( 1.500000000000001332, 14.12499999999999822, 0.000000000000000000 ) ) ;
#5249=CARTESIAN_POINT ( 'NONE',  ( 1.364683531249996529, 11.71354166700806587, 0.7879004041258405033 ) ) ;
#5293=CARTESIAN_POINT ( 'NONE',  ( -1.364683531250014514, 13.15104166700806410, -0.7879004041258335089 ) ) ;
#5298=CARTESIAN_POINT ( 'NONE',  ( -1.500000000000015099, 12.26041666734946212, -0.8660254037844309360 ) ) ;
#5318=CARTESIAN_POINT ( 'NONE',  ( -0.6823417656250039265, 12.81770833367473017, -1.181850606188755259 ) ) ;
#5336=FACE_OUTER_BOUND ( 'NONE', #168055, .T. ) ;
#5358=CARTESIAN_POINT ( 'NONE',  ( 1.499999999999993117, 14.63541666734946567, 0.8660254037844409281 ) ) ;
#5395=CARTESIAN_POINT ( 'NONE',  ( -0.6823417656250003738, 10.90104166700806765, 1.181850606188754593 ) ) ;
#5428=CARTESIAN_POINT ( 'NONE',  ( 0.7144793466747193511, 13.35177634501765453, -1.205057194458958314 ) ) ;
#5477=CARTESIAN_POINT ( 'NONE',  ( 0.000000000000000000, 13.49999999999999822, -1.500000000000000222 ) ) ;
#5542=CARTESIAN_POINT ( 'NONE',  ( -1.364683531250010295, 10.44270833367473017, 0.7879004041258445001 ) ) ;
#5556=( BOUNDED_CURVE ( )  B_SPLINE_CURVE ( 2, ( #9884, #108526, #26132, #124797, #56515, #92244, #158293, #10936, #143139 ),
 .UNSPECIFIED., .F., .T. ) 
 B_SPLINE_CURVE_WITH_KNOTS ( ( 3, 2, 2, 2, 3 ),
 ( 0.7232142857142856984, 0.7261904761904761640, 0.7321428571428570953, 0.7380952380952381375, 0.7410714285714286031 ),
 .UNSPECIFIED. ) 
 CURVE ( )  GEOMETRIC_REPRESENTATION_ITEM ( )  RATIONAL_B_SPLINE_CURVE ( ( 0.9330127018922194093, 0.9330127018922194093, 1.000000000000000000, 0.8660254037844387076, 1.000000000000000000, 0.8660254037844387076, 1.000000000000000000, 0.9330127018922194093, 0.9330127018922194093 ) ) 
 REPRESENTATION_ITEM ( '' )  );
#5568=CARTESIAN_POINT ( 'NONE',  ( -0.6823417656250039265, 14.31770833367473195, -1.181850606188755259 ) ) ;
#5587=VERTEX_POINT ( 'NONE', #46877 ) ;
#5599=CARTESIAN_POINT ( 'NONE',  ( 0.000000000000000000, 13.49999999999999822, 0.000000000000000000 ) ) ;
#5607=CARTESIAN_POINT ( 'NONE',  ( 1.364683531249997417, 8.546875000341403350, 2.602085213965210642E-15 ) ) ;
#5620=ORIENTED_EDGE ( 'NONE', *, *, #66894, .F. ) ;
#5653=CARTESIAN_POINT ( 'NONE',  ( 1.364683531249996529, 15.21354166700806587, 0.7879004041258405033 ) ) ;
#5665=CARTESIAN_POINT ( 'NONE',  ( -1.273593037966616048, 3.712960547652722987, -0.4852599168373451510 ) ) ;
#5690=DIRECTION ( 'NONE',  ( 0.000000000000000000, 1.000000000000000000, 0.000000000000000000 ) ) ;
#5798=CARTESIAN_POINT ( 'NONE',  ( -8.012344526598182026E-15, 14.60937500034139980, -1.575800808251669460 ) ) ;
#5865=CARTESIAN_POINT ( 'NONE',  ( -8.012344526598182026E-15, 12.85937500034139802, -1.575800808251669460 ) ) ;
#5890=EDGE_CURVE ( 'NONE', #194295, #36526, #196032, .T. ) ;
#5900=DIRECTION ( 'NONE',  ( 1.000000000000000000, 0.000000000000000000, 0.000000000000000000 ) ) ;
#5992=CARTESIAN_POINT ( 'NONE',  ( -1.264911064067356206, 3.967544000579928287, -0.5000000000000004441 ) ) ;
#6035=CARTESIAN_POINT ( 'NONE',  ( 0.000000000000000000, 13.49999999999999822, 0.000000000000000000 ) ) ;
#6042=DIRECTION ( 'NONE',  ( 0.000000000000000000, 0.000000000000000000, -1.000000000000000000 ) ) ;
#6060=CARTESIAN_POINT ( 'NONE',  ( -1.402160292154681736E-14, 12.17187500034140513, 1.575800808251682339 ) ) ;
#6067=CARTESIAN_POINT ( 'NONE',  ( -0.7500000000000006661, 9.708333333333332149, -1.299038105676657340 ) ) ;
#6085=CARTESIAN_POINT ( 'NONE',  ( -0.7500000000000179856, 8.822916667349467446, 1.299038105676658228 ) ) ;
#6100=EDGE_LOOP ( 'NONE', ( #55948, #47799, #113647, #88196 ) ) ;
#6115=CARTESIAN_POINT ( 'NONE',  ( -1.364683531250000748, 9.671875000341396245, 0.000000000000000000 ) ) ;
#6130=CARTESIAN_POINT ( 'NONE',  ( -0.4019237886466966447, 12.58258545099816850, 1.500000000000003997 ) ) ;
#6165=CARTESIAN_POINT ( 'NONE',  ( 0.000000000000000000, -1.500000000000001332, 0.000000000000000000 ) ) ;
#6174=CARTESIAN_POINT ( 'NONE',  ( -1.115562610750309283E-14, 9.343750000682801371, 1.500000000000001554 ) ) ;
#6196=DIRECTION ( 'NONE',  ( 0.000000000000000000, -1.000000000000000000, 0.000000000000000000 ) ) ;
#6323=CARTESIAN_POINT ( 'NONE',  ( 0.7500000000000006661, 13.66666666666666785, -1.299038105676657340 ) ) ;
#6329=CARTESIAN_POINT ( 'NONE',  ( 0.6823417656249969321, 10.52604166700806587, -1.181850606188757036 ) ) ;
#6377=CARTESIAN_POINT ( 'NONE',  ( 1.364683531249997417, 12.79687500034139980, 2.602085213965210642E-15 ) ) ;
#6382=CYLINDRICAL_SURFACE ( 'NONE', #89337, 0.6500000000000000222 ) ;
#6403=CARTESIAN_POINT ( 'NONE',  ( -0.6823417656250039265, 13.31770833367473195, -1.181850606188755259 ) ) ;
#6460=ORIENTED_EDGE ( 'NONE', *, *, #38859, .F. ) ;
#6475=CARTESIAN_POINT ( 'NONE',  ( 0.6823417656249969321, 10.52604166700806587, -1.181850606188757036 ) ) ;
#6481=CARTESIAN_POINT ( 'NONE',  ( 0.000000000000000000, -4.500000000000003553, 0.000000000000000000 ) ) ;
#6625=CARTESIAN_POINT ( 'NONE',  ( -1.364683531250000748, 10.67187500034139802, 0.000000000000000000 ) ) ;
#6653=CARTESIAN_POINT ( 'NONE',  ( -0.6823417656250003738, 14.90104166700806410, 1.181850606188754593 ) ) ;
#6696=CARTESIAN_POINT ( 'NONE',  ( -0.6823417656250039265, 8.630208333674733723, -1.181850606188755259 ) ) ;
#6710=CARTESIAN_POINT ( 'NONE',  ( 1.264911064067342217, 3.850000000000006306, -0.4999999999999987232 ) ) ;
#6737=CARTESIAN_POINT ( 'NONE',  ( 1.364683531249997417, 14.98437500034140157, 2.602085213965210642E-15 ) ) ;
#6749=LINE ( 'NONE', #125947, #173657 ) ;
#6876=CARTESIAN_POINT ( 'NONE',  ( -1.364683531250010295, 15.19270833367472839, 0.7879004041258445001 ) ) ;
#6884=CARTESIAN_POINT ( 'NONE',  ( 1.499999999999993117, 12.38541666734946212, 0.8660254037844408170 ) ) ;
#6911=DIRECTION ( 'NONE',  ( 1.000000000000000000, 0.000000000000000000, 0.000000000000000000 ) ) ;
#6936=CARTESIAN_POINT ( 'NONE',  ( -0.6823417656250003738, 13.21354166700806942, 1.181850606188754593 ) ) ;
#6982=CARTESIAN_POINT ( 'NONE',  ( -0.9174905902287084913, -4.140925090156245325, 0.4108596822575558694 ) ) ;
#7108=CARTESIAN_POINT ( 'NONE',  ( 0.7500000000000006661, 8.833333333333332149, 1.299038105676657340 ) ) ;
#7118=CARTESIAN_POINT ( 'NONE',  ( 0.000000000000000000, -1.500000000000001332, 0.000000000000000000 ) ) ;
#7128=CARTESIAN_POINT ( 'NONE',  ( -1.364683531250010740, 10.38020833367473017, 0.7879004041258445001 ) ) ;
#7130=EDGE_CURVE ( 'NONE', #65269, #32497, #48810, .T. ) ;
#7135=CARTESIAN_POINT ( 'NONE',  ( 1.499999999999993117, 9.604166666666669627, 0.8660254037844409281 ) ) ;
#7355=FACE_OUTER_BOUND ( 'NONE', #24652, .T. ) ;
#7393=CARTESIAN_POINT ( 'NONE',  ( 1.499999999999993117, 13.10416666666666963, 0.8660254037844409281 ) ) ;
#7398=CARTESIAN_POINT ( 'NONE',  ( -1.402160292154681736E-14, 10.67187500034139624, 1.575800808251682339 ) ) ;
#7421=ADVANCED_FACE ( 'NONE', ( #105027 ), #121341, .T. ) ;
#7473=CARTESIAN_POINT ( 'NONE',  ( -1.364683531250000748, 12.85937500034139980, 0.000000000000000000 ) ) ;
#7505=LINE ( 'NONE', #41118, #127825 ) ;
#7545=CARTESIAN_POINT ( 'NONE',  ( -8.012344526598182026E-15, 10.29687500034139447, -1.575800808251669460 ) ) ;
#7548=CARTESIAN_POINT ( 'NONE',  ( -2.788906526875773208E-15, 13.21875000068279427, -1.499999999999998446 ) ) ;
#7551=DIRECTION ( 'NONE',  ( 0.000000000000000000, -1.000000000000000000, 0.000000000000000000 ) ) ;
#7601=ORIENTED_EDGE ( 'NONE', *, *, #10916, .T. ) ;
#7653=CARTESIAN_POINT ( 'NONE',  ( -1.286813488861823895, 3.652992958535467238, -0.4595522011843558574 ) ) ;
#7695=CARTESIAN_POINT ( 'NONE',  ( 1.364683531249997417, 9.046875000341403350, 2.602085213965210642E-15 ) ) ;
#7699=ORIENTED_EDGE ( 'NONE', *, *, #116206, .F. ) ;
#7717=CARTESIAN_POINT ( 'NONE',  ( 0.5993104169204894749, 3.417580942362360652, 0.2596433605236490028 ) ) ;
#7718=CARTESIAN_POINT ( 'NONE',  ( 0.7500000000000006661, 9.197916667349467446, -1.299038105676657340 ) ) ;
#7722=CARTESIAN_POINT ( 'NONE',  ( -8.012344526598182026E-15, 14.54687500034139802, -1.575800808251669460 ) ) ;
#7763=CARTESIAN_POINT ( 'NONE',  ( 1.499999999999997113, 14.39583333333333215, -0.8660254037844378194 ) ) ;
#7781=ORIENTED_EDGE ( 'NONE', *, *, #172733, .T. ) ;
#7798=CIRCLE ( 'NONE', #211895, 2.000000000000000000 ) ;
#7809=CARTESIAN_POINT ( 'NONE',  ( -0.6823417656250003738, 14.40104166700806232, 1.181850606188754593 ) ) ;
#7845=CARTESIAN_POINT ( 'NONE',  ( 0.6681007961515190718, -4.204658361605604355, -0.8428154764883271088 ) ) ;
#7953=CARTESIAN_POINT ( 'NONE',  ( 0.6823417656249969321, 14.58854166700806410, -1.181850606188757036 ) ) ;
#8016=DIRECTION ( 'NONE',  ( 0.000000000000000000, 0.000000000000000000, -1.000000000000000000 ) ) ;
#8017=CARTESIAN_POINT ( 'NONE',  ( 1.364683531249996529, 11.52604166700806410, 0.7879004041258405033 ) ) ;
#8064=CARTESIAN_POINT ( 'NONE',  ( -1.500000000000015099, 11.51041666734946567, -0.8660254037844309360 ) ) ;
#8140=EDGE_CURVE ( 'NONE', #170253, #33524, #144837, .T. ) ;
#8211=CARTESIAN_POINT ( 'NONE',  ( 1.364683531249996529, 10.21354166700806587, 0.7879004041258403923 ) ) ;
#8217=CARTESIAN_POINT ( 'NONE',  ( -1.500000000000008216, 8.500000000000000000, 3.469446951953614189E-15 ) ) ;
#8228=ORIENTED_EDGE ( 'NONE', *, *, #1351, .F. ) ;
#8253=VERTEX_POINT ( 'NONE', #161341 ) ;
#8270=CARTESIAN_POINT ( 'NONE',  ( 1.364683531249996529, 8.526041667008065872, 0.7879004041258403923 ) ) ;
#8330=ORIENTED_EDGE ( 'NONE', *, *, #26436, .T. ) ;
#8340=AXIS2_PLACEMENT_3D ( 'NONE', #99507, #202026, #32373 ) ;
#8401=DIRECTION ( 'NONE',  ( 0.000000000000000000, 0.000000000000000000, 1.000000000000000000 ) ) ;
#8413=CARTESIAN_POINT ( 'NONE',  ( 0.4019237886466814902, 12.60491455036742892, 1.499999999999999334 ) ) ;
#8420=VECTOR ( 'NONE', #46689, 1000.000000000000000 ) ;
#8460=AXIS2_PLACEMENT_3D ( 'NONE', #77835, #191573, #142885 ) ;
#8470=CARTESIAN_POINT ( 'NONE',  ( 1.499999999999993117, 12.35416666666666785, 0.8660254037844409281 ) ) ;
#8475=AXIS2_PLACEMENT_3D ( 'NONE', #93523, #110881, #193126 ) ;
#8476=CARTESIAN_POINT ( 'NONE',  ( -1.364683531250000748, 10.60937500034139802, 0.000000000000000000 ) ) ;
#8522=CARTESIAN_POINT ( 'NONE',  ( 0.6823417656249969321, 12.58854166700806942, -1.181850606188757036 ) ) ;
#8534=DIRECTION ( 'NONE',  ( 0.000000000000000000, -1.000000000000000000, 0.000000000000000000 ) ) ;
#8551=CARTESIAN_POINT ( 'NONE',  ( 1.364683531249996529, 12.71354166700806232, 0.7879004041258403923 ) ) ;
#8590=ORIENTED_EDGE ( 'NONE', *, *, #71115, .F. ) ;
#8621=CARTESIAN_POINT ( 'NONE',  ( -8.012344526598182026E-15, 10.04687500034140335, -1.575800808251669460 ) ) ;
#8679=VERTEX_POINT ( 'NONE', #29497 ) ;
#8775=CARTESIAN_POINT ( 'NONE',  ( -1.402160292154681736E-14, 9.734375000341399797, 1.575800808251682339 ) ) ;
#8800=CARTESIAN_POINT ( 'NONE',  ( 0.6823417656249969321, 14.52604166700806410, -1.181850606188757036 ) ) ;
#8835=CARTESIAN_POINT ( 'NONE',  ( 0.2026985623045176044, -4.140708350189164832, 1.000000000000004441 ) ) ;
#8843=CARTESIAN_POINT ( 'NONE',  ( -0.7500000000000179856, 14.79166666666666785, 1.299038105676658228 ) ) ;
#8886=CARTESIAN_POINT ( 'NONE',  ( 0.6823417656249934904, 14.44270833367473195, 1.181850606188764807 ) ) ;
#8919=( BOUNDED_CURVE ( )  B_SPLINE_CURVE ( 2, ( #6174, #187074, #72243, #201173, #52812, #36553, #70102, #204367, #193214 ),
 .UNSPECIFIED., .F., .T. ) 
 B_SPLINE_CURVE_WITH_KNOTS ( ( 3, 2, 2, 2, 3 ),
 ( 0.8482142857142856984, 0.8511904761904761640, 0.8571428571428570953, 0.8630952380952381375, 0.8660714285714286031 ),
 .UNSPECIFIED. ) 
 CURVE ( )  GEOMETRIC_REPRESENTATION_ITEM ( )  RATIONAL_B_SPLINE_CURVE ( ( 0.9330127018922194093, 0.9330127018922194093, 1.000000000000000000, 0.8660254037844387076, 1.000000000000000000, 0.8660254037844387076, 1.000000000000000000, 0.9330127018922194093, 0.9330127018922194093 ) ) 
 REPRESENTATION_ITEM ( '' )  );
#9036=CARTESIAN_POINT ( 'NONE',  ( 1.364683531249997417, 14.04687500034140157, 2.602085213965210642E-15 ) ) ;
#9100=CARTESIAN_POINT ( 'NONE',  ( 0.6823417656249969321, 12.33854166700806765, -1.181850606188757036 ) ) ;
#9142=CARTESIAN_POINT ( 'NONE',  ( -0.7500000000000006661, 11.73958333401613174, -1.299038105676657340 ) ) ;
#9233=ORIENTED_EDGE ( 'NONE', *, *, #114075, .F. ) ;
#9268=CARTESIAN_POINT ( 'NONE',  ( 1.346456596051760490, 4.237728335763024212, -0.3357819570988694324 ) ) ;
#9286=CARTESIAN_POINT ( 'NONE',  ( -1.364683531250000748, 10.10937500034139802, 0.000000000000000000 ) ) ;
#9291=LINE ( 'NONE', #50065, #127123 ) ;
#9292=CARTESIAN_POINT ( 'NONE',  ( 1.500000000000001332, 8.625000000000000000, 0.000000000000000000 ) ) ;
#9315=CARTESIAN_POINT ( 'NONE',  ( -1.500000000000001110, 8.552083334016133520, 0.8660254037844418162 ) ) ;
#9331=EDGE_CURVE ( 'NONE', #83117, #147564, #190323, .T. ) ;
#9356=CARTESIAN_POINT ( 'NONE',  ( -0.6823417656250039265, 15.13020833367473372, -1.181850606188755259 ) ) ;
#9383=CARTESIAN_POINT ( 'NONE',  ( -5.000000000000009770, 3.850000000000006306, 6.071532165918824830E-15 ) ) ;
#9464=ADVANCED_FACE ( 'NONE', ( #163329 ), #14909, .F. ) ;
#9489=CARTESIAN_POINT ( 'NONE',  ( 1.499999999999996891, 12.67708333401612819, -0.8660254037844378194 ) ) ;
#9546=CARTESIAN_POINT ( 'NONE',  ( -1.402160292154681736E-14, 12.06250000000000000, 1.732050807568881190 ) ) ;
#9552=CARTESIAN_POINT ( 'NONE',  ( -0.6823417656250003738, 10.40104166700806587, 1.181850606188754593 ) ) ;
#9568=DIRECTION ( 'NONE',  ( 0.000000000000000000, -1.000000000000000000, 0.000000000000000000 ) ) ;
#9591=CARTESIAN_POINT ( 'NONE',  ( 1.364683531249997417, 12.29687500034139980, 2.602085213965210642E-15 ) ) ;
#9604=EDGE_CURVE ( 'NONE', #110599, #80954, #96640, .T. ) ;
#9633=EDGE_LOOP ( 'NONE', ( #44582, #185136, #40205, #131913 ) ) ;
#9657=CARTESIAN_POINT ( 'NONE',  ( -1.500000000000015099, 15.01041666734946745, -0.8660254037844309360 ) ) ;
#9665=FACE_OUTER_BOUND ( 'NONE', #177141, .T. ) ;
#9691=CARTESIAN_POINT ( 'NONE',  ( 1.364683531249996529, 10.96354166700806942, 0.7879004041258405033 ) ) ;
#9694=ORIENTED_EDGE ( 'NONE', *, *, #165975, .F. ) ;
#9733=EDGE_LOOP ( 'NONE', ( #177182, #32572, #185276, #212455 ) ) ;
#9741=ORIENTED_EDGE ( 'NONE', *, *, #193016, .T. ) ;
#9762=ORIENTED_EDGE ( 'NONE', *, *, #15859, .F. ) ;
#9841=CARTESIAN_POINT ( 'NONE',  ( -1.364683531250000748, 10.17187500034139802, 0.000000000000000000 ) ) ;
#9842=ADVANCED_FACE ( 'NONE', ( #11482 ), #92316, .T. ) ;
#9850=DIRECTION ( 'NONE',  ( 0.000000000000000000, 0.000000000000000000, -1.000000000000000000 ) ) ;
#9884=CARTESIAN_POINT ( 'NONE',  ( -2.788906526875773208E-15, 10.43750000000000000, -1.499999999999998446 ) ) ;
#9898=AXIS2_PLACEMENT_3D ( 'NONE', #102502, #183747, #6042 ) ;
#9902=CARTESIAN_POINT ( 'NONE',  ( -0.7500000000000006661, 12.98958333401613352, -1.299038105676657340 ) ) ;
#9910=CARTESIAN_POINT ( 'NONE',  ( -0.7500000000000179856, 15.29166666666666785, 1.299038105676658228 ) ) ;
#9953=CARTESIAN_POINT ( 'NONE',  ( -1.364683531250000748, 14.60937500034140157, 0.000000000000000000 ) ) ;
#9994=CARTESIAN_POINT ( 'NONE',  ( -1.274579945453880425, 3.984756441945468630, 0.4827076737218306546 ) ) ;
#10001=EDGE_LOOP ( 'NONE', ( #60368, #63576, #62075, #112237 ) ) ;
#10070=CARTESIAN_POINT ( 'NONE',  ( 1.264548378739733581, 3.788599454610471984, -0.5006372017796714147 ) ) ;
#10095=CARTESIAN_POINT ( 'NONE',  ( 0.6823417656249969321, 13.83854166700806942, -1.181850606188757036 ) ) ;
#10158=CARTESIAN_POINT ( 'NONE',  ( 0.6823417656249969321, 12.08854166700806765, -1.181850606188757036 ) ) ;
#10196=CARTESIAN_POINT ( 'NONE',  ( -0.4019237886466871523, 11.19866454968462754, -1.499999999999998668 ) ) ;
#10201=CARTESIAN_POINT ( 'NONE',  ( 1.499999999999997113, 11.17708333401612819, -0.8660254037844378194 ) ) ;
#10302=CARTESIAN_POINT ( 'NONE',  ( 1.500236433942635950, 4.350729682706125701, -0.06629318219673785428 ) ) ;
#10321=CARTESIAN_POINT ( 'NONE',  ( -1.265299903344048404, 3.920951693072811661, 0.4993168358707228971 ) ) ;
#10336=CARTESIAN_POINT ( 'NONE',  ( -8.012344526598182026E-15, 11.29687500034139980, -1.575800808251669460 ) ) ;
#10343=CARTESIAN_POINT ( 'NONE',  ( 1.499999999999993117, 8.854166666666667851, 0.8660254037844409281 ) ) ;
#10599=CARTESIAN_POINT ( 'NONE',  ( -6.009258394948636914E-15, 11.93750000000000000, -1.732050807568875195 ) ) ;
#10605=CARTESIAN_POINT ( 'NONE',  ( -8.012344526598182026E-15, 10.04687500034140335, -1.575800808251669460 ) ) ;
#10616=CARTESIAN_POINT ( 'NONE',  ( -0.4019237886466871523, 10.72991455036742892, -1.499999999999998668 ) ) ;
#10641=CARTESIAN_POINT ( 'NONE',  ( 1.364683531250000748, 11.56770833367472839, -0.7879004041258355073 ) ) ;
#10648=CARTESIAN_POINT ( 'NONE',  ( 0.4019237886466778820, 9.823664549684629321, 1.500000000000001554 ) ) ;
#10666=DIRECTION ( 'NONE',  ( 0.000000000000000000, -1.000000000000000000, 0.000000000000000000 ) ) ;
#10716=CARTESIAN_POINT ( 'NONE',  ( -1.500000000000008216, 13.28125000068279604, 3.469446951953614189E-15 ) ) ;
#10749=CARTESIAN_POINT ( 'NONE',  ( -8.012344526598182026E-15, 9.046875000341405126, -1.575800808251669460 ) ) ;
#10846=CARTESIAN_POINT ( 'NONE',  ( 0.000000000000000000, 13.49999999999999822, 0.000000000000000000 ) ) ;
#10894=CARTESIAN_POINT ( 'NONE',  ( 1.364683531249997417, 9.546875000341396245, 2.602085213965210642E-15 ) ) ;
#10906=ORIENTED_EDGE ( 'NONE', *, *, #83416, .F. ) ;
#10916=EDGE_CURVE ( 'NONE', #14542, #45069, #56199, .T. ) ;
#10936=CARTESIAN_POINT ( 'NONE',  ( 0.4019237886466778820, 10.32366454968463110, 1.500000000000001554 ) ) ;
#10965=CARTESIAN_POINT ( 'NONE',  ( -6.009258394948636914E-15, 14.68749999999999822, -1.732050807568875195 ) ) ;
#10970=ADVANCED_FACE ( 'NONE', ( #74584 ), #140687, .T. ) ;
#10988=LINE ( 'NONE', #28323, #73718 ) ;
#11009=CARTESIAN_POINT ( 'NONE',  ( -1.402160292154681736E-14, 13.92187500034139624, 1.575800808251682339 ) ) ;
#11110=CARTESIAN_POINT ( 'NONE',  ( -1.364643601765285208, 3.684187268283338312, 0.6238217115099010668 ) ) ;
#11129=CARTESIAN_POINT ( 'NONE',  ( 1.273593037967014618, 3.987039452347238999, -0.4852599168373658567 ) ) ;
#11152=CARTESIAN_POINT ( 'NONE',  ( -1.364683531250014514, 14.15104166700806765, -0.7879004041258335089 ) ) ;
#11208=DIRECTION ( 'NONE',  ( 0.000000000000000000, 0.000000000000000000, -1.000000000000000000 ) ) ;
#11219=CARTESIAN_POINT ( 'NONE',  ( -1.364683531250010295, 11.19270833367473550, 0.7879004041258445001 ) ) ;
#11260=CARTESIAN_POINT ( 'NONE',  ( -1.500000000000001110, 11.27083333333333393, 0.8660254037844418162 ) ) ;
#11265=CARTESIAN_POINT ( 'NONE',  ( -1.402160292154681736E-14, 10.84375000068279782, 1.732050807568881190 ) ) ;
#11274=CARTESIAN_POINT ( 'NONE',  ( 1.500000000000001332, 10.15625000068279249, 0.000000000000000000 ) ) ;
#11364=FACE_OUTER_BOUND ( 'NONE', #112380, .T. ) ;
#11365=CARTESIAN_POINT ( 'NONE',  ( 1.423138288543973617, 3.789741015373900623, 0.4995221786828039634 ) ) ;
#11385=CARTESIAN_POINT ( 'NONE',  ( -1.443823057115803055, 3.571423696980855489, 0.4219843264275927597 ) ) ;
#11403=CARTESIAN_POINT ( 'NONE',  ( -1.364683531250010740, 9.380208333674735499, 0.7879004041258445001 ) ) ;
#11421=EDGE_LOOP ( 'NONE', ( #161579, #41739, #186545, #14360, #111637, #203733, #125969, #131833 ) ) ;
#11482=FACE_OUTER_BOUND ( 'NONE', #131641, .T. ) ;
#11553=( NAMED_UNIT ( * ) PLANE_ANGLE_UNIT ( ) SI_UNIT ( $, .RADIAN. ) );
#11612=CARTESIAN_POINT ( 'NONE',  ( 1.499999999999993117, 12.63541666734946389, 0.8660254037844408170 ) ) ;
#11670=CARTESIAN_POINT ( 'NONE',  ( -1.500000000000008216, 12.49999999999999645, 3.469446951953614189E-15 ) ) ;
#11675=CARTESIAN_POINT ( 'NONE',  ( -1.402160292154681736E-14, 9.421875000341398021, 1.575800808251682339 ) ) ;
#11714=CARTESIAN_POINT ( 'NONE',  ( -1.364683531250010740, 11.69270833367473017, 0.7879004041258445001 ) ) ;
#11721=ORIENTED_EDGE ( 'NONE', *, *, #154961, .T. ) ;
#11783=CARTESIAN_POINT ( 'NONE',  ( 0.7500000000000006661, 13.94791666734946567, -1.299038105676657340 ) ) ;
#11817=CARTESIAN_POINT ( 'NONE',  ( -1.364683531250000748, 8.859375000341396245, 0.000000000000000000 ) ) ;
#11824=FACE_OUTER_BOUND ( 'NONE', #161814, .T. ) ;
#11826=LINE ( 'NONE', #162373, #194839 ) ;
#11860=ORIENTED_EDGE ( 'NONE', *, *, #78658, .T. ) ;
#11879=VERTEX_POINT ( 'NONE', #172756 ) ;
#11970=CARTESIAN_POINT ( 'NONE',  ( -1.364683531250000748, 9.171875000341403350, 0.000000000000000000 ) ) ;
#12044=CYLINDRICAL_SURFACE ( 'NONE', #201574, 1.500000000000000222 ) ;
#12059=ORIENTED_EDGE ( 'NONE', *, *, #111106, .T. ) ;
#12066=DIRECTION ( 'NONE',  ( 0.000000000000000000, -1.000000000000000000, 0.000000000000000000 ) ) ;
#12086=CARTESIAN_POINT ( 'NONE',  ( 0.6823417656249934904, 13.44270833367473195, 1.181850606188764807 ) ) ;
#12088=ORIENTED_EDGE ( 'NONE', *, *, #192671, .F. ) ;
#12203=CARTESIAN_POINT ( 'NONE',  ( 1.500267808745624709, 3.349173475877287753, 0.06648599600050619784 ) ) ;
#12225=CARTESIAN_POINT ( 'NONE',  ( 1.364683531249996529, 13.52604166700806587, 0.7879004041258405033 ) ) ;
#12283=CARTESIAN_POINT ( 'NONE',  ( 1.364683531249997417, 11.54687500034139802, 2.602085213965210642E-15 ) ) ;
#12327=CARTESIAN_POINT ( 'NONE',  ( 0.7500000000000006661, 9.614583334016129967, 1.299038105676657340 ) ) ;
#12380=CARTESIAN_POINT ( 'NONE',  ( -0.5151611981367305582, 4.156673609434548666, -0.3998388334338457972 ) ) ;
#12429=CARTESIAN_POINT ( 'NONE',  ( 1.494007359806955204, 4.332045425165421904, 0.1499524099050986436 ) ) ;
#12450=CARTESIAN_POINT ( 'NONE',  ( -1.315333408008317884, 3.546208470693949621, 0.4024190470832751387 ) ) ;
#12453=VECTOR ( 'NONE', #107570, 1000.000000000000000 ) ;
#12471=CARTESIAN_POINT ( 'NONE',  ( -0.6823417656250039265, 9.567708333674735499, -1.181850606188755259 ) ) ;
#12474=MANIFOLD_SOLID_BREP ( 'Fillet1', #43064 ) ;
#12478=CARTESIAN_POINT ( 'NONE',  ( 0.7500000000000006661, 8.916666666666669627, -1.299038105676657340 ) ) ;
#12710=CARTESIAN_POINT ( 'NONE',  ( 4.764381983412778688E-15, 12.71875000068279782, -1.499999999999998446 ) ) ;
#12727=CARTESIAN_POINT ( 'NONE',  ( -1.500000000000015099, 12.47916666666666607, -0.8660254037844309360 ) ) ;
#12732=CARTESIAN_POINT ( 'NONE',  ( -1.364683531250000748, 9.859375000341398021, 0.000000000000000000 ) ) ;
#12768=CARTESIAN_POINT ( 'NONE',  ( -1.364683531250014514, 10.65104166700806942, -0.7879004041258335089 ) ) ;
#12840=CARTESIAN_POINT ( 'NONE',  ( 0.7500000000000006661, 14.44791666734946567, -1.299038105676657340 ) ) ;
#12875=CARTESIAN_POINT ( 'NONE',  ( 1.364683531249996529, 8.463541667008065872, 0.7879004041258405033 ) ) ;
#12932=VERTEX_POINT ( 'NONE', #61944 ) ;
#13029=CARTESIAN_POINT ( 'NONE',  ( -0.6823417656250003738, 8.963541667008065872, 1.181850606188754593 ) ) ;
#13040=CARTESIAN_POINT ( 'NONE',  ( 1.279995097189621012, 4.016078936648800557, -0.4728108786798641550 ) ) ;
#13149=CARTESIAN_POINT ( 'NONE',  ( 1.364683531249996529, 12.71354166700806232, 0.7879004041258405033 ) ) ;
#13161=CARTESIAN_POINT ( 'NONE',  ( -1.445379498298575260, 4.137219402008315505, 0.4160626371120850209 ) ) ;
#13203=ORIENTED_EDGE ( 'NONE', *, *, #212409, .T. ) ;
#13220=ORIENTED_EDGE ( 'NONE', *, *, #116206, .T. ) ;
#13270=ORIENTED_EDGE ( 'NONE', *, *, #5165, .T. ) ;
#13278=CARTESIAN_POINT ( 'NONE',  ( 1.400363088670474765, 3.349293939923656982, 0.06128031220414761893 ) ) ;
#13301=CARTESIAN_POINT ( 'NONE',  ( -0.6823417656250003738, 14.21354166700806232, 1.181850606188754593 ) ) ;
#13340=ORIENTED_EDGE ( 'NONE', *, *, #3077, .F. ) ;
#13362=CARTESIAN_POINT ( 'NONE',  ( 1.364683531249996529, 10.52604166700806765, 0.7879004041258405033 ) ) ;
#13376=DIRECTION ( 'NONE',  ( 0.000000000000000000, 0.000000000000000000, -1.000000000000000000 ) ) ;
#13402=CARTESIAN_POINT ( 'NONE',  ( 1.499999999999993117, 9.885416667349465669, 0.8660254037844409281 ) ) ;
#13412=CARTESIAN_POINT ( 'NONE',  ( 0.7500000000000006661, 10.19791666734946922, -1.299038105676657340 ) ) ;
#13496=ADVANCED_FACE ( 'NONE', ( #24422 ), #171764, .T. ) ;
#13507=CARTESIAN_POINT ( 'NONE',  ( 1.399654745096419406, 4.349328649162782057, 0.07090406488317976819 ) ) ;
#13527=CARTESIAN_POINT ( 'NONE',  ( -1.273728293839776926, 3.987841871246060155, 0.4850152072975402739 ) ) ;
#13528=EDGE_CURVE ( 'NONE', #102754, #127955, #202955, .T. ) ;
#13545=CARTESIAN_POINT ( 'NONE',  ( -0.6823417656250003738, 9.901041667008065872, 1.181850606188754593 ) ) ;
#13616=CARTESIAN_POINT ( 'NONE',  ( -1.402160292154681736E-14, 15.23437500034140157, 1.575800808251682339 ) ) ;
#13624=FACE_OUTER_BOUND ( 'NONE', #48632, .T. ) ;
#13682=SHAPE_REPRESENTATION_RELATIONSHIP ( 'NONE' , 'NONE' ,  #137092, #176823 ) ;
#13739=CARTESIAN_POINT ( 'NONE',  ( -0.4019237886466871523, 8.948664549684629321, -1.499999999999998668 ) ) ;
#13797=CARTESIAN_POINT ( 'NONE',  ( -1.500000000000001110, 11.27083333333333393, 0.8660254037844419273 ) ) ;
#13800=( BOUNDED_CURVE ( )  B_SPLINE_CURVE ( 2, ( #79094, #57528, #191770, #159282, #76956, #140946, #60712, #126876, #44492 ),
 .UNSPECIFIED., .F., .T. ) 
 B_SPLINE_CURVE_WITH_KNOTS ( ( 3, 2, 2, 2, 3 ),
 ( 0.5267857142857143016, 0.5297619047619047672, 0.5357142857142856984, 0.5416666666666666297, 0.5446428571428572063 ),
 .UNSPECIFIED. ) 
 CURVE ( )  GEOMETRIC_REPRESENTATION_ITEM ( )  RATIONAL_B_SPLINE_CURVE ( ( 0.9330127018922194093, 0.9330127018922194093, 1.000000000000000000, 0.8660254037844387076, 1.000000000000000000, 0.8660254037844387076, 1.000000000000000000, 0.9330127018922180770, 0.9330127018922194093 ) ) 
 REPRESENTATION_ITEM ( '' )  );
#13804=CARTESIAN_POINT ( 'NONE',  ( 1.364683531249997417, 8.984375000341396245, 2.602085213965210642E-15 ) ) ;
#13837=CARTESIAN_POINT ( 'NONE',  ( 0.6823417656249934904, 10.75520833367472839, 1.181850606188764807 ) ) ;
#13863=FACE_OUTER_BOUND ( 'NONE', #6100, .T. ) ;
#13906=CARTESIAN_POINT ( 'NONE',  ( -1.402160292154681736E-14, 13.59375000068279604, 1.732050807568881190 ) ) ;
#13914=ADVANCED_FACE ( 'NONE', ( #161936 ), #71375, .T. ) ;
#13939=CARTESIAN_POINT ( 'NONE',  ( 0.6823417656249969321, 9.526041667008065872, -1.181850606188757036 ) ) ;
#14062=CYLINDRICAL_SURFACE ( 'NONE', #23922, 2.000000000000000000 ) ;
#14197=CARTESIAN_POINT ( 'NONE',  ( -8.012344526598182026E-15, 13.29687500034140157, -1.575800808251669460 ) ) ;
#14299=ADVANCED_FACE ( 'NONE', ( #72930 ), #32815, .T. ) ;
#14325=CARTESIAN_POINT ( 'NONE',  ( 1.424698021954186711, 3.742711217035210147, -0.4926413923218386781 ) ) ;
#14337=PRODUCT ( 'positive pin', 'positive pin', '', ( #198820 ) ) ;
#14352=CARTESIAN_POINT ( 'NONE',  ( 0.6823417656249934904, 12.75520833367473017, 1.181850606188764807 ) ) ;
#14360=ORIENTED_EDGE ( 'NONE', *, *, #154706, .T. ) ;
#14370=AXIS2_PLACEMENT_3D ( 'NONE', #176347, #74579, #43169 ) ;
#14413=AXIS2_PLACEMENT_3D ( 'NONE', #198487, #3477, #136723 ) ;
#14415=CARTESIAN_POINT ( 'NONE',  ( 1.364683531249997417, 11.04687500034139802, 2.602085213965210642E-15 ) ) ;
#14456=CARTESIAN_POINT ( 'NONE',  ( 1.499999999999997113, 10.17708333401613174, -0.8660254037844378194 ) ) ;
#14505=VECTOR ( 'NONE', #91247, 1000.000000000000000 ) ;
#14542=VERTEX_POINT ( 'NONE', #88962 ) ;
#14579=CARTESIAN_POINT ( 'NONE',  ( -1.369767765231834300, 3.411414233851330025, -0.2488260012212513972 ) ) ;
#14598=CARTESIAN_POINT ( 'NONE',  ( -0.6823417656250039265, 9.067708333674733723, -1.181850606188755259 ) ) ;
#14599=LINE ( 'NONE', #80696, #162376 ) ;
#14612=CARTESIAN_POINT ( 'NONE',  ( 0.000000000000000000, -4.500000000000003553, 0.000000000000000000 ) ) ;
#14641=ADVANCED_FACE ( 'NONE', ( #93238 ), #75892, .T. ) ;
#14672=CARTESIAN_POINT ( 'NONE',  ( -1.402160292154681736E-14, 13.73437500034139624, 1.575800808251682339 ) ) ;
#14689=B_SPLINE_CURVE_WITH_KNOTS ( 'NONE', 3,
 ( #154462, #56957, #9268, #89474, #123129, #137151, #88395, #104650, #189088, #25512 ),
 .UNSPECIFIED., .F., .F.,
 ( 4, 2, 2, 2, 4 ),
 ( 0.0002061898317416346730, 0.0005587239135660432461, 0.0009112579953904516566, 0.001263792077214860067, 0.001616326159039268694 ),
 .UNSPECIFIED. ) ;
#14706=DIRECTION ( 'NONE',  ( 0.000000000000000000, 0.000000000000000000, -1.000000000000000000 ) ) ;
#14855=CARTESIAN_POINT ( 'NONE',  ( -1.500000000000008216, 11.49999999999999645, 3.469446951953614189E-15 ) ) ;
#14861=CARTESIAN_POINT ( 'NONE',  ( 0.6823417656249969321, 9.526041667008065872, -1.181850606188757036 ) ) ;
#14895=CARTESIAN_POINT ( 'NONE',  ( 0.6823417656249969321, 10.08854166700806587, -1.181850606188757036 ) ) ;
#14909=CYLINDRICAL_SURFACE ( 'NONE', #44833, 0.5000000000000003331 ) ;
#14910=DIRECTION ( 'NONE',  ( 0.000000000000000000, 0.000000000000000000, -1.000000000000000000 ) ) ;
#14965=CARTESIAN_POINT ( 'NONE',  ( -1.500000000000008216, 12.28125000068279427, 3.469446951953614189E-15 ) ) ;
#15002=CARTESIAN_POINT ( 'NONE',  ( -1.402160292154681736E-14, 9.171875000341396245, 1.575800808251682339 ) ) ;
#15011=ADVANCED_FACE ( 'NONE', ( #162489 ), #14062, .T. ) ;
#15113=CYLINDRICAL_SURFACE ( 'NONE', #45898, 1.500000000000000222 ) ;
#15158=CARTESIAN_POINT ( 'NONE',  ( -0.7807912181424305764, 13.24045051524828942, -1.280767376876722041 ) ) ;
#15170=CARTESIAN_POINT ( 'NONE',  ( -0.4019237886467001974, 9.551335450315368902, 1.500000000000001998 ) ) ;
#15269=CARTESIAN_POINT ( 'NONE',  ( 0.6823417656249969321, 12.52604166700806232, -1.181850606188757036 ) ) ;
#15282=CARTESIAN_POINT ( 'NONE',  ( -1.493145604987279107, 4.435543764411821854, 0.1636410324438698216 ) ) ;
#15299=CARTESIAN_POINT ( 'NONE',  ( 0.9322618968498219694, 13.30364107006543861, 1.097267912408639967 ) ) ;
#15315=ORIENTED_EDGE ( 'NONE', *, *, #68075, .T. ) ;
#15320=ORIENTED_EDGE ( 'NONE', *, *, #34340, .F. ) ;
#15417=CARTESIAN_POINT ( 'NONE',  ( -1.402160292154681736E-14, 12.98437500034139980, 1.575800808251682339 ) ) ;
#15457=ORIENTED_EDGE ( 'NONE', *, *, #15859, .T. ) ;
#15480=CARTESIAN_POINT ( 'NONE',  ( -0.6823417656250039265, 10.13020833367472839, -1.181850606188755259 ) ) ;
#15522=CARTESIAN_POINT ( 'NONE',  ( 1.500000000000001332, 9.406250000682799595, 0.000000000000000000 ) ) ;
#15533=LINE ( 'NONE', #78417, #24717 ) ;
#15650=ADVANCED_FACE ( 'NONE', ( #113276, #95914 ), #178214, .T. ) ;
#15664=CARTESIAN_POINT ( 'NONE',  ( -0.6823417656250039265, 9.317708333674733723, -1.181850606188755259 ) ) ;
#15676=( BOUNDED_CURVE ( )  B_SPLINE_CURVE ( 2, ( #103489, #2752, #169550, #134944, #52599, #118727, #203089, #168482, #171680 ),
 .UNSPECIFIED., .F., .T. ) 
 B_SPLINE_CURVE_WITH_KNOTS ( ( 3, 2, 2, 2, 3 ),
 ( 0.5982142857142856984, 0.6011904761904761640, 0.6071428571428570953, 0.6130952380952381375, 0.6160714285714286031 ),
 .UNSPECIFIED. ) 
 CURVE ( )  GEOMETRIC_REPRESENTATION_ITEM ( )  RATIONAL_B_SPLINE_CURVE ( ( 0.9330127018922194093, 0.9330127018922194093, 1.000000000000000000, 0.8660254037844387076, 1.000000000000000000, 0.8660254037844387076, 1.000000000000000000, 0.9330127018922194093, 0.9330127018922194093 ) ) 
 REPRESENTATION_ITEM ( '' )  );
#15735=CARTESIAN_POINT ( 'NONE',  ( -1.402160292154681736E-14, 14.23437500034139624, 1.575800808251682339 ) ) ;
#15776=ORIENTED_EDGE ( 'NONE', *, *, #9604, .F. ) ;
#15794=CARTESIAN_POINT ( 'NONE',  ( 1.500000000000001332, 8.656250000682797818, 0.000000000000000000 ) ) ;
#15859=EDGE_CURVE ( 'NONE', #166249, #139889, #179281, .T. ) ;
#15870=DIRECTION ( 'NONE',  ( 0.000000000000000000, -1.000000000000000000, 0.000000000000000000 ) ) ;
#15920=CARTESIAN_POINT ( 'NONE',  ( 1.500000000000001332, 11.37499999999999645, 0.000000000000000000 ) ) ;
#15924=CARTESIAN_POINT ( 'NONE',  ( 1.364683531250000303, 9.255208333674733723, -0.7879004041258355073 ) ) ;
#15934=CARTESIAN_POINT ( 'NONE',  ( -0.6386677588215945445, 3.364506011487724990, 0.1366812159789567160 ) ) ;
#15942=CARTESIAN_POINT ( 'NONE',  ( -1.286813488861823895, 3.652992958535467238, -0.4595522011843558574 ) ) ;
#15960=CARTESIAN_POINT ( 'NONE',  ( -1.364683531250010740, 10.19270833367473017, 0.7879004041258445001 ) ) ;
#16032=CARTESIAN_POINT ( 'NONE',  ( -1.500000000000015099, 12.01041666734946034, -0.8660254037844309360 ) ) ;
#16035=ORIENTED_EDGE ( 'NONE', *, *, #37798, .F. ) ;
#16075=CARTESIAN_POINT ( 'NONE',  ( -0.7500000000000006661, 9.489583334016129967, -1.299038105676657340 ) ) ;
#16212=CARTESIAN_POINT ( 'NONE',  ( -1.364683531250014514, 8.901041667008069425, -0.7879004041258335089 ) ) ;
#16219=CARTESIAN_POINT ( 'NONE',  ( -1.500000000000001110, 12.05208333401613174, 0.8660254037844418162 ) ) ;
#16251=CARTESIAN_POINT ( 'NONE',  ( -1.500000000000008216, 10.03125000068279959, 3.469446951953614189E-15 ) ) ;
#16257=CARTESIAN_POINT ( 'NONE',  ( -2.788906526875773208E-15, 10.71875000068279604, -1.499999999999998446 ) ) ;
#16293=ORIENTED_EDGE ( 'NONE', *, *, #56964, .F. ) ;
#16326=CARTESIAN_POINT ( 'NONE',  ( -0.6823417656250003738, 13.15104166700806232, 1.181850606188754593 ) ) ;
#16360=CARTESIAN_POINT ( 'NONE',  ( 0.6253970069214125349, 13.29757588023696435, 1.303592148572699339 ) ) ;
#16479=CARTESIAN_POINT ( 'NONE',  ( 1.364683531249996529, 12.52604166700806054, 0.7879004041258405033 ) ) ;
#16542=CARTESIAN_POINT ( 'NONE',  ( -1.402160292154681736E-14, 9.984375000341401574, 1.575800808251682339 ) ) ;
#16584=CARTESIAN_POINT ( 'NONE',  ( -0.7500000000000006661, 9.739583334016129967, -1.299038105676657340 ) ) ;
#16794=CARTESIAN_POINT ( 'NONE',  ( 0.6823417656249969321, 14.58854166700806410, -1.181850606188757036 ) ) ;
#16801=FACE_BOUND ( 'NONE', #23516, .T. ) ;
#16854=CARTESIAN_POINT ( 'NONE',  ( 1.499999999999993117, 8.635416667349460340, 0.8660254037844408170 ) ) ;
#16890=AXIS2_PLACEMENT_3D ( 'NONE', #145836, #63478, #127508 ) ;
#16982=CARTESIAN_POINT ( 'NONE',  ( -0.7500000000000179856, 11.54166666666666607, 1.299038105676658228 ) ) ;
#16986=CARTESIAN_POINT ( 'NONE',  ( -1.364683531250000748, 15.42187500034139447, 0.000000000000000000 ) ) ;
#17029=CARTESIAN_POINT ( 'NONE',  ( -1.364683531250010740, 10.69270833367473195, 0.7879004041258445001 ) ) ;
#17100=CARTESIAN_POINT ( 'NONE',  ( 0.7500000000000006661, 12.61458333401613352, 1.299038105676657340 ) ) ;
#17117=( BOUNDED_CURVE ( )  B_SPLINE_CURVE ( 2, ( #151343, #86330, #187020, #38653, #88481, #152401, #136163, #203258, #70049 ),
 .UNSPECIFIED., .F., .T. ) 
 B_SPLINE_CURVE_WITH_KNOTS ( ( 3, 2, 2, 2, 3 ),
 ( 0.7053571428571427937, 0.7083333333333333703, 0.7142857142857143016, 0.7202380952380952328, 0.7232142857142856984 ),
 .UNSPECIFIED. ) 
 CURVE ( )  GEOMETRIC_REPRESENTATION_ITEM ( )  RATIONAL_B_SPLINE_CURVE ( ( 0.9330127018922194093, 0.9330127018922180770, 1.000000000000000000, 0.8660254037844387076, 1.000000000000000000, 0.8660254037844387076, 1.000000000000000000, 0.9330127018922194093, 0.9330127018922194093 ) ) 
 REPRESENTATION_ITEM ( '' )  );
#17281=CARTESIAN_POINT ( 'NONE',  ( -8.012344526598182026E-15, 8.609375000341403350, -1.575800808251669460 ) ) ;
#17293=CARTESIAN_POINT ( 'NONE',  ( -2.788906526875773208E-15, 9.437499999999998224, -1.499999999999998446 ) ) ;
#17326=CARTESIAN_POINT ( 'NONE',  ( 0.4019237886466847653, 10.60491455036742892, 1.499999999999997113 ) ) ;
#17391=CARTESIAN_POINT ( 'NONE',  ( -1.364683531250000748, 12.10937500034139980, 0.000000000000000000 ) ) ;
#17455=CARTESIAN_POINT ( 'NONE',  ( -0.9657642407454779532, -4.140281660848668999, -0.3272472668956744601 ) ) ;
#17482=ORIENTED_EDGE ( 'NONE', *, *, #207043, .F. ) ;
#17537=CARTESIAN_POINT ( 'NONE',  ( 0.6823417656249934904, 13.00520833367473017, 1.181850606188764807 ) ) ;
#17554=CARTESIAN_POINT ( 'NONE',  ( 1.664652168048566030E-16, -4.500000000000003553, 1.359291649810836722 ) ) ;
#17605=CARTESIAN_POINT ( 'NONE',  ( -1.364683531250014514, 10.15104166700806587, -0.7879004041258335089 ) ) ;
#17648=CARTESIAN_POINT ( 'NONE',  ( -1.364683531250014514, 15.08854166700806587, -0.7879004041258335089 ) ) ;
#17750=EDGE_CURVE ( 'NONE', #147564, #48301, #172628, .T. ) ;
#17783=CARTESIAN_POINT ( 'NONE',  ( -1.364683531250000748, 8.359375000341396245, 0.000000000000000000 ) ) ;
#17820=EDGE_CURVE ( 'NONE', #31261, #73128, #51875, .T. ) ;
#17855=CARTESIAN_POINT ( 'NONE',  ( -0.6823417656250039265, 14.88020833367473195, -1.181850606188755259 ) ) ;
#18034=EDGE_CURVE ( 'NONE', #103348, #179825, #128429, .T. ) ;
#18038=CARTESIAN_POINT ( 'NONE',  ( 3.834746474454188013E-15, 13.09375000068279959, 1.500000000000001554 ) ) ;
#18046=CARTESIAN_POINT ( 'NONE',  ( 0.6823417656249969321, 12.27604166700806054, -1.181850606188757036 ) ) ;
#18052=CARTESIAN_POINT ( 'NONE',  ( -1.500000000000008216, 10.99999999999999645, 3.469446951953614189E-15 ) ) ;
#18097=CARTESIAN_POINT ( 'NONE',  ( -1.364683531250010740, 8.942708333674731946, 0.7879004041258445001 ) ) ;
#18113=( BOUNDED_CURVE ( )  B_SPLINE_CURVE ( 2, ( #200103, #51753, #120014, #117876, #19225, #85303, #152446, #151389, #2959 ),
 .UNSPECIFIED., .F., .T. ) 
 B_SPLINE_CURVE_WITH_KNOTS ( ( 3, 2, 2, 2, 3 ),
 ( 0.5267857142857143016, 0.5297619047619047672, 0.5357142857142856984, 0.5416666666666666297, 0.5446428571428572063 ),
 .UNSPECIFIED. ) 
 CURVE ( )  GEOMETRIC_REPRESENTATION_ITEM ( )  RATIONAL_B_SPLINE_CURVE ( ( 0.9330127018922194093, 0.9330127018922194093, 1.000000000000000000, 0.8660254037844387076, 1.000000000000000000, 0.8660254037844387076, 1.000000000000000000, 0.9330127018922180770, 0.9330127018922194093 ) ) 
 REPRESENTATION_ITEM ( '' )  );
#18155=DIRECTION ( 'NONE',  ( 0.000000000000000000, -1.000000000000000000, 0.000000000000000000 ) ) ;
#18172=CARTESIAN_POINT ( 'NONE',  ( 0.7500000000000006661, 12.69791666734946389, -1.299038105676657340 ) ) ;
#18264=CARTESIAN_POINT ( 'NONE',  ( -1.402160292154681736E-14, 13.42187500034140157, 1.575800808251682339 ) ) ;
#18319=CARTESIAN_POINT ( 'NONE',  ( -1.364683531250010295, 11.88020833367473017, 0.7879004041258445001 ) ) ;
#18435=CARTESIAN_POINT ( 'NONE',  ( -1.115562610750309283E-14, 9.843750000682801371, 1.500000000000001554 ) ) ;
#18460=CARTESIAN_POINT ( 'NONE',  ( 0.5727794709109834681, 4.245899076361618008, 0.3117576387476162503 ) ) ;
#18468=CARTESIAN_POINT ( 'NONE',  ( -1.364683531250014514, 11.83854166700806587, -0.7879004041258335089 ) ) ;
#18515=ORIENTED_EDGE ( 'NONE', *, *, #29848, .T. ) ;
#18621=CARTESIAN_POINT ( 'NONE',  ( -1.402160292154681736E-14, 11.73437500034140335, 1.575800808251682339 ) ) ;
#18633=VERTEX_POINT ( 'NONE', #208686 ) ;
#18669=CARTESIAN_POINT ( 'NONE',  ( -1.115562610750309283E-14, 8.343750000682796042, 1.500000000000001554 ) ) ;
#18671=CARTESIAN_POINT ( 'NONE',  ( 0.6823417656249969321, 13.02604166700806232, -1.181850606188757036 ) ) ;
#18684=CARTESIAN_POINT ( 'NONE',  ( 0.6823417656249934904, 9.505208333674728394, 1.181850606188764807 ) ) ;
#18722=CARTESIAN_POINT ( 'NONE',  ( -0.6823417656250039265, 15.06770833367473195, -1.181850606188755259 ) ) ;
#18798=ORIENTED_EDGE ( 'NONE', *, *, #28769, .T. ) ;
#18806=CARTESIAN_POINT ( 'NONE',  ( -2.788906526875773208E-15, 8.687500000000000000, -1.499999999999998446 ) ) ;
#18859=CARTESIAN_POINT ( 'NONE',  ( -1.364683531250000748, 8.609375000341396245, 0.000000000000000000 ) ) ;
#18916=DIRECTION ( 'NONE',  ( 0.000000000000000000, -1.000000000000000000, 0.000000000000000000 ) ) ;
#18927=CARTESIAN_POINT ( 'NONE',  ( 0.6823417656249969321, 13.83854166700806942, -1.181850606188757036 ) ) ;
#18978=EDGE_CURVE ( 'NONE', #8679, #93531, #28898, .T. ) ;
#19108=VERTEX_POINT ( 'NONE', #50469 ) ;
#19119=CARTESIAN_POINT ( 'NONE',  ( 0.6823417656249969321, 12.02604166700806054, -1.181850606188757036 ) ) ;
#19125=CARTESIAN_POINT ( 'NONE',  ( 0.7500000000000006661, 9.166666666666669627, -1.299038105676657340 ) ) ;
#19150=EDGE_CURVE ( 'NONE', #183272, #133306, #131766, .T. ) ;
#19159=ORIENTED_EDGE ( 'NONE', *, *, #90678, .T. ) ;
#19174=CARTESIAN_POINT ( 'NONE',  ( -1.364683531250014514, 9.151041667008062319, -0.7879004041258335089 ) ) ;
#19189=CARTESIAN_POINT ( 'NONE',  ( 1.499999999999993117, 10.85416666666666785, 0.8660254037844408170 ) ) ;
#19225=CARTESIAN_POINT ( 'NONE',  ( -1.500000000000008216, 11.53125000068279427, 3.469446951953614189E-15 ) ) ;
#19245=CARTESIAN_POINT ( 'NONE',  ( -1.402160292154681736E-14, 12.09375000068279782, 1.732050807568881190 ) ) ;
#19336=CARTESIAN_POINT ( 'NONE',  ( 1.364683531249996529, 12.96354166700806410, 0.7879004041258405033 ) ) ;
#19378=CARTESIAN_POINT ( 'NONE',  ( 1.499999999999997113, 13.89583333333333037, -0.8660254037844378194 ) ) ;
#19385=CARTESIAN_POINT ( 'NONE',  ( 1.364683531250000303, 12.50520833367473195, -0.7879004041258355073 ) ) ;
#19432=CARTESIAN_POINT ( 'NONE',  ( 1.364683531250000748, 13.31770833367473195, -0.7879004041258355073 ) ) ;
#19465=ORIENTED_EDGE ( 'NONE', *, *, #56238, .T. ) ;
#19481=CARTESIAN_POINT ( 'NONE',  ( 0.5773502691896124084, -2.500000000000002220, -0.9999999999999991118 ) ) ;
#19499=DIRECTION ( 'NONE',  ( 0.000000000000000000, -1.000000000000000000, 0.000000000000000000 ) ) ;
#19525=CARTESIAN_POINT ( 'NONE',  ( 0.4153311931458965045, 3.919844006742699616, -0.4999999999999988343 ) ) ;
#19535=CARTESIAN_POINT ( 'NONE',  ( -0.6823417656250039265, 11.56770833367473017, -1.181850606188755259 ) ) ;
#19688=CARTESIAN_POINT ( 'NONE',  ( -0.6823417656250039265, 10.38020833367472839, -1.181850606188755259 ) ) ;
#19753=CARTESIAN_POINT ( 'NONE',  ( -1.364683531250014514, 9.651041667008064096, -0.7879004041258335089 ) ) ;
#19777=LINE ( 'NONE', #69578, #202302 ) ;
#19794=CARTESIAN_POINT ( 'NONE',  ( -0.7500000000000006661, 8.489583334016129967, -1.299038105676657340 ) ) ;
#19860=EDGE_CURVE ( 'NONE', #127955, #183713, #151657, .T. ) ;
#19938=CARTESIAN_POINT ( 'NONE',  ( -0.4019237886466871523, 10.47991455036742714, -1.499999999999998668 ) ) ;
#19997=CARTESIAN_POINT ( 'NONE',  ( 0.4019237886466814902, 12.82366454968462754, 1.499999999999999334 ) ) ;
#19998=CARTESIAN_POINT ( 'NONE',  ( 0.6823417656249969321, 13.33854166700806942, -1.181850606188757036 ) ) ;
#20130=LINE ( 'NONE', #22248, #118175 ) ;
#20182=CARTESIAN_POINT ( 'NONE',  ( 1.364683531250000748, 11.50520833367472839, -0.7879004041258355073 ) ) ;
#20187=CARTESIAN_POINT ( 'NONE',  ( 1.499999999999993117, 9.104166666666666075, 0.8660254037844409281 ) ) ;
#20206=CARTESIAN_POINT ( 'NONE',  ( -1.115562610750309283E-14, 9.562500000000000000, 1.500000000000001554 ) ) ;
#20238=CARTESIAN_POINT ( 'NONE',  ( 1.364683531250000748, 9.067708333674731946, -0.7879004041258355073 ) ) ;
#20314=CARTESIAN_POINT ( 'NONE',  ( -1.402160292154681736E-14, 11.84375000068279604, 1.732050807568881190 ) ) ;
#20404=CARTESIAN_POINT ( 'NONE',  ( 0.6823417656249934904, 12.69270833367473017, 1.181850606188764807 ) ) ;
#20424=CARTESIAN_POINT ( 'NONE',  ( 1.291015824433225490, 3.619357176192806946, -0.4575187270168888931 ) ) ;
#20446=CARTESIAN_POINT ( 'NONE',  ( -1.500000000000001110, 13.77083333333332860, 0.8660254037844419273 ) ) ;
#20452=CARTESIAN_POINT ( 'NONE',  ( -8.012344526598182026E-15, 11.79687500034140157, -1.575800808251669460 ) ) ;
#20539=CARTESIAN_POINT ( 'NONE',  ( -1.500000000000001110, 11.52083333333333393, 0.8660254037844418162 ) ) ;
#20586=CARTESIAN_POINT ( 'NONE',  ( 0.5149768381150775509, 4.156357524118265090, -0.4000488691750970216 ) ) ;
#20595=CARTESIAN_POINT ( 'NONE',  ( -1.364683531250010295, 12.13020833367473017, 0.7879004041258445001 ) ) ;
#20602=LINE ( 'NONE', #185237, #101092 ) ;
#20684=ORIENTED_EDGE ( 'NONE', *, *, #145950, .T. ) ;
#20709=EDGE_LOOP ( 'NONE', ( #207102, #57626 ) ) ;
#20739=CARTESIAN_POINT ( 'NONE',  ( -1.364683531250000748, 11.17187500034139802, 0.000000000000000000 ) ) ;
#20751=CARTESIAN_POINT ( 'NONE',  ( -2.788906526875773208E-15, 10.68750000000000000, -1.499999999999998446 ) ) ;
#20766=CARTESIAN_POINT ( 'NONE',  ( -1.402160292154681736E-14, 15.17187500034140157, 1.575800808251682339 ) ) ;
#20806=CARTESIAN_POINT ( 'NONE',  ( -1.402160292154681736E-14, 8.734375000341403350, 1.575800808251682339 ) ) ;
#20846=CARTESIAN_POINT ( 'NONE',  ( -1.364683531250014514, 15.33854166700806587, -0.7879004041258335089 ) ) ;
#20917=CARTESIAN_POINT ( 'NONE',  ( -2.788906526875773208E-15, 10.68750000000000000, -1.499999999999998446 ) ) ;
#20921=ORIENTED_EDGE ( 'NONE', *, *, #48897, .F. ) ;
#20929=( BOUNDED_CURVE ( )  B_SPLINE_CURVE ( 2, ( #186240, #72486, #183052, #20539, #21581, #201411, #118125, #70341, #38943 ),
 .UNSPECIFIED., .F., .T. ) 
 B_SPLINE_CURVE_WITH_KNOTS ( ( 3, 2, 2, 2, 3 ),
 ( 0.5625000000000000000, 0.5654761904761904656, 0.5714285714285713969, 0.5773809523809523281, 0.5803571428571429047 ),
 .UNSPECIFIED. ) 
 CURVE ( )  GEOMETRIC_REPRESENTATION_ITEM ( )  RATIONAL_B_SPLINE_CURVE ( ( 0.9330127018922194093, 0.9330127018922194093, 1.000000000000000000, 0.8660254037844387076, 1.000000000000000000, 0.8660254037844387076, 1.000000000000000000, 0.9330127018922180770, 0.9330127018922194093 ) ) 
 REPRESENTATION_ITEM ( '' )  );
#20981=CARTESIAN_POINT ( 'NONE',  ( -2.788906526875773208E-15, 12.68749999999999822, -1.499999999999998446 ) ) ;
#20983=CARTESIAN_POINT ( 'NONE',  ( -0.4019237886466871523, 13.19866454968462932, -1.499999999999998668 ) ) ;
#20987=CARTESIAN_POINT ( 'NONE',  ( 0.6823417656249934904, 15.00520833367473195, 1.181850606188764807 ) ) ;
#21036=CARTESIAN_POINT ( 'NONE',  ( -1.500000000000015099, 8.729166666666664298, -0.8660254037844309360 ) ) ;
#21048=CARTESIAN_POINT ( 'NONE',  ( 1.364683531249997417, 13.04687500034139980, 2.602085213965210642E-15 ) ) ;
#21236=CARTESIAN_POINT ( 'NONE',  ( -0.6823417656250039265, 12.31770833367473017, -1.181850606188755259 ) ) ;
#21241=CARTESIAN_POINT ( 'NONE',  ( -0.7500000000000179856, 9.791666666666671404, 1.299038105676658228 ) ) ;
#21294=CARTESIAN_POINT ( 'NONE',  ( -0.6823417656250003738, 9.713541667008065872, 1.181850606188754593 ) ) ;
#21365=CARTESIAN_POINT ( 'NONE',  ( -1.500000000000008216, 11.78125000068279427, 3.469446951953614189E-15 ) ) ;
#21436=CARTESIAN_POINT ( 'NONE',  ( 1.492729907964629898, 3.265405474989949486, 0.1664789471928639075 ) ) ;
#21437=CARTESIAN_POINT ( 'NONE',  ( 0.000000000000000000, -0.5000000000000004441, 1.249999999999999778 ) ) ;
#21451=CARTESIAN_POINT ( 'NONE',  ( 0.6823417656249934904, 13.44270833367473195, 1.181850606188764807 ) ) ;
#21493=CARTESIAN_POINT ( 'NONE',  ( -1.500000000000015099, 13.72916666666666607, -0.8660254037844309360 ) ) ;
#21501=CARTESIAN_POINT ( 'NONE',  ( -1.364683531250010295, 12.13020833367473017, 0.7879004041258445001 ) ) ;
#21544=CARTESIAN_POINT ( 'NONE',  ( 0.09094460184115825407, 13.35659826982236531, -1.523293917897329708 ) ) ;
#21571=CARTESIAN_POINT ( 'NONE',  ( 1.220146605508150803E-14, 11.68749999999999822, -1.499999999999998446 ) ) ;
#21581=CARTESIAN_POINT ( 'NONE',  ( -1.500000000000008216, 11.49999999999999645, 3.469446951953614189E-15 ) ) ;
#21608=CARTESIAN_POINT ( 'NONE',  ( -0.7500000000000006661, 15.23958333401612819, -1.299038105676657340 ) ) ;
#21615=FACE_OUTER_BOUND ( 'NONE', #115763, .T. ) ;
#21641=CARTESIAN_POINT ( 'NONE',  ( -0.6823417656250039265, 10.06770833367473550, -1.181850606188755259 ) ) ;
#21719=VECTOR ( 'NONE', #71573, 1000.000000000000000 ) ;
#21793=CARTESIAN_POINT ( 'NONE',  ( 1.364683531249996529, 10.52604166700806765, 0.7879004041258405033 ) ) ;
#21820=CARTESIAN_POINT ( 'NONE',  ( -1.402160292154681736E-14, 14.42187500034139980, 1.575800808251682339 ) ) ;
#21846=CARTESIAN_POINT ( 'NONE',  ( 1.500000000000001332, 11.65625000068279427, 0.000000000000000000 ) ) ;
#21852=LINE ( 'NONE', #50132, #184023 ) ;
#21860=CARTESIAN_POINT ( 'NONE',  ( -0.6823417656250003738, 9.213541667008065872, 1.181850606188754593 ) ) ;
#21904=CARTESIAN_POINT ( 'NONE',  ( 1.364683531250000303, 15.25520833367473017, -0.7879004041258355073 ) ) ;
#21915=CARTESIAN_POINT ( 'NONE',  ( -1.363015705810363576, 4.003158907273498990, -0.6271916676896991394 ) ) ;
#22002=CARTESIAN_POINT ( 'NONE',  ( 0.4019237886466816012, 8.457585450998168497, -1.499999999999998668 ) ) ;
#22047=CARTESIAN_POINT ( 'NONE',  ( 0.6823417656249934904, 15.25520833367473372, 1.181850606188764807 ) ) ;
#22051=CARTESIAN_POINT ( 'NONE',  ( -1.500000000000008216, 10.53125000068279249, 3.469446951953614189E-15 ) ) ;
#22108=CARTESIAN_POINT ( 'NONE',  ( -1.364683531250000748, 13.17187500034139980, 0.000000000000000000 ) ) ;
#22248=CARTESIAN_POINT ( 'NONE',  ( 0.000000000000000000, 13.49999999999999822, -1.500000000000000222 ) ) ;
#22251=ORIENTED_EDGE ( 'NONE', *, *, #167500, .F. ) ;
#22289=ORIENTED_EDGE ( 'NONE', *, *, #26436, .F. ) ;
#22303=CARTESIAN_POINT ( 'NONE',  ( -1.364683531250000748, 12.10937500034139980, 0.000000000000000000 ) ) ;
#22309=CARTESIAN_POINT ( 'NONE',  ( 1.499999999999997113, 9.895833333333335702, -0.8660254037844378194 ) ) ;
#22364=CARTESIAN_POINT ( 'NONE',  ( -1.364683531250010740, 8.692708333674730170, 0.7879004041258445001 ) ) ;
#22526=CARTESIAN_POINT ( 'NONE',  ( -0.6823417656250003738, 13.15104166700806232, 1.181850606188754593 ) ) ;
#22539=CARTESIAN_POINT ( 'NONE',  ( 1.500000000000001332, 12.15625000068279427, 0.000000000000000000 ) ) ;
#22575=CARTESIAN_POINT ( 'NONE',  ( -1.402160292154681736E-14, 14.31250000000000355, 1.732050807568881190 ) ) ;
#22580=CARTESIAN_POINT ( 'NONE',  ( 1.364683531249997417, 11.23437500034139802, 2.602085213965210642E-15 ) ) ;
#22623=CARTESIAN_POINT ( 'NONE',  ( -1.364683531250010740, 12.69270833367473550, 0.7879004041258445001 ) ) ;
#22722=CARTESIAN_POINT ( 'NONE',  ( -1.402160292154681736E-14, 9.671875000341399797, 1.575800808251682339 ) ) ;
#22829=VECTOR ( 'NONE', #108296, 1000.000000000000000 ) ;
#22870=CARTESIAN_POINT ( 'NONE',  ( 0.6823417656249934904, 10.75520833367472839, 1.181850606188764807 ) ) ;
#22874=ORIENTED_EDGE ( 'NONE', *, *, #174144, .F. ) ;
#22879=FACE_OUTER_BOUND ( 'NONE', #204899, .T. ) ;
#22882=CARTESIAN_POINT ( 'NONE',  ( -0.4019237886466933696, 10.80133545031537068, 1.500000000000005995 ) ) ;
#22896=CARTESIAN_POINT ( 'NONE',  ( 0.6823417656249934904, 14.94270833367473195, 1.181850606188764807 ) ) ;
#22933=DIRECTION ( 'NONE',  ( 0.000000000000000000, 1.000000000000000000, 0.000000000000000000 ) ) ;
#22939=CARTESIAN_POINT ( 'NONE',  ( -1.500000000000008216, 15.50000000000000000, 3.469446951953614189E-15 ) ) ;
#22946=CARTESIAN_POINT ( 'NONE',  ( -1.499912825862921073, 4.449810153648276589, 0.08469158891784515919 ) ) ;
#22983=CARTESIAN_POINT ( 'NONE',  ( 1.364683531249996529, 14.96354166700806410, 0.7879004041258405033 ) ) ;
#22991=AXIS2_PLACEMENT_3D ( 'NONE', #142719, #44131, #8401 ) ;
#23018=CARTESIAN_POINT ( 'NONE',  ( 1.154700538379228147, -4.295408888568413630, -1.734723475976807094E-15 ) ) ;
#23125=CARTESIAN_POINT ( 'NONE',  ( -0.6823417656250039265, 14.63020833367473195, -1.181850606188755259 ) ) ;
#23147=FACE_OUTER_BOUND ( 'NONE', #54163, .T. ) ;
#23187=CARTESIAN_POINT ( 'NONE',  ( -0.6823417656250003738, 12.46354166700806765, 1.181850606188754593 ) ) ;
#23383=CARTESIAN_POINT ( 'NONE',  ( 0.6823417656249934904, 11.19270833367473550, 1.181850606188764807 ) ) ;
#23389=CARTESIAN_POINT ( 'NONE',  ( -0.7500000000000006661, 9.958333333333332149, -1.299038105676657340 ) ) ;
#23453=CARTESIAN_POINT ( 'NONE',  ( -1.500000000000008216, 12.53125000068279427, 3.469446951953614189E-15 ) ) ;
#23506=AXIS2_PLACEMENT_3D ( 'NONE', #196842, #213073, #163287 ) ;
#23516=EDGE_LOOP ( 'NONE', ( #202803, #156643 ) ) ;
#23617=CARTESIAN_POINT ( 'NONE',  ( 0.7500000000000006661, 12.19791666734946389, -1.299038105676657340 ) ) ;
#23652=CARTESIAN_POINT ( 'NONE',  ( -1.500000000000008216, 13.49999999999999822, 3.469446951953614189E-15 ) ) ;
#23657=CARTESIAN_POINT ( 'NONE',  ( -1.402160292154681736E-14, 10.92187500034139802, 1.575800808251682339 ) ) ;
#23710=CARTESIAN_POINT ( 'NONE',  ( 3.834746474454188013E-15, 12.34375000068279959, 1.500000000000001554 ) ) ;
#23722=CARTESIAN_POINT ( 'NONE',  ( -0.4019237886467001974, 10.30133545031537246, 1.500000000000001998 ) ) ;
#23723=EDGE_CURVE ( 'NONE', #187426, #209493, #194736, .T. ) ;
#23731=CARTESIAN_POINT ( 'NONE',  ( 0.6823417656249934904, 13.19270833367473195, 1.181850606188764807 ) ) ;
#23757=LINE ( 'NONE', #89862, #53502 ) ;
#23769=FACE_OUTER_BOUND ( 'NONE', #212598, .T. ) ;
#23777=DIRECTION ( 'NONE',  ( 0.000000000000000000, -1.000000000000000000, 0.000000000000000000 ) ) ;
#23802=CARTESIAN_POINT ( 'NONE',  ( -1.364683531250014514, 10.58854166700806765, -0.7879004041258335089 ) ) ;
#23822=EDGE_LOOP ( 'NONE', ( #131877, #85770, #102643, #82449 ) ) ;
#23855=EDGE_LOOP ( 'NONE', ( #164371, #62047, #136118, #39169 ) ) ;
#23901=DIRECTION ( 'NONE',  ( 0.000000000000000000, 1.000000000000000000, 0.000000000000000000 ) ) ;
#23905=CARTESIAN_POINT ( 'NONE',  ( -1.382866120668046372, 3.383804033233791309, 0.2144190051505676931 ) ) ;
#23922=AXIS2_PLACEMENT_3D ( 'NONE', #65993, #47683, #198149 ) ;
#23948=CARTESIAN_POINT ( 'NONE',  ( -0.6823417656250003738, 11.21354166700806765, 1.181850606188754593 ) ) ;
#23961=CARTESIAN_POINT ( 'NONE',  ( -0.4019237886466871523, 10.69866454968463110, -1.499999999999998668 ) ) ;
#23974=CARTESIAN_POINT ( 'NONE',  ( 0.6823417656249934904, 14.19270833367473195, 1.181850606188764807 ) ) ;
#24017=CARTESIAN_POINT ( 'NONE',  ( -0.7500000000000006661, 14.45833333333333748, -1.299038105676657340 ) ) ;
#24063=CARTESIAN_POINT ( 'NONE',  ( 0.6823417656249969321, 13.77604166700806232, -1.181850606188757036 ) ) ;
#24074=FACE_OUTER_BOUND ( 'NONE', #200429, .T. ) ;
#24196=CARTESIAN_POINT ( 'NONE',  ( -1.364683531250010295, 14.44270833367473550, 0.7879004041258445001 ) ) ;
#24213=( GEOMETRIC_REPRESENTATION_CONTEXT ( 3 ) GLOBAL_UNCERTAINTY_ASSIGNED_CONTEXT ( ( #94982 ) ) GLOBAL_UNIT_ASSIGNED_CONTEXT ( ( #159440, #42523, #74999 ) ) REPRESENTATION_CONTEXT ( 'NONE', 'WORKASPACE' ) );
#24259=CARTESIAN_POINT ( 'NONE',  ( -1.364683531250010295, 12.94270833367473550, 0.7879004041258445001 ) ) ;
#24366=EDGE_CURVE ( 'NONE', #196686, #132613, #87038, .T. ) ;
#24422=FACE_OUTER_BOUND ( 'NONE', #24909, .T. ) ;
#24446=CARTESIAN_POINT ( 'NONE',  ( -0.6823417656250003738, 10.65104166700806765, 1.181850606188754593 ) ) ;
#24453=CARTESIAN_POINT ( 'NONE',  ( -0.7500000000000179856, 8.791666666666669627, 1.299038105676658228 ) ) ;
#24475=CARTESIAN_POINT ( 'NONE',  ( 3.834746474454188013E-15, 8.843750000682797818, 1.500000000000001554 ) ) ;
#24509=CARTESIAN_POINT ( 'NONE',  ( 1.364683531249997417, 8.546875000341403350, 2.602085213965210642E-15 ) ) ;
#24652=EDGE_LOOP ( 'NONE', ( #78227, #100239, #211382, #68722 ) ) ;
#24717=VECTOR ( 'NONE', #77353, 1000.000000000000000 ) ;
#24718=CARTESIAN_POINT ( 'NONE',  ( -1.500000000000008216, 12.74999999999999822, 3.469446951953614189E-15 ) ) ;
#24723=CARTESIAN_POINT ( 'NONE',  ( -8.012344526598182026E-15, 11.04687500034139980, -1.575800808251669460 ) ) ;
#24748=DIRECTION ( 'NONE',  ( 0.000000000000000000, 0.000000000000000000, -1.000000000000000000 ) ) ;
#24768=CARTESIAN_POINT ( 'NONE',  ( 0.6823417656249969321, 11.83854166700806765, -1.181850606188757036 ) ) ;
#24826=EDGE_CURVE ( 'NONE', #113572, #177076, #179569, .T. ) ;
#24868=CARTESIAN_POINT ( 'NONE',  ( -1.364683531250000748, 10.85937500034139802, 0.000000000000000000 ) ) ;
#24909=EDGE_LOOP ( 'NONE', ( #19159, #136035, #181034, #152695 ) ) ;
#24914=CARTESIAN_POINT ( 'NONE',  ( -0.4019237886466966447, 11.83258545099816317, 1.500000000000003997 ) ) ;
#25021=CARTESIAN_POINT ( 'NONE',  ( -1.364683531250000748, 9.921875000341398021, 0.000000000000000000 ) ) ;
#25025=ORIENTED_EDGE ( 'NONE', *, *, #68075, .F. ) ;
#25030=CARTESIAN_POINT ( 'NONE',  ( -1.040834085586084257E-14, 13.49999999999999822, 1.240450515248290753 ) ) ;
#25047=CARTESIAN_POINT ( 'NONE',  ( -1.364683531250014514, 14.33854166700806232, -0.7879004041258335089 ) ) ;
#25053=CARTESIAN_POINT ( 'NONE',  ( -1.115562610750309283E-14, 8.562500000000000000, 1.500000000000001554 ) ) ;
#25089=CARTESIAN_POINT ( 'NONE',  ( -6.009258394948636914E-15, 15.18750000000000000, -1.732050807568875195 ) ) ;
#25134=CARTESIAN_POINT ( 'NONE',  ( -1.364683531250010295, 14.88020833367472839, 0.7879004041258445001 ) ) ;
#25145=CARTESIAN_POINT ( 'NONE',  ( -1.297623789354738655, 4.098502054883955914, -0.4387493294077370320 ) ) ;
#25186=( BOUNDED_CURVE ( )  B_SPLINE_CURVE ( 2, ( #90111, #171335, #55458, #191841, #158310, #141023, #9902, #121613, #73845 ),
 .UNSPECIFIED., .F., .T. ) 
 B_SPLINE_CURVE_WITH_KNOTS ( ( 3, 2, 2, 2, 3 ),
 ( 0.3124999999999999445, 0.3154761904761904656, 0.3214285714285714524, 0.3273809523809523836, 0.3303571428571428492 ),
 .UNSPECIFIED. ) 
 CURVE ( )  GEOMETRIC_REPRESENTATION_ITEM ( )  RATIONAL_B_SPLINE_CURVE ( ( 0.9330127018922194093, 0.9330127018922180770, 1.000000000000000000, 0.8660254037844387076, 1.000000000000000000, 0.8660254037844387076, 1.000000000000000000, 0.9330127018922194093, 0.9330127018922194093 ) ) 
 REPRESENTATION_ITEM ( '' )  );
#25198=CARTESIAN_POINT ( 'NONE',  ( 0.4019237886466884846, 11.45758545099816494, -1.499999999999994449 ) ) ;
#25280=CARTESIAN_POINT ( 'NONE',  ( -8.012344526598182026E-15, 14.10937500034139802, -1.575800808251669460 ) ) ;
#25283=CONICAL_SURFACE ( 'NONE', #187777, 1.540450515248283025, 0.7853981633974428389 ) ;
#25344=CARTESIAN_POINT ( 'NONE',  ( -0.6823417656250003738, 11.71354166700806765, 1.181850606188754593 ) ) ;
#25380=CARTESIAN_POINT ( 'NONE',  ( -1.500000000000008216, 11.24999999999999645, 3.469446951953614189E-15 ) ) ;
#25386=CARTESIAN_POINT ( 'NONE',  ( 1.500000000000001332, 10.65625000068279249, 0.000000000000000000 ) ) ;
#25507=CARTESIAN_POINT ( 'NONE',  ( 0.7500000000000006661, 8.864583334016129967, 1.299038105676657340 ) ) ;
#25512=CARTESIAN_POINT ( 'NONE',  ( 1.264911064067348656, 3.849999999999994316, 0.5000000000000064393 ) ) ;
#25528=CARTESIAN_POINT ( 'NONE',  ( -8.012344526598182026E-15, 10.54687500034139624, -1.575800808251669460 ) ) ;
#25642=ORIENTED_EDGE ( 'NONE', *, *, #19150, .T. ) ;
#25787=CARTESIAN_POINT ( 'NONE',  ( -1.500000000000015099, 12.72916666666666963, -0.8660254037844309360 ) ) ;
#25794=CARTESIAN_POINT ( 'NONE',  ( -1.364683531250014514, 11.08854166700806410, -0.7879004041258335089 ) ) ;
#25806=CARTESIAN_POINT ( 'NONE',  ( -0.4019237886467001974, 10.83258545099816672, 1.500000000000001998 ) ) ;
#25832=CARTESIAN_POINT ( 'NONE',  ( -0.6823417656250039265, 11.88020833367473017, -1.181850606188755259 ) ) ;
#25855=CARTESIAN_POINT ( 'NONE',  ( 0.000000000000000000, 13.49999999999999822, 0.000000000000000000 ) ) ;
#25914=ADVANCED_FACE ( 'NONE', ( #50563 ), #101442, .F. ) ;
#25937=CARTESIAN_POINT ( 'NONE',  ( -1.402160292154681736E-14, 10.67187500034139624, 1.575800808251682339 ) ) ;
#25993=EDGE_LOOP ( 'NONE', ( #26618, #205681, #503, #58083, #168067 ) ) ;
#26033=CARTESIAN_POINT ( 'NONE',  ( 0.000000000000000000, 13.49999999999999822, 0.000000000000000000 ) ) ;
#26063=CARTESIAN_POINT ( 'NONE',  ( 0.000000000000000000, 13.49999999999999822, 0.000000000000000000 ) ) ;
#26087=CARTESIAN_POINT ( 'NONE',  ( -1.402160292154681736E-14, 9.234375000341398021, 1.575800808251682339 ) ) ;
#26108=CARTESIAN_POINT ( 'NONE',  ( 0.5727075793229207124, 3.454207612412955708, -0.3118784721225411061 ) ) ;
#26132=CARTESIAN_POINT ( 'NONE',  ( 0.7500000000000006661, 10.41666666666667140, -1.299038105676657340 ) ) ;
#26158=CARTESIAN_POINT ( 'NONE',  ( 0.7500000000000006661, 14.66666666666666785, -1.299038105676657340 ) ) ;
#26168=DIRECTION ( 'NONE',  ( 0.000000000000000000, 0.3953086839949192521, -0.9185483353412627894 ) ) ;
#26175=EDGE_LOOP ( 'NONE', ( #142943, #94038 ) ) ;
#26177=ADVANCED_FACE ( 'NONE', ( #54367 ), #147941, .T. ) ;
#26201=CARTESIAN_POINT ( 'NONE',  ( 0.6823417656249934904, 13.94270833367473195, 1.181850606188764807 ) ) ;
#26233=FACE_OUTER_BOUND ( 'NONE', #131216, .T. ) ;
#26262=CARTESIAN_POINT ( 'NONE',  ( -1.115562610750309283E-14, 11.34375000068279604, 1.500000000000001554 ) ) ;
#26279=EDGE_CURVE ( 'NONE', #72363, #110148, #195919, .T. ) ;
#26318=CARTESIAN_POINT ( 'NONE',  ( 1.464648953335777604, 3.471602976812853125, -0.3340396966001203394 ) ) ;
#26344=CARTESIAN_POINT ( 'NONE',  ( -1.364683531250000748, 13.42187500034139980, 0.000000000000000000 ) ) ;
#26382=CARTESIAN_POINT ( 'NONE',  ( -5.000000000000009770, 3.850000000000006306, -0.4999999999999942824 ) ) ;
#26410=CARTESIAN_POINT ( 'NONE',  ( 1.364683531249997417, 12.04687500034139980, 2.602085213965210642E-15 ) ) ;
#26436=EDGE_CURVE ( 'NONE', #86666, #205543, #85501, .T. ) ;
#26446=( BOUNDED_CURVE ( )  B_SPLINE_CURVE ( 2, ( #31471, #130108, #127995, #129051, #43468, #193950, #175592, #45597, #111713 ),
 .UNSPECIFIED., .F., .T. ) 
 B_SPLINE_CURVE_WITH_KNOTS ( ( 3, 2, 2, 2, 3 ),
 ( 0.5446428571428572063, 0.5476190476190476719, 0.5535714285714286031, 0.5595238095238095344, 0.5625000000000000000 ),
 .UNSPECIFIED. ) 
 CURVE ( )  GEOMETRIC_REPRESENTATION_ITEM ( )  RATIONAL_B_SPLINE_CURVE ( ( 0.9330127018922194093, 0.9330127018922206306, 1.000000000000000000, 0.8660254037844387076, 1.000000000000000000, 0.8660254037844387076, 1.000000000000000000, 0.9330127018922194093, 0.9330127018922194093 ) ) 
 REPRESENTATION_ITEM ( '' )  );
#26453=CARTESIAN_POINT ( 'NONE',  ( -6.009258394948636914E-15, 11.21875000068279249, -1.732050807568875195 ) ) ;
#26490=B_SPLINE_CURVE_WITH_KNOTS ( 'NONE', 3,
 ( #79137, #29332, #97544, #177722, #161478, #109587, #178792, #162542, #145253, #159324, #62882, #196101, #46660, #30405 ),
 .UNSPECIFIED., .F., .F.,
 ( 4, 2, 2, 2, 2, 2, 4 ),
 ( 0.001731424703407325296, 0.001978656695461681377, 0.002225888687516038977, 0.002720352671624756344, 0.002967584663679115678, 0.003214816655733475012, 0.003709280639842193680 ),
 .UNSPECIFIED. ) ;
#26595=CARTESIAN_POINT ( 'NONE',  ( -1.364683531250014514, 11.33854166700806410, -0.7879004041258335089 ) ) ;
#26618=ORIENTED_EDGE ( 'NONE', *, *, #54713, .F. ) ;
#26774=CARTESIAN_POINT ( 'NONE',  ( 1.499999999999993117, 11.85416666666666430, 0.8660254037844408170 ) ) ;
#26835=FACE_OUTER_BOUND ( 'NONE', #177169, .T. ) ;
#26855=CARTESIAN_POINT ( 'NONE',  ( -1.402160292154681736E-14, 11.81250000000000000, 1.732050807568881190 ) ) ;
#26861=CARTESIAN_POINT ( 'NONE',  ( -1.364683531250000748, 10.10937500034139802, 0.000000000000000000 ) ) ;
#26873=CARTESIAN_POINT ( 'NONE',  ( -0.7500000000000006661, 10.73958333401613174, -1.299038105676657340 ) ) ;
#26900=CARTESIAN_POINT ( 'NONE',  ( 0.6823417656249969321, 11.58854166700806765, -1.181850606188757036 ) ) ;
#26967=CARTESIAN_POINT ( 'NONE',  ( -1.402160292154681736E-14, 14.34375000068279249, 1.732050807568881190 ) ) ;
#26970=EDGE_LOOP ( 'NONE', ( #52555, #113306, #91209, #193012 ) ) ;
#27000=CARTESIAN_POINT ( 'NONE',  ( 1.364683531250000303, 8.505208333674730170, -0.7879004041258355073 ) ) ;
#27123=ORIENTED_EDGE ( 'NONE', *, *, #37635, .F. ) ;
#27157=CARTESIAN_POINT ( 'NONE',  ( 0.6823417656249934904, 9.755208333674728394, 1.181850606188764807 ) ) ;
#27176=CARTESIAN_POINT ( 'NONE',  ( 1.500000000000001332, 9.156250000682799595, 0.000000000000000000 ) ) ;
#27224=CARTESIAN_POINT ( 'NONE',  ( -1.500000000000008216, 14.75000000000000000, 3.469446951953614189E-15 ) ) ;
#27266=CARTESIAN_POINT ( 'NONE',  ( -8.012344526598182026E-15, 14.54687500034139802, -1.575800808251669460 ) ) ;
#27296=FILL_AREA_STYLE ('',( #91269 ) ) ;
#27391=CARTESIAN_POINT ( 'NONE',  ( 1.422919017935823982, 3.797748325714608519, -0.5004465702263648508 ) ) ;
#27416=CARTESIAN_POINT ( 'NONE',  ( -0.6823417656250039265, 14.13020833367473195, -1.181850606188755259 ) ) ;
#27456=ORIENTED_EDGE ( 'NONE', *, *, #80770, .F. ) ;
#27462=ORIENTED_EDGE ( 'NONE', *, *, #108943, .F. ) ;
#27480=CARTESIAN_POINT ( 'NONE',  ( 0.6823417656249969321, 11.33854166700806765, -1.181850606188757036 ) ) ;
#27523=CARTESIAN_POINT ( 'NONE',  ( -0.7500000000000179856, 11.32291666734946212, 1.299038105676658228 ) ) ;
#27626=CARTESIAN_POINT ( 'NONE',  ( 1.390391755498380011, 4.148600085824341477, 0.5639175007713970178 ) ) ;
#27637=MECHANICAL_DESIGN_GEOMETRIC_PRESENTATION_REPRESENTATION('',(#124515),#24213);
#27645=CARTESIAN_POINT ( 'NONE',  ( -1.393530502278612637, 3.362191428456961617, -0.1277288169565338194 ) ) ;
#27666=CARTESIAN_POINT ( 'NONE',  ( 0.6823417656249969321, 10.02604166700806587, -1.181850606188757036 ) ) ;
#27704=ORIENTED_EDGE ( 'NONE', *, *, #90295, .T. ) ;
#27753=CARTESIAN_POINT ( 'NONE',  ( 1.499999999999993117, 13.10416666666666963, 0.8660254037844408170 ) ) ;
#27881=CARTESIAN_POINT ( 'NONE',  ( 0.000000000000000000, 13.49999999999999822, -1.500000000000000222 ) ) ;
#27925=EDGE_CURVE ( 'NONE', #66068, #30840, #127444, .T. ) ;
#27934=CARTESIAN_POINT ( 'NONE',  ( -6.009258394948636914E-15, 12.68749999999999645, -1.732050807568875195 ) ) ;
#27939=CARTESIAN_POINT ( 'NONE',  ( -1.364683531250000748, 9.109375000341396245, 0.000000000000000000 ) ) ;
#27947=AXIS2_PLACEMENT_3D ( 'NONE', #160470, #45674, #112854 ) ;
#27978=CARTESIAN_POINT ( 'NONE',  ( -1.364683531250014514, 11.40104166700806410, -0.7879004041258335089 ) ) ;
#28009=VERTEX_POINT ( 'NONE', #65516 ) ;
#28040=CARTESIAN_POINT ( 'NONE',  ( 1.836970198721030181E-16, 13.49999999999999822, 1.500000000000000222 ) ) ;
#28050=CARTESIAN_POINT ( 'NONE',  ( -0.7500000000000006661, 13.48958333401613352, -1.299038105676657340 ) ) ;
#28081=CARTESIAN_POINT ( 'NONE',  ( 1.364683531249997417, 8.484375000341396245, 2.602085213965210642E-15 ) ) ;
#28233=CARTESIAN_POINT ( 'NONE',  ( -0.6823417656250003738, 9.213541667008065872, 1.181850606188754593 ) ) ;
#28245=CARTESIAN_POINT ( 'NONE',  ( 1.274519002043996707, 3.984210321688911094, -0.4828173461639029274 ) ) ;
#28323=CARTESIAN_POINT ( 'NONE',  ( 0.5773502691896124084, -2.500000000000002220, -0.9999999999999991118 ) ) ;
#28345=CARTESIAN_POINT ( 'NONE',  ( -1.402160292154681736E-14, 13.42187500034140157, 1.575800808251682339 ) ) ;
#28417=ORIENTED_EDGE ( 'NONE', *, *, #158884, .T. ) ;
#28434=CARTESIAN_POINT ( 'NONE',  ( 1.499999999999996891, 10.14583333333333570, -0.8660254037844378194 ) ) ;
#28439=EDGE_CURVE ( 'NONE', #185232, #33711, #87119, .T. ) ;
#28466=CARTESIAN_POINT ( 'NONE',  ( 1.399605654164548296, 3.350766839404967889, -0.07230550894161540121 ) ) ;
#28490=CARTESIAN_POINT ( 'NONE',  ( 0.6823417656249934904, 13.75520833367473195, 1.181850606188764807 ) ) ;
#28543=CYLINDRICAL_SURFACE ( 'NONE', #149661, 1.500000000000000222 ) ;
#28557=CARTESIAN_POINT ( 'NONE',  ( 1.364683531249996529, 12.27604166700806054, 0.7879004041258405033 ) ) ;
#28580=EDGE_CURVE ( 'NONE', #79633, #5587, #107713, .T. ) ;
#28603=CARTESIAN_POINT ( 'NONE',  ( -0.7500000000000006661, 9.989583334016129967, -1.299038105676657340 ) ) ;
#28704=CARTESIAN_POINT ( 'NONE',  ( 1.476571758179666016, 4.272627612153384824, 0.2774774824060997069 ) ) ;
#28723=CARTESIAN_POINT ( 'NONE',  ( -1.464817136648365103, 3.470859643012771389, 0.3332976056707414592 ) ) ;
#28741=CARTESIAN_POINT ( 'NONE',  ( -0.6823417656250003738, 9.401041667008065872, 1.181850606188754593 ) ) ;
#28748=CARTESIAN_POINT ( 'NONE',  ( -1.500000000000001110, 8.520833333333337478, 0.8660254037844419273 ) ) ;
#28769=EDGE_CURVE ( 'NONE', #30840, #100761, #92494, .T. ) ;
#28848=DIRECTION ( 'NONE',  ( 0.000000000000000000, -1.000000000000000000, 0.000000000000000000 ) ) ;
#28898=LINE ( 'NONE', #43037, #2493 ) ;
#28963=CARTESIAN_POINT ( 'NONE',  ( -1.500000000000001110, 10.52083333333333037, 0.8660254037844418162 ) ) ;
#29004=CARTESIAN_POINT ( 'NONE',  ( -1.402160292154681736E-14, 12.81249999999999645, 1.732050807568881190 ) ) ;
#29010=CARTESIAN_POINT ( 'NONE',  ( -1.364683531250010295, 9.880208333674728394, 0.7879004041258445001 ) ) ;
#29050=CARTESIAN_POINT ( 'NONE',  ( 1.364683531249997417, 11.79687500034139802, 2.602085213965210642E-15 ) ) ;
#29117=CARTESIAN_POINT ( 'NONE',  ( 1.500000000000001332, 14.40625000068279604, 0.000000000000000000 ) ) ;
#29151=CARTESIAN_POINT ( 'NONE',  ( 1.364683531249996529, 8.963541667008067648, 0.7879004041258405033 ) ) ;
#29332=CARTESIAN_POINT ( 'NONE',  ( 1.364417678870917472, 3.686064748296142390, 0.6242711042719444325 ) ) ;
#29359=CARTESIAN_POINT ( 'NONE',  ( 0.7500000000000006661, 11.41666666666666607, -1.299038105676657340 ) ) ;
#29366=CARTESIAN_POINT ( 'NONE',  ( -1.500000000000008216, 8.500000000000000000, 3.469446951953614189E-15 ) ) ;
#29422=CARTESIAN_POINT ( 'NONE',  ( -1.364683531250000748, 13.35937500034139980, 0.000000000000000000 ) ) ;
#29433=CARTESIAN_POINT ( 'NONE',  ( -1.399605654164548296, 4.349233160595044723, -0.07230550894161411057 ) ) ;
#29485=VERTEX_POINT ( 'NONE', #69259 ) ;
#29497=CARTESIAN_POINT ( 'NONE',  ( 0.000000000000000000, -0.5000000000000004441, 2.000000000000000000 ) ) ;
#29537=EDGE_CURVE ( 'NONE', #45069, #194295, #200406, .T. ) ;
#29542=CARTESIAN_POINT ( 'NONE',  ( 1.364564222265990390, 4.014448417934980640, -0.6239050962421918145 ) ) ;
#29566=CARTESIAN_POINT ( 'NONE',  ( 1.364683531249997417, 13.29687500034139980, 2.602085213965210642E-15 ) ) ;
#29590=DIRECTION ( 'NONE',  ( 0.000000000000000000, -1.000000000000000000, 0.000000000000000000 ) ) ;
#29592=CARTESIAN_POINT ( 'NONE',  ( -0.4019237886466966447, 12.05133545031537068, 1.500000000000003997 ) ) ;
#29614=VERTEX_POINT ( 'NONE', #784 ) ;
#29622=( BOUNDED_CURVE ( )  B_SPLINE_CURVE ( 2, ( #80036, #146139, #212152, #114740, #129946, #98429, #144024, #210019, #47571 ),
 .UNSPECIFIED., .F., .T. ) 
 B_SPLINE_CURVE_WITH_KNOTS ( ( 3, 2, 2, 2, 3 ),
 ( 0.6160714285714286031, 0.6190476190476190688, 0.6250000000000000000, 0.6309523809523809312, 0.6339285714285713969 ),
 .UNSPECIFIED. ) 
 CURVE ( )  GEOMETRIC_REPRESENTATION_ITEM ( )  RATIONAL_B_SPLINE_CURVE ( ( 0.9330127018922194093, 0.9330127018922194093, 1.000000000000000000, 0.8660254037844387076, 1.000000000000000000, 0.8660254037844387076, 1.000000000000000000, 0.9330127018922194093, 0.9330127018922194093 ) ) 
 REPRESENTATION_ITEM ( '' )  );
#29631=CARTESIAN_POINT ( 'NONE',  ( -1.402160292154681736E-14, 11.23437500034139980, 1.575800808251682339 ) ) ;
#29675=CARTESIAN_POINT ( 'NONE',  ( -1.500000000000015099, 10.51041666734946034, -0.8660254037844309360 ) ) ;
#29728=CARTESIAN_POINT ( 'NONE',  ( -0.5723387408578866076, 4.245249788590611750, 0.3125093782470893533 ) ) ;
#29777=CARTESIAN_POINT ( 'NONE',  ( 1.367525579689990778, 4.283758018875697182, 0.2571629661623252572 ) ) ;
#29793=AXIS2_PLACEMENT_3D ( 'NONE', #7118, #122051, #139297 ) ;
#29797=CARTESIAN_POINT ( 'NONE',  ( -1.355678468426067429, 3.935142031700837428, 0.6419787906858558379 ) ) ;
#29817=CARTESIAN_POINT ( 'NONE',  ( 1.364683531249997417, 8.734375000341396245, 2.602085213965210642E-15 ) ) ;
#29848=EDGE_CURVE ( 'NONE', #93531, #135057, #7798, .T. ) ;
#29895=PLANE ( 'NONE',  #174057 ) ;
#30008=ORIENTED_EDGE ( 'NONE', *, *, #158451, .T. ) ;
#30013=CARTESIAN_POINT ( 'NONE',  ( -2.788906526875773208E-15, 8.937500000000001776, -1.499999999999998446 ) ) ;
#30031=CARTESIAN_POINT ( 'NONE',  ( 3.834746474454188013E-15, 10.56250000000000178, 1.500000000000001554 ) ) ;
#30070=CARTESIAN_POINT ( 'NONE',  ( -1.402160292154681736E-14, 11.31249999999999822, 1.732050807568881190 ) ) ;
#30076=CARTESIAN_POINT ( 'NONE',  ( -0.6823417656250039265, 9.317708333674733723, -1.181850606188755259 ) ) ;
#30110=CARTESIAN_POINT ( 'NONE',  ( -0.6823417656250003738, 10.21354166700806587, 1.181850606188754593 ) ) ;
#30181=CARTESIAN_POINT ( 'NONE',  ( -1.500000000000001110, 13.80208333401613352, 0.8660254037844419273 ) ) ;
#30205=VECTOR ( 'NONE', #48363, 999.9999999999998863 ) ;
#30220=CARTESIAN_POINT ( 'NONE',  ( 0.6823417656249934904, 8.692708333674733723, 1.181850606188764807 ) ) ;
#30377=CARTESIAN_POINT ( 'NONE',  ( -1.364683531250000748, 8.671875000341403350, 0.000000000000000000 ) ) ;
#30383=CARTESIAN_POINT ( 'NONE',  ( -1.397780926668899415, 13.25520333592606015, 0.5144292668303754867 ) ) ;
#30400=CARTESIAN_POINT ( 'NONE',  ( 0.7500000000000006661, 9.083333333333332149, 1.299038105676657340 ) ) ;
#30405=CARTESIAN_POINT ( 'NONE',  ( 1.378728738066221871, 4.086408449757453099, -0.5908528300941785494 ) ) ;
#30490=CARTESIAN_POINT ( 'NONE',  ( 1.364683531249997417, 13.23437500034139980, 2.602085213965210642E-15 ) ) ;
#30614=CARTESIAN_POINT ( 'NONE',  ( 0.000000000000000000, 13.49999999999999822, -1.500000000000000222 ) ) ;
#30615=CARTESIAN_POINT ( 'NONE',  ( 1.297623789354739987, 3.601497945116066468, -0.4387493294077405293 ) ) ;
#30637=EDGE_CURVE ( 'NONE', #211395, #109852, #106246, .T. ) ;
#30641=CARTESIAN_POINT ( 'NONE',  ( -1.402160292154681736E-14, 12.73437500034139980, 1.575800808251682339 ) ) ;
#30704=CARTESIAN_POINT ( 'NONE',  ( 1.364683531250000303, 10.31770833367473195, -0.7879004041258355073 ) ) ;
#30723=ORIENTED_EDGE ( 'NONE', *, *, #146061, .T. ) ;
#30746=CARTESIAN_POINT ( 'NONE',  ( -1.500000000000001110, 9.802083334016129967, 0.8660254037844419273 ) ) ;
#30800=CARTESIAN_POINT ( 'NONE',  ( -0.6499431002536736335, 4.349926030312408542, 0.06915891592278980426 ) ) ;
#30840=VERTEX_POINT ( 'NONE', #105841 ) ;
#30852=CARTESIAN_POINT ( 'NONE',  ( 1.467608305004829194, 4.376302920305730204, -0.3199191423968851256 ) ) ;
#30890=CARTESIAN_POINT ( 'NONE',  ( -0.6823417656250003738, 9.651041667008065872, 1.181850606188754593 ) ) ;
#30964=CARTESIAN_POINT ( 'NONE',  ( 1.364683531250000303, 13.81770833367473017, -0.7879004041258355073 ) ) ;
#31023=CARTESIAN_POINT ( 'NONE',  ( 0.4019237886466847653, 8.604914550367425363, 1.499999999999997113 ) ) ;
#31030=FILL_AREA_STYLE ('',( #62441 ) ) ;
#31062=ADVANCED_FACE ( 'NONE', ( #16801, #13624 ), #29895, .F. ) ;
#31147=CARTESIAN_POINT ( 'NONE',  ( -1.500000000000008216, 11.24999999999999645, 3.469446951953614189E-15 ) ) ;
#31152=CARTESIAN_POINT ( 'NONE',  ( -0.6823417656250039265, 8.817708333674733723, -1.181850606188755259 ) ) ;
#31186=CARTESIAN_POINT ( 'NONE',  ( 1.364683531250000748, 11.31770833367473728, -0.7879004041258355073 ) ) ;
#31195=ORIENTED_EDGE ( 'NONE', *, *, #62276, .F. ) ;
#31201=CARTESIAN_POINT ( 'NONE',  ( 0.4019237886466816012, 10.92633545031537068, -1.499999999999998668 ) ) ;
#31202=CYLINDRICAL_SURFACE ( 'NONE', #213032, 1.500000000000000222 ) ;
#31259=CARTESIAN_POINT ( 'NONE',  ( 0.7500000000000006661, 13.86458333401613352, 1.299038105676657340 ) ) ;
#31261=VERTEX_POINT ( 'NONE', #97850 ) ;
#31292=CARTESIAN_POINT ( 'NONE',  ( -1.402160292154681736E-14, 9.421875000341398021, 1.575800808251682339 ) ) ;
#31332=DIRECTION ( 'NONE',  ( 8.659560562354884787E-17, -0.7071067811865513475, 0.7071067811865435759 ) ) ;
#31398=CARTESIAN_POINT ( 'NONE',  ( 0.6823417656249934904, 12.44270833367473017, 1.181850606188764807 ) ) ;
#31440=CARTESIAN_POINT ( 'NONE',  ( -1.402160292154681736E-14, 8.484375000341403350, 1.575800808251682339 ) ) ;
#31447=CARTESIAN_POINT ( 'NONE',  ( -1.101813147103377633, 13.26515898734009369, 0.9875499716500963920 ) ) ;
#31471=CARTESIAN_POINT ( 'NONE',  ( 1.220146605508150803E-14, 11.68749999999999822, -1.499999999999998446 ) ) ;
#31482=CARTESIAN_POINT ( 'NONE',  ( -1.500000000000001110, 10.05208333401613174, 0.8660254037844418162 ) ) ;
#31489=ORIENTED_EDGE ( 'NONE', *, *, #67112, .T. ) ;
#31499=CARTESIAN_POINT ( 'NONE',  ( 1.499999999999996891, 11.39583333333333393, -0.8660254037844378194 ) ) ;
#31527=CARTESIAN_POINT ( 'NONE',  ( -1.500000000000001110, 8.302083334016129967, 0.8660254037844418162 ) ) ;
#31555=CARTESIAN_POINT ( 'NONE',  ( -1.364683531250000748, 13.10937500034139980, 0.000000000000000000 ) ) ;
#31567=CARTESIAN_POINT ( 'NONE',  ( -1.352846302990983851, 4.252095575701212660, 0.3040853380226599678 ) ) ;
#31703=CARTESIAN_POINT ( 'NONE',  ( 0.6823417656249934904, 12.25520833367473017, 1.181850606188764807 ) ) ;
#31729=DIRECTION ( 'NONE',  ( 0.000000000000000000, -0.7071067811865469066, -0.7071067811865482389 ) ) ;
#31740=ADVANCED_FACE ( 'NONE', ( #168161 ), #25283, .T. ) ;
#31769=CARTESIAN_POINT ( 'NONE',  ( -0.6823417656250039265, 10.38020833367472839, -1.181850606188755259 ) ) ;
#31810=CARTESIAN_POINT ( 'NONE',  ( 1.500000000000001332, 10.40625000068279249, 0.000000000000000000 ) ) ;
#31832=EDGE_CURVE ( 'NONE', #33125, #96430, #164345, .T. ) ;
#31945=CARTESIAN_POINT ( 'NONE',  ( -1.364683531250014514, 9.338541667008062319, -0.7879004041258335089 ) ) ;
#32015=CARTESIAN_POINT ( 'NONE',  ( -1.364683531250014514, 14.40104166700806410, -0.7879004041258335089 ) ) ;
#32148=LINE ( 'NONE', #52654, #77189 ) ;
#32174=FACE_OUTER_BOUND ( 'NONE', #59146, .T. ) ;
#32196=CARTESIAN_POINT ( 'NONE',  ( -6.009258394948636914E-15, 11.68750000000000000, -1.732050807568875195 ) ) ;
#32201=CARTESIAN_POINT ( 'NONE',  ( -8.012344526598182026E-15, 8.796875000341401574, -1.575800808251669460 ) ) ;
#32212=CARTESIAN_POINT ( 'NONE',  ( -0.6500572981163014186, 3.349925512430769636, 0.06817653764027252483 ) ) ;
#32240=CARTESIAN_POINT ( 'NONE',  ( -1.364683531250014514, 10.40104166700806587, -0.7879004041258335089 ) ) ;
#32255=DIRECTION ( 'NONE',  ( 0.000000000000000000, 0.000000000000000000, -1.000000000000000000 ) ) ;
#32262=EDGE_CURVE ( 'NONE', #170262, #211395, #66296, .T. ) ;
#32277=ORIENTED_EDGE ( 'NONE', *, *, #24826, .F. ) ;
#32314=CARTESIAN_POINT ( 'NONE',  ( 0.7500000000000006661, 12.36458333401613174, 1.299038105676657340 ) ) ;
#32316=EDGE_LOOP ( 'NONE', ( #40118, #70708, #187879, #121294 ) ) ;
#32367=CARTESIAN_POINT ( 'NONE',  ( -1.286956418854592332, 4.087185210396952151, 0.5511290012047664888 ) ) ;
#32373=DIRECTION ( 'NONE',  ( 0.000000000000000000, 0.000000000000000000, -1.000000000000000000 ) ) ;
#32442=CARTESIAN_POINT ( 'NONE',  ( -1.378881877344243945, 4.087185210397143109, 0.5904953584335903560 ) ) ;
#32486=CARTESIAN_POINT ( 'NONE',  ( 0.3985077402203209274, -4.205987624083768139, -0.9999999999999993339 ) ) ;
#32493=CYLINDRICAL_SURFACE ( 'NONE', #8475, 1.500000000000000222 ) ;
#32497=VERTEX_POINT ( 'NONE', #86017 ) ;
#32572=ORIENTED_EDGE ( 'NONE', *, *, #175320, .T. ) ;
#32580=EDGE_LOOP ( 'NONE', ( #187456, #182201, #113529, #66728 ) ) ;
#32587=CARTESIAN_POINT ( 'NONE',  ( -1.500000000000001110, 9.770833333333333925, 0.8660254037844418162 ) ) ;
#32604=CARTESIAN_POINT ( 'NONE',  ( -1.402160292154681736E-14, 12.42187500034139802, 1.575800808251682339 ) ) ;
#32664=CARTESIAN_POINT ( 'NONE',  ( -0.7641400526929537085, -4.157144623729230659, -0.6764706046374679982 ) ) ;
#32753=CARTESIAN_POINT ( 'NONE',  ( 1.364683531249996529, 12.77604166700806587, 0.7879004041258405033 ) ) ;
#32815=( BOUNDED_SURFACE ( )  B_SPLINE_SURFACE ( 3, 2, ( 
 ( #205060, #56702, #193091 ),
 ( #11129, #43673, #29542 ),
 ( #143325, #211464, #194159 ),
 ( #10070, #27391, #208262 ),
 ( #94558, #14325, #175799 ),
 ( #30615, #93491, #209318 ),
 ( #190945, #174744, #44740 ),
 ( #109791, #26318, #92430 ),
 ( #110847, #192008, #127121 ),
 ( #60965, #126046, #95634 ),
 ( #28466, #128199, #42609 ),
 ( #13278, #12203, #59895 ),
 ( #45807, #78274, #176852 ),
 ( #160600, #179000, #77206 ),
 ( #161684, #145470, #144401 ),
 ( #111927, #159530, #76146 ),
 ( #210402, #62045, #177928 ),
 ( #79352, #63099, #96703 ) ),
 .UNSPECIFIED., .F., .F., .T. ) 
 B_SPLINE_SURFACE_WITH_KNOTS ( ( 4, 2, 2, 2, 2, 2, 2, 2, 4 ),
 ( 3, 3 ),
 ( 0.000000000000000000, 0.0002366965742690631822, 0.0004733931485381263644, 0.0007100897228071895466, 0.0009467862970762527287, 0.001183482871345315803, 0.001420179445614379093, 0.001656876019883442384, 0.001893572594152505457 ),
 ( 0.000000000000000000, 1.000000000000000000 ),
 .UNSPECIFIED. ) 
 GEOMETRIC_REPRESENTATION_ITEM ( )  RATIONAL_B_SPLINE_SURFACE ( (
 ( 1.000000000000000000, 0.5647844906712728985, 1.000000000000000000),
 ( 1.000000000000000000, 0.5466263600439142945, 1.000000000000000000),
 ( 1.000000000000000000, 0.5350732119542429555, 1.000000000000000000),
 ( 1.000000000000000000, 0.5340116227283870920, 1.000000000000000000),
 ( 1.000000000000000000, 0.5448366076419797199, 1.000000000000000000),
 ( 1.000000000000000000, 0.5794957582366657700, 1.000000000000000000),
 ( 1.000000000000000000, 0.6029004271911160284, 1.000000000000000000),
 ( 1.000000000000000000, 0.6471109807879786846, 1.000000000000000000),
 ( 1.000000000000000000, 0.6680936278988408583, 1.000000000000000000),
 ( 1.000000000000000000, 0.6979136174567169837, 1.000000000000000000),
 ( 1.000000000000000000, 0.7066420332305399787, 1.000000000000000000),
 ( 1.000000000000000000, 0.7075346919462069950, 1.000000000000000000),
 ( 1.000000000000000000, 0.6996296472763482432, 1.000000000000000000),
 ( 1.000000000000000000, 0.6710614938507178939, 1.000000000000000000),
 ( 1.000000000000000000, 0.6504127778617547762, 1.000000000000000000),
 ( 1.000000000000000000, 0.6064966788548298293, 1.000000000000000000),
 ( 1.000000000000000000, 0.5828236970731119904, 1.000000000000000000),
 ( 1.000000000000000000, 0.5649783097559315515, 1.000000000000000000) ) ) 
 REPRESENTATION_ITEM ( '' )  SURFACE ( )  );
#32821=CARTESIAN_POINT ( 'NONE',  ( -1.364683531250010295, 10.94270833367473372, 0.7879004041258445001 ) ) ;
#32849=CARTESIAN_POINT ( 'NONE',  ( -2.788906526875773208E-15, 12.18750000000000178, -1.499999999999998446 ) ) ;
#32863=CARTESIAN_POINT ( 'NONE',  ( -1.402160292154681736E-14, 9.343750000682801371, 1.732050807568881190 ) ) ;
#32943=CARTESIAN_POINT ( 'NONE',  ( -1.500000000000001110, 12.80208333401612819, 0.8660254037844418162 ) ) ;
#33003=CARTESIAN_POINT ( 'NONE',  ( -1.364683531250014514, 9.588541667008064096, -0.7879004041258335089 ) ) ;
#33073=CARTESIAN_POINT ( 'NONE',  ( 1.364683531249996529, 14.27604166700806942, 0.7879004041258405033 ) ) ;
#33125=VERTEX_POINT ( 'NONE', #34820 ) ;
#33232=CARTESIAN_POINT ( 'NONE',  ( 0.4019237886466816012, 11.95758545099816494, -1.499999999999998668 ) ) ;
#33254=CARTESIAN_POINT ( 'NONE',  ( -1.402160292154681736E-14, 11.06250000000000355, 1.732050807568881190 ) ) ;
#33259=CARTESIAN_POINT ( 'NONE',  ( -1.364683531250000748, 14.92187500034139447, 0.000000000000000000 ) ) ;
#33260=ORIENTED_EDGE ( 'NONE', *, *, #66919, .F. ) ;
#33296=CARTESIAN_POINT ( 'NONE',  ( 0.6823417656249934904, 10.25520833367472839, 1.181850606188764807 ) ) ;
#33309=DIRECTION ( 'NONE',  ( 0.000000000000000000, 0.000000000000000000, -1.000000000000000000 ) ) ;
#33370=CARTESIAN_POINT ( 'NONE',  ( 1.500000000000001332, 12.65625000068279427, 0.000000000000000000 ) ) ;
#33380=CARTESIAN_POINT ( 'NONE',  ( -0.7500000000000006661, 12.70833333333333570, -1.299038105676657340 ) ) ;
#33422=CARTESIAN_POINT ( 'NONE',  ( -1.500000000000001110, 11.30208333401612997, 0.8660254037844418162 ) ) ;
#33448=CARTESIAN_POINT ( 'NONE',  ( 1.408744241983818757, 3.463408486559384603, -0.5205678189275573242 ) ) ;
#33524=VERTEX_POINT ( 'NONE', #85715 ) ;
#33553=CARTESIAN_POINT ( 'NONE',  ( 1.364683531250000303, 8.817708333674731946, -0.7879004041258355073 ) ) ;
#33661=CARTESIAN_POINT ( 'NONE',  ( -0.6823417656250039265, 12.06770833367473017, -1.181850606188755259 ) ) ;
#33664=CARTESIAN_POINT ( 'NONE',  ( 1.286956418854607431, 3.652345658002486672, 0.4592741676706121323 ) ) ;
#33668=CARTESIAN_POINT ( 'NONE',  ( 0.000000000000000000, -4.500000000000003553, 0.000000000000000000 ) ) ;
#33694=CARTESIAN_POINT ( 'NONE',  ( -1.119339255005453736E-13, 13.28612805825129151, 1.454322456996997470 ) ) ;
#33711=VERTEX_POINT ( 'NONE', #56427 ) ;
#33781=EDGE_LOOP ( 'NONE', ( #139352, #100708, #70596, #94875 ) ) ;
#33812=CARTESIAN_POINT ( 'NONE',  ( 1.364683531249997417, 12.79687500034139980, 2.602085213965210642E-15 ) ) ;
#33868=DIRECTION ( 'NONE',  ( 0.000000000000000000, -1.000000000000000000, 0.000000000000000000 ) ) ;
#33876=CARTESIAN_POINT ( 'NONE',  ( 1.364683531250000303, 10.56770833367473195, -0.7879004041258355073 ) ) ;
#33920=CARTESIAN_POINT ( 'NONE',  ( 0.7500000000000006661, 8.364583334016128191, 1.299038105676657340 ) ) ;
#33997=ADVANCED_FACE ( 'NONE', ( #127922 ), #210114, .F. ) ;
#34018=CARTESIAN_POINT ( 'NONE',  ( 2.449293598294706414E-16, -4.500000000000003553, -2.000000000000000000 ) ) ;
#34020=CARTESIAN_POINT ( 'NONE',  ( -0.7500000000000006661, 9.208333333333332149, -1.299038105676657340 ) ) ;
#34022=CARTESIAN_POINT ( 'NONE',  ( 1.430889623655247744, 4.024647178788855584, -0.4691377289697504227 ) ) ;
#34069=CARTESIAN_POINT ( 'NONE',  ( 1.836970198721030181E-16, 13.49999999999999822, 1.500000000000000222 ) ) ;
#34087=AXIS2_PLACEMENT_3D ( 'NONE', #4046, #136227, #150343 ) ;
#34126=EDGE_CURVE ( 'NONE', #86318, #128668, #165443, .T. ) ;
#34129=CARTESIAN_POINT ( 'NONE',  ( -1.402160292154681736E-14, 14.48437500034139980, 1.575800808251682339 ) ) ;
#34303=CARTESIAN_POINT ( 'NONE',  ( 1.499999999999993117, 13.13541666734946567, 0.8660254037844408170 ) ) ;
#34314=CARTESIAN_POINT ( 'NONE',  ( -1.500000000000015099, 10.47916666666666607, -0.8660254037844309360 ) ) ;
#34319=CARTESIAN_POINT ( 'NONE',  ( 0.6823417656249969321, 14.83854166700806410, -1.181850606188757036 ) ) ;
#34340=EDGE_CURVE ( 'NONE', #19108, #190224, #197883, .T. ) ;
#34357=ORIENTED_EDGE ( 'NONE', *, *, #41033, .F. ) ;
#34362=CARTESIAN_POINT ( 'NONE',  ( 1.364683531250000748, 11.06770833367473372, -0.7879004041258355073 ) ) ;
#34435=CARTESIAN_POINT ( 'NONE',  ( 1.499999999999997113, 13.17708333401613174, -0.8660254037844378194 ) ) ;
#34526=CARTESIAN_POINT ( 'NONE',  ( -1.364683531250014514, 12.83854166700806232, -0.7879004041258335089 ) ) ;
#34578=CARTESIAN_POINT ( 'NONE',  ( 1.364683531250000303, 11.75520833367473017, -0.7879004041258355073 ) ) ;
#34706=DIRECTION ( 'NONE',  ( 0.000000000000000000, -1.000000000000000000, 0.000000000000000000 ) ) ;
#34721=CARTESIAN_POINT ( 'NONE',  ( -0.6823417656250039265, 11.06770833367473550, -1.181850606188755259 ) ) ;
#34750=CARTESIAN_POINT ( 'NONE',  ( 1.415355422365517146, 13.32676603809294136, -0.06183170064162012147 ) ) ;
#34776=CARTESIAN_POINT ( 'NONE',  ( -1.115562610750309283E-14, 9.562500000000000000, 1.500000000000001554 ) ) ;
#34820=CARTESIAN_POINT ( 'NONE',  ( -1.378728738066235859, 3.613591550242559070, -0.5908528300941767730 ) ) ;
#34865=CARTESIAN_POINT ( 'NONE',  ( 1.364683531250000303, 12.31770833367473195, -0.7879004041258355073 ) ) ;
#34873=CARTESIAN_POINT ( 'NONE',  ( -1.154700538379266339, -2.500000000000002220, 2.602085213965210642E-15 ) ) ;
#34893=CIRCLE ( 'NONE', #27947, 1.500000000000000222 ) ;
#34923=FACE_BOUND ( 'NONE', #26175, .T. ) ;
#34934=CARTESIAN_POINT ( 'NONE',  ( 1.364683531249996529, 9.526041667008062319, 0.7879004041258405033 ) ) ;
#34976=CARTESIAN_POINT ( 'NONE',  ( -6.009258394948636914E-15, 9.218750000682799595, -1.732050807568875195 ) ) ;
#35075=CARTESIAN_POINT ( 'NONE',  ( 1.378728738066228754, 4.086408449757453099, -0.5908528300941744416 ) ) ;
#35168=DIRECTION ( 'NONE',  ( 0.000000000000000000, 0.000000000000000000, 1.000000000000000000 ) ) ;
#35181=CARTESIAN_POINT ( 'NONE',  ( -1.364683531250010295, 14.94270833367472839, 0.7879004041258445001 ) ) ;
#35190=EDGE_CURVE ( 'NONE', #140850, #37159, #13800, .T. ) ;
#35334=CARTESIAN_POINT ( 'NONE',  ( 0.000000000000000000, 13.49999999999999822, -1.240450515248286534 ) ) ;
#35375=CARTESIAN_POINT ( 'NONE',  ( -1.364683531250010740, 12.38020833367473195, 0.7879004041258445001 ) ) ;
#35381=CARTESIAN_POINT ( 'NONE',  ( -1.500000000000001110, 9.270833333333332149, 0.8660254037844419273 ) ) ;
#35427=CARTESIAN_POINT ( 'NONE',  ( -0.6823417656250039265, 9.880208333674728394, -1.181850606188755259 ) ) ;
#35428=ADVANCED_FACE ( 'NONE', ( #22879, #107425 ), #173450, .F. ) ;
#35440=CARTESIAN_POINT ( 'NONE',  ( 0.7500000000000006661, 10.91666666666666430, -1.299038105676657340 ) ) ;
#35500=CARTESIAN_POINT ( 'NONE',  ( 0.7500000000000006661, 12.11458333401613174, 1.299038105676657340 ) ) ;
#35502=VERTEX_POINT ( 'NONE', #144176 ) ;
#35574=DIRECTION ( 'NONE',  ( 0.8660254037844411501, -0.4999999999999956146, -5.551115123125779621E-17 ) ) ;
#35588=CARTESIAN_POINT ( 'NONE',  ( 1.364683531249996529, 13.21354166700806410, 0.7879004041258405033 ) ) ;
#35622=CARTESIAN_POINT ( 'NONE',  ( -1.378728738066235859, 3.613591550242559070, -0.5908528300941767730 ) ) ;
#35640=CARTESIAN_POINT ( 'NONE',  ( -8.012344526598182026E-15, 12.54687500034139624, -1.575800808251669460 ) ) ;
#35730=FACE_OUTER_BOUND ( 'NONE', #94145, .T. ) ;
#35747=VECTOR ( 'NONE', #110270, 1000.000000000000000 ) ;
#35791=CARTESIAN_POINT ( 'NONE',  ( -0.6823417656250039265, 11.81770833367473017, -1.181850606188755259 ) ) ;
#35806=VECTOR ( 'NONE', #121635, 1000.000000000000000 ) ;
#35831=DIRECTION ( 'NONE',  ( 0.000000000000000000, -1.000000000000000000, 0.000000000000000000 ) ) ;
#35855=CARTESIAN_POINT ( 'NONE',  ( -0.6685859206620391459, -4.211945764156043381, -0.8419752161881570718 ) ) ;
#35902=AXIS2_PLACEMENT_3D ( 'NONE', #46037, #211696, #108951 ) ;
#35940=CARTESIAN_POINT ( 'NONE',  ( -1.364683531250014514, 10.65104166700806942, -0.7879004041258335089 ) ) ;
#35951=DIRECTION ( 'NONE',  ( 0.4999999999999999445, 0.000000000000000000, -0.8660254037844387076 ) ) ;
#35988=DIRECTION ( 'NONE',  ( 0.000000000000000000, -1.000000000000000000, 0.000000000000000000 ) ) ;
#36004=CARTESIAN_POINT ( 'NONE',  ( 1.364683531249997417, 9.546875000341396245, 2.602085213965210642E-15 ) ) ;
#36046=CARTESIAN_POINT ( 'NONE',  ( 1.364683531250000303, 15.00520833367472839, -0.7879004041258355073 ) ) ;
#36184=CARTESIAN_POINT ( 'NONE',  ( 0.7500000000000006661, 12.66666666666666607, -1.299038105676657340 ) ) ;
#36235=CARTESIAN_POINT ( 'NONE',  ( 0.000000000000000000, 0.000000000000000000, 0.000000000000000000 ) ) ;
#36248=CARTESIAN_POINT ( 'NONE',  ( 0.6823417656249934904, 12.75520833367473017, 1.181850606188764807 ) ) ;
#36405=DIRECTION ( 'NONE',  ( 0.000000000000000000, -1.000000000000000000, 0.000000000000000000 ) ) ;
#36445=CARTESIAN_POINT ( 'NONE',  ( -8.012344526598182026E-15, 11.54687500034139980, -1.575800808251669460 ) ) ;
#36450=CARTESIAN_POINT ( 'NONE',  ( 1.499999999999993117, 10.35416666666666607, 0.8660254037844409281 ) ) ;
#36466=CARTESIAN_POINT ( 'NONE',  ( 1.220146605508150803E-14, 9.687500000000000000, -1.499999999999998446 ) ) ;
#36497=CARTESIAN_POINT ( 'NONE',  ( -0.6823417656250039265, 9.130208333674726617, -1.181850606188755259 ) ) ;
#36526=VERTEX_POINT ( 'NONE', #190758 ) ;
#36553=CARTESIAN_POINT ( 'NONE',  ( -1.500000000000015099, 9.260416667349463893, -0.8660254037844309360 ) ) ;
#36567=CARTESIAN_POINT ( 'NONE',  ( -0.7500000000000006661, 11.98958333401613174, -1.299038105676657340 ) ) ;
#36576=CARTESIAN_POINT ( 'NONE',  ( -0.7500000000000179856, 12.79166666666666607, 1.299038105676658228 ) ) ;
#36615=CARTESIAN_POINT ( 'NONE',  ( 1.280216254274687104, 3.682822186084150573, 0.4723901200327977890 ) ) ;
#36657=CARTESIAN_POINT ( 'NONE',  ( -1.402160292154681736E-14, 12.67187500034139802, 1.575800808251682339 ) ) ;
#36665=CARTESIAN_POINT ( 'NONE',  ( 1.499999999999993117, 12.13541666734946212, 0.8660254037844408170 ) ) ;
#36700=CARTESIAN_POINT ( 'NONE',  ( -0.7500000000000006661, 14.20833333333333748, -1.299038105676657340 ) ) ;
#36706=CARTESIAN_POINT ( 'NONE',  ( 0.6823417656249934904, 11.44270833367473728, 1.181850606188764807 ) ) ;
#36782=EDGE_CURVE ( 'NONE', #81332, #111937, #190929, .T. ) ;
#36793=CYLINDRICAL_SURFACE ( 'NONE', #57058, 1.500000000000000222 ) ;
#36800=EDGE_CURVE ( 'NONE', #81951, #45069, #5556, .T. ) ;
#36852=CARTESIAN_POINT ( 'NONE',  ( 1.364683531249997417, 12.23437500034139980, 2.602085213965210642E-15 ) ) ;
#36886=CARTESIAN_POINT ( 'NONE',  ( 0.8723278719310798568, 13.34875300405935761, -1.099941997284231476 ) ) ;
#36929=CARTESIAN_POINT ( 'NONE',  ( -1.500000000000015099, 12.76041666734946212, -0.8660254037844309360 ) ) ;
#37006=CARTESIAN_POINT ( 'NONE',  ( -0.6823417656250003738, 11.46354166700806765, 1.181850606188754593 ) ) ;
#37019=ORIENTED_EDGE ( 'NONE', *, *, #209526, .T. ) ;
#37029=CARTESIAN_POINT ( 'NONE',  ( 1.364683531249996529, 15.21354166700806587, 0.7879004041258405033 ) ) ;
#37045=ADVANCED_FACE ( 'NONE', ( #51991 ), #67135, .T. ) ;
#37075=CARTESIAN_POINT ( 'NONE',  ( 0.6823417656249969321, 8.838541667008065872, -1.181850606188757036 ) ) ;
#37119=CARTESIAN_POINT ( 'NONE',  ( -1.402160292154681736E-14, 8.843750000682797818, 1.732050807568881190 ) ) ;
#37135=( BOUNDED_CURVE ( )  B_SPLINE_CURVE ( 2, ( #104673, #69991, #136103, #39660, #37522, #206416, #169655, #202119, #119912 ),
 .UNSPECIFIED., .F., .T. ) 
 B_SPLINE_CURVE_WITH_KNOTS ( ( 3, 2, 2, 2, 3 ),
 ( 0.8660714285714286031, 0.8690476190476190688, 0.8750000000000000000, 0.8809523809523809312, 0.8839285714285713969 ),
 .UNSPECIFIED. ) 
 CURVE ( )  GEOMETRIC_REPRESENTATION_ITEM ( )  RATIONAL_B_SPLINE_CURVE ( ( 0.9330127018922194093, 0.9330127018922194093, 1.000000000000000000, 0.8660254037844387076, 1.000000000000000000, 0.8660254037844387076, 1.000000000000000000, 0.9330127018922194093, 0.9330127018922194093 ) ) 
 REPRESENTATION_ITEM ( '' )  );
#37159=VERTEX_POINT ( 'NONE', #21571 ) ;
#37263=CARTESIAN_POINT ( 'NONE',  ( 0.7500000000000006661, 12.58333333333333570, 1.299038105676657340 ) ) ;
#37265=CARTESIAN_POINT ( 'NONE',  ( -0.7500000000000006661, 13.20833333333333570, -1.299038105676657340 ) ) ;
#37272=CARTESIAN_POINT ( 'NONE',  ( -0.4019237886466933696, 10.58258545099816850, 1.500000000000005995 ) ) ;
#37328=CARTESIAN_POINT ( 'NONE',  ( 0.6823417656249934904, 13.50520833367473195, 1.181850606188764807 ) ) ;
#37477=DIRECTION ( 'NONE',  ( 0.000000000000000000, -1.000000000000000000, 0.000000000000000000 ) ) ;
#37518=CARTESIAN_POINT ( 'NONE',  ( -1.364683531250000748, 11.35937500034139802, 0.000000000000000000 ) ) ;
#37522=CARTESIAN_POINT ( 'NONE',  ( 1.500000000000001332, 9.375000000000001776, 0.000000000000000000 ) ) ;
#37523=CARTESIAN_POINT ( 'NONE',  ( -1.402160292154681736E-14, 10.06249999999999822, 1.732050807568881190 ) ) ;
#37529=ORIENTED_EDGE ( 'NONE', *, *, #120145, .F. ) ;
#37573=CARTESIAN_POINT ( 'NONE',  ( 1.364683531250000748, 9.817708333674737275, -0.7879004041258355073 ) ) ;
#37584=AXIS2_PLACEMENT_3D ( 'NONE', #108442, #191733, #109510 ) ;
#37635=EDGE_CURVE ( 'NONE', #30840, #127879, #127738, .T. ) ;
#37643=DIRECTION ( 'NONE',  ( 0.000000000000000000, 0.000000000000000000, -1.000000000000000000 ) ) ;
#37647=CARTESIAN_POINT ( 'NONE',  ( 1.500000000000001332, 10.90625000068279249, 0.000000000000000000 ) ) ;
#37699=CARTESIAN_POINT ( 'NONE',  ( -0.7500000000000006661, 11.23958333401613174, -1.299038105676657340 ) ) ;
#37722=LINE ( 'NONE', #150422, #82208 ) ;
#37736=CARTESIAN_POINT ( 'NONE',  ( -0.4019237886466871523, 12.44866454968463287, -1.499999999999998668 ) ) ;
#37737=CARTESIAN_POINT ( 'NONE',  ( -0.6823417656250039265, 13.06770833367473017, -1.181850606188755259 ) ) ;
#37782=CARTESIAN_POINT ( 'NONE',  ( 0.7500000000000006661, 13.16666666666666607, -1.299038105676657340 ) ) ;
#37789=CARTESIAN_POINT ( 'NONE',  ( -0.6823417656250003738, 12.15104166700806054, 1.181850606188754593 ) ) ;
#37798=EDGE_CURVE ( 'NONE', #33524, #37159, #7505, .T. ) ;
#37937=CARTESIAN_POINT ( 'NONE',  ( -0.6823417656250039265, 11.31770833367473728, -1.181850606188755259 ) ) ;
#38046=CARTESIAN_POINT ( 'NONE',  ( -1.264911064067348656, 3.850000000000018296, 0.5000000000000064393 ) ) ;
#38090=CARTESIAN_POINT ( 'NONE',  ( 0.6823417656249969321, 10.58854166700806587, -1.181850606188757036 ) ) ;
#38098=CARTESIAN_POINT ( 'NONE',  ( -1.360607927818985541, 13.37576698399828778, 0.2084529114367693059 ) ) ;
#38115=CARTESIAN_POINT ( 'NONE',  ( 0.6823417656249969321, 15.02604166700806410, -1.181850606188757036 ) ) ;
#38148=DIRECTION ( 'NONE',  ( 0.000000000000000000, 0.000000000000000000, -1.000000000000000000 ) ) ;
#38156=CARTESIAN_POINT ( 'NONE',  ( -1.364683531250014514, 8.651041667008065872, -0.7879004041258335089 ) ) ;
#38169=CARTESIAN_POINT ( 'NONE',  ( 1.500000000000001332, 9.656250000682799595, 0.000000000000000000 ) ) ;
#38198=CARTESIAN_POINT ( 'NONE',  ( 0.7500000000000006661, 8.614583334016129967, 1.299038105676657340 ) ) ;
#38337=CARTESIAN_POINT ( 'NONE',  ( -1.364683531250014514, 15.15104166700806587, -0.7879004041258335089 ) ) ;
#38346=CARTESIAN_POINT ( 'NONE',  ( 0.4019237886466816012, 12.45758545099816850, -1.499999999999998668 ) ) ;
#38367=EDGE_CURVE ( 'NONE', #60619, #98073, #86282, .T. ) ;
#38399=CARTESIAN_POINT ( 'NONE',  ( 1.364683531250000303, 13.06770833367473728, -0.7879004041258355073 ) ) ;
#38514=CARTESIAN_POINT ( 'NONE',  ( 1.500000000000001332, 12.90625000068279604, 0.000000000000000000 ) ) ;
#38592=CARTESIAN_POINT ( 'NONE',  ( 1.364683531249997417, 12.23437500034139980, 2.602085213965210642E-15 ) ) ;
#38597=CARTESIAN_POINT ( 'NONE',  ( -0.7500000000000179856, 10.04166666666667140, 1.299038105676658228 ) ) ;
#38649=CARTESIAN_POINT ( 'NONE',  ( -0.6823417656250003738, 9.213541667008065872, 1.181850606188754593 ) ) ;
#38653=CARTESIAN_POINT ( 'NONE',  ( -1.500000000000001110, 10.30208333401612997, 0.8660254037844418162 ) ) ;
#38699=DIRECTION ( 'NONE',  ( 0.000000000000000000, 0.000000000000000000, 1.000000000000000000 ) ) ;
#38700=CARTESIAN_POINT ( 'NONE',  ( 0.000000000000000000, 13.49999999999999822, 0.000000000000000000 ) ) ;
#38707=CARTESIAN_POINT ( 'NONE',  ( 0.4019237886466847653, 12.32366454968463287, 1.499999999999997113 ) ) ;
#38805=CARTESIAN_POINT ( 'NONE',  ( -0.6823417656250039265, 13.31770833367473195, -1.181850606188755259 ) ) ;
#38851=CARTESIAN_POINT ( 'NONE',  ( -1.500000000000015099, 13.22916666666667140, -0.8660254037844309360 ) ) ;
#38857=CARTESIAN_POINT ( 'NONE',  ( -0.6823417656250039265, 11.56770833367473017, -1.181850606188755259 ) ) ;
#38859=EDGE_CURVE ( 'NONE', #115710, #191004, #213351, .T. ) ;
#38903=CARTESIAN_POINT ( 'NONE',  ( -1.402160292154681736E-14, 12.73437500034139980, 1.575800808251682339 ) ) ;
#38943=CARTESIAN_POINT ( 'NONE',  ( 1.220146605508150803E-14, 11.43749999999999822, -1.499999999999998446 ) ) ;
#38945=EDGE_CURVE ( 'NONE', #152917, #195805, #137407, .T. ) ;
#39006=CARTESIAN_POINT ( 'NONE',  ( 1.364683531249996529, 9.713541667008064096, 0.7879004041258405033 ) ) ;
#39051=CARTESIAN_POINT ( 'NONE',  ( -0.4019237886466871523, 11.72991455036742714, -1.499999999999998668 ) ) ;
#39155=CARTESIAN_POINT ( 'NONE',  ( -1.402160292154681736E-14, 10.73437500034139802, 1.575800808251682339 ) ) ;
#39166=CARTESIAN_POINT ( 'NONE',  ( 3.834746474454188013E-15, 10.81250000000000355, 1.500000000000001554 ) ) ;
#39169=ORIENTED_EDGE ( 'NONE', *, *, #154979, .T. ) ;
#39179=CARTESIAN_POINT ( 'NONE',  ( 1.364683531249996529, 14.96354166700806410, 0.7879004041258405033 ) ) ;
#39191=CARTESIAN_POINT ( 'NONE',  ( 0.7500000000000006661, 9.947916667349469222, -1.299038105676657340 ) ) ;
#39216=CARTESIAN_POINT ( 'NONE',  ( 0.6823417656249934904, 9.005208333674726617, 1.181850606188764807 ) ) ;
#39220=VECTOR ( 'NONE', #204091, 1000.000000000000000 ) ;
#39224=CARTESIAN_POINT ( 'NONE',  ( -1.492729907964628788, 4.434594525010058241, 0.1664789471928727893 ) ) ;
#39247=CARTESIAN_POINT ( 'NONE',  ( -1.500000000000008216, 8.281250000682797818, 3.469446951953614189E-15 ) ) ;
#39261=CARTESIAN_POINT ( 'NONE',  ( 0.6823417656249934904, 14.69270833367473195, 1.181850606188764807 ) ) ;
#39378=CIRCLE ( 'NONE', #160438, 0.6500000000000000222 ) ;
#39387=ADVANCED_FACE ( 'NONE', ( #26835 ), #92938, .T. ) ;
#39406=CARTESIAN_POINT ( 'NONE',  ( 1.364683531250000303, 15.06770833367473017, -0.7879004041258355073 ) ) ;
#39413=CARTESIAN_POINT ( 'NONE',  ( 0.4019237886466847653, 12.35491455036742892, 1.499999999999997113 ) ) ;
#39437=VERTEX_POINT ( 'NONE', #161117 ) ;
#39464=CARTESIAN_POINT ( 'NONE',  ( 1.364683531249997417, 12.79687500034139980, 2.602085213965210642E-15 ) ) ;
#39613=CARTESIAN_POINT ( 'NONE',  ( 0.000000000000000000, -1.500000000000001332, 0.000000000000000000 ) ) ;
#39654=CARTESIAN_POINT ( 'NONE',  ( -1.364683531250000748, 10.85937500034139802, 0.000000000000000000 ) ) ;
#39660=CARTESIAN_POINT ( 'NONE',  ( 1.499999999999996891, 9.395833333333332149, -0.8660254037844378194 ) ) ;
#39661=CARTESIAN_POINT ( 'NONE',  ( 1.499999999999997113, 9.395833333333332149, -0.8660254037844378194 ) ) ;
#39693=AXIS2_PLACEMENT_3D ( 'NONE', #19481, #72495, #170001 ) ;
#39712=CARTESIAN_POINT ( 'NONE',  ( -8.012344526598182026E-15, 9.109375000341396245, -1.575800808251669460 ) ) ;
#39789=VERTEX_POINT ( 'NONE', #96138 ) ;
#39927=CARTESIAN_POINT ( 'NONE',  ( -1.500000000000015099, 14.22916666666666785, -0.8660254037844309360 ) ) ;
#39933=CARTESIAN_POINT ( 'NONE',  ( -1.364683531250010295, 11.13020833367473372, 0.7879004041258445001 ) ) ;
#39959=CARTESIAN_POINT ( 'NONE',  ( 0.000000000000000000, 13.49999999999999822, 0.000000000000000000 ) ) ;
#39974=ORIENTED_EDGE ( 'NONE', *, *, #135584, .T. ) ;
#39979=CARTESIAN_POINT ( 'NONE',  ( -1.364683531250000748, 12.92187500034139980, 0.000000000000000000 ) ) ;
#39984=CARTESIAN_POINT ( 'NONE',  ( -2.788906526875773208E-15, 12.21875000068279782, -1.499999999999998446 ) ) ;
#40005=CARTESIAN_POINT ( 'NONE',  ( 1.364683531249997417, 12.98437500034139980, 2.602085213965210642E-15 ) ) ;
#40044=CARTESIAN_POINT ( 'NONE',  ( 1.499999999999993117, 15.13541666734946745, 0.8660254037844409281 ) ) ;
#40076=CARTESIAN_POINT ( 'NONE',  ( -0.6823417656250039265, 10.31770833367473550, -1.181850606188755259 ) ) ;
#40118=ORIENTED_EDGE ( 'NONE', *, *, #199528, .F. ) ;
#40190=CARTESIAN_POINT ( 'NONE',  ( -0.7500000000000006661, 10.95833333333333393, -1.299038105676657340 ) ) ;
#40203=AXIS2_PLACEMENT_3D ( 'NONE', #101807, #54131, #137525 ) ;
#40205=ORIENTED_EDGE ( 'NONE', *, *, #146727, .T. ) ;
#40226=CARTESIAN_POINT ( 'NONE',  ( -1.402160292154681736E-14, 10.48437500034139447, 1.575800808251682339 ) ) ;
#40251=CARTESIAN_POINT ( 'NONE',  ( 0.6823417656249969321, 14.77604166700806410, -1.181850606188757036 ) ) ;
#40283=VERTEX_POINT ( 'NONE', #153390 ) ;
#40294=ADVANCED_FACE ( 'NONE', ( #152322, #184797 ), #139290, .T. ) ;
#40295=CARTESIAN_POINT ( 'NONE',  ( 0.7500000000000006661, 14.58333333333333748, 1.299038105676657340 ) ) ;
#40346=CARTESIAN_POINT ( 'NONE',  ( 0.6823417656249969321, 14.02604166700806232, -1.181850606188757036 ) ) ;
#40355=AXIS2_PLACEMENT_3D ( 'NONE', #122292, #67283, #68356 ) ;
#40381=CARTESIAN_POINT ( 'NONE',  ( 0.9174905902279941738, -4.140925090156048149, -0.4108596822587322062 ) ) ;
#40410=CARTESIAN_POINT ( 'NONE',  ( 1.220146605508150803E-14, 11.46875000068279604, -1.499999999999998446 ) ) ;
#40488=CARTESIAN_POINT ( 'NONE',  ( -1.364683531250014514, 15.40104166700806765, -0.7879004041258335089 ) ) ;
#40551=CARTESIAN_POINT ( 'NONE',  ( -0.6823417656250039265, 12.63020833367473017, -1.181850606188755259 ) ) ;
#40700=DIRECTION ( 'NONE',  ( 0.000000000000000000, 0.000000000000000000, 1.000000000000000000 ) ) ;
#40738=CARTESIAN_POINT ( 'NONE',  ( 1.364683531249996529, 10.96354166700806942, 0.7879004041258403923 ) ) ;
#40853=EDGE_CURVE ( 'NONE', #112831, #48301, #66247, .T. ) ;
#40970=CARTESIAN_POINT ( 'NONE',  ( 3.834746474454188013E-15, 12.09375000068279604, 1.500000000000001554 ) ) ;
#40981=DIRECTION ( 'NONE',  ( 0.4999999999999998890, 0.000000000000000000, 0.8660254037844385966 ) ) ;
#41003=CARTESIAN_POINT ( 'NONE',  ( 0.7500000000000006661, 14.33333333333333748, 1.299038105676657340 ) ) ;
#41009=CARTESIAN_POINT ( 'NONE',  ( -0.6823417656250003738, 10.15104166700806587, 1.181850606188754593 ) ) ;
#41033=EDGE_CURVE ( 'NONE', #142064, #83117, #49874, .T. ) ;
#41054=CARTESIAN_POINT ( 'NONE',  ( -0.6823417656250039265, 12.13020833367473017, -1.181850606188755259 ) ) ;
#41097=B_SPLINE_CURVE_WITH_KNOTS ( 'NONE', 3,
 ( #197291, #148562, #35855, #32664, #69405, #17455, #83540, #181048 ),
 .UNSPECIFIED., .F., .F.,
 ( 4, 2, 2, 4 ),
 ( 2.544396950729599234E-07, 0.0002984430161323445535, 0.0005966315925696161248, 0.001193008745444159267 ),
 .UNSPECIFIED. ) ;
#41118=CARTESIAN_POINT ( 'NONE',  ( 0.000000000000000000, 13.49999999999999822, -1.500000000000000222 ) ) ;
#41123=CARTESIAN_POINT ( 'NONE',  ( 1.500000000000001332, 14.90625000068279604, 0.000000000000000000 ) ) ;
#41131=B_SPLINE_CURVE_WITH_KNOTS ( 'NONE', 3,
 ( #99685, #114932, #213412, #2145 ),
 .UNSPECIFIED., .F., .F.,
 ( 4, 4 ),
 ( 0.007151640131792815283, 0.007705906178639654498 ),
 .UNSPECIFIED. ) ;
#41132=EDGE_CURVE ( 'NONE', #144059, #156928, #153629, .T. ) ;
#41157=CARTESIAN_POINT ( 'NONE',  ( -1.364683531250000748, 10.60937500034139802, 0.000000000000000000 ) ) ;
#41309=CARTESIAN_POINT ( 'NONE',  ( -0.6823417656250003738, 9.963541667008065872, 1.181850606188754593 ) ) ;
#41317=CYLINDRICAL_SURFACE ( 'NONE', #95241, 2.000000000000000000 ) ;
#41335=CARTESIAN_POINT ( 'NONE',  ( 0.6823417656249969321, 14.02604166700806232, -1.181850606188757036 ) ) ;
#41366=CARTESIAN_POINT ( 'NONE',  ( 0.4019237886466778820, 11.60491455036742536, 1.500000000000001554 ) ) ;
#41379=CARTESIAN_POINT ( 'NONE',  ( 0.7500000000000006661, 15.41666666666666963, -1.299038105676657340 ) ) ;
#41423=CARTESIAN_POINT ( 'NONE',  ( 0.6823417656249934904, 14.94270833367473195, 1.181850606188764807 ) ) ;
#41456=CARTESIAN_POINT ( 'NONE',  ( 0.9679107548759222635, -4.157144623729205790, -0.3235293953625327235 ) ) ;
#41459=ORIENTED_EDGE ( 'NONE', *, *, #78717, .F. ) ;
#41563=CARTESIAN_POINT ( 'NONE',  ( -1.402160292154681736E-14, 13.48437500034139269, 1.575800808251682339 ) ) ;
#41585=( BOUNDED_CURVE ( )  B_SPLINE_CURVE ( 2, ( #102315, #200854, #54635, #155342, #119703, #21036, #87135, #153206, #48518 ),
 .UNSPECIFIED., .F., .T. ) 
 B_SPLINE_CURVE_WITH_KNOTS ( ( 3, 2, 2, 2, 3 ),
 ( 0.9553571428571427937, 0.9583333333333333703, 0.9642857142857143016, 0.9702380952380952328, 0.9732142857142856984 ),
 .UNSPECIFIED. ) 
 CURVE ( )  GEOMETRIC_REPRESENTATION_ITEM ( )  RATIONAL_B_SPLINE_CURVE ( ( 0.9330127018922194093, 0.9330127018922180770, 1.000000000000000000, 0.8660254037844387076, 1.000000000000000000, 0.8660254037844387076, 1.000000000000000000, 0.9330127018922194093, 0.9330127018922194093 ) ) 
 REPRESENTATION_ITEM ( '' )  );
#41593=ADVANCED_FACE ( 'NONE', ( #44941, #129459 ), #64368, .T. ) ;
#41629=CARTESIAN_POINT ( 'NONE',  ( -1.364683531250014514, 11.40104166700806410, -0.7879004041258335089 ) ) ;
#41666=CYLINDRICAL_SURFACE ( 'NONE', #61930, 1.500000000000000222 ) ;
#41671=CARTESIAN_POINT ( 'NONE',  ( 1.499999999999997113, 11.42708333401612997, -0.8660254037844378194 ) ) ;
#41739=ORIENTED_EDGE ( 'NONE', *, *, #170196, .T. ) ;
#41782=EDGE_CURVE ( 'NONE', #47758, #8679, #124253, .T. ) ;
#41795=DIRECTION ( 'NONE',  ( 0.000000000000000000, 0.000000000000000000, -1.000000000000000000 ) ) ;
#41815=CARTESIAN_POINT ( 'NONE',  ( 1.220146605508150803E-14, 11.46875000068279604, -1.499999999999998446 ) ) ;
#41817=CARTESIAN_POINT ( 'NONE',  ( -1.364683531250000748, 11.10937500034139802, 0.000000000000000000 ) ) ;
#41823=CARTESIAN_POINT ( 'NONE',  ( 1.500000000000001332, 8.875000000000001776, 0.000000000000000000 ) ) ;
#41846=ADVANCED_FACE ( 'NONE', ( #1457 ), #182357, .T. ) ;
#41859=ORIENTED_EDGE ( 'NONE', *, *, #172644, .F. ) ;
#41875=CARTESIAN_POINT ( 'NONE',  ( -1.364683531250014514, 8.651041667008067648, -0.7879004041258335089 ) ) ;
#41981=ORIENTED_EDGE ( 'NONE', *, *, #173052, .F. ) ;
#41982=CIRCLE ( 'NONE', #121511, 1.240450515248286534 ) ;
#41988=AXIS2_PLACEMENT_3D ( 'NONE', #79396, #29590, #160646 ) ;
#42007=ORIENTED_EDGE ( 'NONE', *, *, #179256, .T. ) ;
#42009=CYLINDRICAL_SURFACE ( 'NONE', #22991, 2.000000000000000000 ) ;
#42075=CARTESIAN_POINT ( 'NONE',  ( -1.500000000000001110, 12.77083333333333215, 0.8660254037844419273 ) ) ;
#42080=CARTESIAN_POINT ( 'NONE',  ( -0.6823417656250003738, 10.90104166700806765, 1.181850606188754593 ) ) ;
#42099=EDGE_CURVE ( 'NONE', #185232, #47534, #145448, .T. ) ;
#42123=CARTESIAN_POINT ( 'NONE',  ( -1.364683531250010740, 11.94270833367473017, 0.7879004041258445001 ) ) ;
#42190=CARTESIAN_POINT ( 'NONE',  ( -1.500000000000015099, 14.76041666734946567, -0.8660254037844309360 ) ) ;
#42222=CARTESIAN_POINT ( 'NONE',  ( 1.364683531249996529, 9.963541667008065872, 0.7879004041258405033 ) ) ;
#42350=DIRECTION ( 'NONE',  ( 0.000000000000000000, 1.000000000000000000, 0.000000000000000000 ) ) ;
#42370=CARTESIAN_POINT ( 'NONE',  ( -1.500000000000015099, 10.51041666734946389, -0.8660254037844309360 ) ) ;
#42378=CARTESIAN_POINT ( 'NONE',  ( 1.364683531250000303, 9.317708333674735499, -0.7879004041258355073 ) ) ;
#42402=CARTESIAN_POINT ( 'NONE',  ( -1.402160292154681736E-14, 14.67187500034139980, 1.575800808251682339 ) ) ;
#42409=CARTESIAN_POINT ( 'NONE',  ( -0.7500000000000179856, 8.541666666666669627, 1.299038105676658228 ) ) ;
#42447=CARTESIAN_POINT ( 'NONE',  ( 1.500000000000001332, 14.87500000000000000, 0.000000000000000000 ) ) ;
#42462=VERTEX_POINT ( 'NONE', #161629 ) ;
#42488=CARTESIAN_POINT ( 'NONE',  ( 0.6823417656249969321, 14.52604166700806410, -1.181850606188757036 ) ) ;
#42498=ADVANCED_FACE ( 'NONE', ( #93438, #193030 ), #94507, .T. ) ;
#42523=( NAMED_UNIT ( * ) PLANE_ANGLE_UNIT ( ) SI_UNIT ( $, .RADIAN. ) );
#42577=ORIENTED_EDGE ( 'NONE', *, *, #36782, .F. ) ;
#42589=CARTESIAN_POINT ( 'NONE',  ( 0.4019237886466778820, 8.354914550367425363, 1.500000000000001554 ) ) ;
#42609=CARTESIAN_POINT ( 'NONE',  ( 1.499577476386907637, 3.250920186034359727, -0.09296422598485129529 ) ) ;
#42634=CARTESIAN_POINT ( 'NONE',  ( 0.6823417656249969321, 14.08854166700806232, -1.181850606188757036 ) ) ;
#42701=CARTESIAN_POINT ( 'NONE',  ( -1.402160292154681736E-14, 11.48437500034139980, 1.575800808251682339 ) ) ;
#42742=CARTESIAN_POINT ( 'NONE',  ( 1.499999999999997113, 11.67708333401613174, -0.8660254037844378194 ) ) ;
#42881=CARTESIAN_POINT ( 'NONE',  ( 1.364683531249997417, 10.23437500034139802, 2.602085213965210642E-15 ) ) ;
#43037=CARTESIAN_POINT ( 'NONE',  ( 0.000000000000000000, -4.500000000000003553, 2.000000000000000000 ) ) ;
#43064=CLOSED_SHELL ( 'NONE', ( #14299, #173242, #9464, #194489, #31740, #44454, #55983, #49335, #148103, #15011, #109894, #40294, #49195, #108168, #135667, #13496, #167834, #145855, #207902, #104850, #37045, #47647, #148672, #212987, #47766, #44953, #112326, #2436, #119338, #145352, #89860, #189809, #78890, #90880, #41846, #79763, #206917, #62032, #177972, #176500, #212939, #14641, #89328, #160593, #78978, #10970, #39387, #75222, #145443, #65099, #179249, #93645, #180647, #25914, #85053, #33997, #122879, #84375, #105310, #15650, #31062, #42498, #133859, #125848, #41593, #7421, #174659, #9842, #26177, #104477, #35428, #203317, #206276, #203897, #13914, #129097 ) ) ;
#43086=CARTESIAN_POINT ( 'NONE',  ( -0.7500000000000179856, 9.041666666666669627, 1.299038105676658228 ) ) ;
#43149=CARTESIAN_POINT ( 'NONE',  ( -0.7500000000000006661, 12.95833333333333570, -1.299038105676657340 ) ) ;
#43155=CARTESIAN_POINT ( 'NONE',  ( 1.364683531249997417, 10.23437500034139802, 2.602085213965210642E-15 ) ) ;
#43169=DIRECTION ( 'NONE',  ( 0.000000000000000000, 0.000000000000000000, -1.000000000000000000 ) ) ;
#43191=CARTESIAN_POINT ( 'NONE',  ( -1.364683531250000748, 11.92187500034139980, 0.000000000000000000 ) ) ;
#43197=CARTESIAN_POINT ( 'NONE',  ( 0.7500000000000006661, 9.833333333333332149, 1.299038105676657340 ) ) ;
#43256=CARTESIAN_POINT ( 'NONE',  ( 1.499999999999993117, 13.63541666734946034, 0.8660254037844409281 ) ) ;
#43290=CARTESIAN_POINT ( 'NONE',  ( 1.364683531250000303, 9.755208333674735499, -0.7879004041258355073 ) ) ;
#43297=CARTESIAN_POINT ( 'NONE',  ( -2.788906526875773208E-15, 11.93750000000000000, -1.499999999999998446 ) ) ;
#43309=CARTESIAN_POINT ( 'NONE',  ( -0.5773502691896261751, -2.500000000000002220, -0.9999999999999991118 ) ) ;
#43438=CARTESIAN_POINT ( 'NONE',  ( -1.364683531250010295, 10.19270833367473017, 0.7879004041258445001 ) ) ;
#43468=CARTESIAN_POINT ( 'NONE',  ( 1.500000000000001332, 11.62499999999999645, 0.000000000000000000 ) ) ;
#43511=CARTESIAN_POINT ( 'NONE',  ( 0.7500000000000006661, 14.91666666666666785, -1.299038105676657340 ) ) ;
#43554=CARTESIAN_POINT ( 'NONE',  ( -1.364683531250010295, 14.13020833367473372, 0.7879004041258445001 ) ) ;
#43565=CARTESIAN_POINT ( 'NONE',  ( -2.788906526875773208E-15, 9.218750000682799595, -1.499999999999998446 ) ) ;
#43642=CARTESIAN_POINT ( 'NONE',  ( 0.7500000000000006661, 10.16666666666667140, -1.299038105676657340 ) ) ;
#43673=CARTESIAN_POINT ( 'NONE',  ( 1.425126390603690174, 3.965403223221183548, -0.4909503797921681012 ) ) ;
#43697=CARTESIAN_POINT ( 'NONE',  ( -1.364683531250000748, 13.92187500034140157, 0.000000000000000000 ) ) ;
#43747=DIRECTION ( 'NONE',  ( 0.000000000000000000, -1.000000000000000000, 0.000000000000000000 ) ) ;
#43764=CARTESIAN_POINT ( 'NONE',  ( -1.364683531250000748, 11.42187500034139802, 0.000000000000000000 ) ) ;
#43806=CARTESIAN_POINT ( 'NONE',  ( -0.7500000000000179856, 11.07291666734946212, 1.299038105676658228 ) ) ;
#43846=ORIENTED_EDGE ( 'NONE', *, *, #194138, .F. ) ;
#43905=CARTESIAN_POINT ( 'NONE',  ( 1.378881877344245055, 3.612814789602863730, 0.5904953584335879135 ) ) ;
#43925=CARTESIAN_POINT ( 'NONE',  ( -1.465205965978033209, 3.329490383941810183, 0.3306380942217598262 ) ) ;
#43940=CARTESIAN_POINT ( 'NONE',  ( 0.6823417656249969321, 10.52604166700806587, -1.181850606188757036 ) ) ;
#43947=CARTESIAN_POINT ( 'NONE',  ( -1.500000000000015099, 8.729166666666664298, -0.8660254037844309360 ) ) ;
#43972=CARTESIAN_POINT ( 'NONE',  ( -0.7500000000000179856, 8.572916667349467446, 1.299038105676658228 ) ) ;
#44030=ORIENTED_EDGE ( 'NONE', *, *, #188668, .F. ) ;
#44131=DIRECTION ( 'NONE',  ( 0.000000000000000000, 1.000000000000000000, 0.000000000000000000 ) ) ;
#44149=LINE ( 'NONE', #27881, #35747 ) ;
#44152=CARTESIAN_POINT ( 'NONE',  ( -1.247849810309911600, 13.37576698399836594, 0.5524780460566154350 ) ) ;
#44200=CARTESIAN_POINT ( 'NONE',  ( -1.500000000000015099, 12.97916666666666963, -0.8660254037844309360 ) ) ;
#44207=CARTESIAN_POINT ( 'NONE',  ( 1.364683531249996529, 9.963541667008065872, 0.7879004041258405033 ) ) ;
#44240=ORIENTED_EDGE ( 'NONE', *, *, #212216, .T. ) ;
#44245=CARTESIAN_POINT ( 'NONE',  ( -8.012344526598182026E-15, 11.35937500034139980, -1.575800808251669460 ) ) ;
#44314=CARTESIAN_POINT ( 'NONE',  ( -1.402160292154681736E-14, 14.09375000068279959, 1.732050807568881190 ) ) ;
#44316=ORIENTED_EDGE ( 'NONE', *, *, #153335, .F. ) ;
#44348=CARTESIAN_POINT ( 'NONE',  ( -1.364683531250014514, 9.588541667008064096, -0.7879004041258335089 ) ) ;
#44454=ADVANCED_FACE ( 'NONE', ( #82506 ), #81458, .T. ) ;
#44492=CARTESIAN_POINT ( 'NONE',  ( 1.220146605508150803E-14, 11.68749999999999822, -1.499999999999998446 ) ) ;
#44504=CARTESIAN_POINT ( 'NONE',  ( 0.6823417656249969321, 9.338541667008065872, -1.181850606188757036 ) ) ;
#44574=CARTESIAN_POINT ( 'NONE',  ( 1.499999999999997113, 14.64583333333333393, -0.8660254037844378194 ) ) ;
#44582=ORIENTED_EDGE ( 'NONE', *, *, #34126, .F. ) ;
#44616=CARTESIAN_POINT ( 'NONE',  ( -0.6823417656250039265, 12.56770833367473017, -1.181850606188755259 ) ) ;
#44627=CARTESIAN_POINT ( 'NONE',  ( -1.500267808745624709, 4.350826524122706651, 0.06648599600051158243 ) ) ;
#44719=CARTESIAN_POINT ( 'NONE',  ( -1.455305287003866965, 3.352261184402082428, -0.3947446046151094623 ) ) ;
#44740=CARTESIAN_POINT ( 'NONE',  ( 1.409302795777320982, 3.485449738227918370, -0.5172811130322817474 ) ) ;
#44765=CARTESIAN_POINT ( 'NONE',  ( -1.364683531250010295, 13.44270833367473017, 0.7879004041258445001 ) ) ;
#44816=CARTESIAN_POINT ( 'NONE',  ( 0.000000000000000000, 13.49999999999999822, 0.000000000000000000 ) ) ;
#44830=CARTESIAN_POINT ( 'NONE',  ( 1.364683531250000303, 12.06770833367473195, -0.7879004041258355073 ) ) ;
#44833=AXIS2_PLACEMENT_3D ( 'NONE', #81003, #147091, #32255 ) ;
#44874=CARTESIAN_POINT ( 'NONE',  ( 0.7500000000000006661, 10.94791666734946212, -1.299038105676657340 ) ) ;
#44924=DIRECTION ( 'NONE',  ( 1.000000000000000000, 0.000000000000000000, -1.665334536937734811E-16 ) ) ;
#44928=CARTESIAN_POINT ( 'NONE',  ( 1.154700538379228147, -4.295408888568413630, -1.734723475976807094E-15 ) ) ;
#44941=FACE_BOUND ( 'NONE', #97390, .T. ) ;
#44953=ADVANCED_FACE ( 'NONE', ( #74805 ), #58548, .T. ) ;
#44962=ORIENTED_EDGE ( 'NONE', *, *, #48897, .T. ) ;
#44974=CARTESIAN_POINT ( 'NONE',  ( 1.464817136648363327, 4.229140356987229232, 0.3332976056707502299 ) ) ;
#44992=CARTESIAN_POINT ( 'NONE',  ( -1.364708430267705497, 4.015407764754321818, 0.6235921627254642496 ) ) ;
#45003=( BOUNDED_CURVE ( )  B_SPLINE_CURVE ( 2, ( #154596, #152454, #67959, #203307, #84246, #134103, #122178, #38707, #51763 ),
 .UNSPECIFIED., .F., .T. ) 
 B_SPLINE_CURVE_WITH_KNOTS ( ( 3, 2, 2, 2, 3 ),
 ( 0.4375000000000000000, 0.4404761904761904656, 0.4464285714285714524, 0.4523809523809523836, 0.4553571428571427937 ),
 .UNSPECIFIED. ) 
 CURVE ( )  GEOMETRIC_REPRESENTATION_ITEM ( )  RATIONAL_B_SPLINE_CURVE ( ( 0.9330127018922194093, 0.9330127018922194093, 1.000000000000000000, 0.8660254037844387076, 1.000000000000000000, 0.8660254037844387076, 1.000000000000000000, 0.9330127018922206306, 0.9330127018922194093 ) ) 
 REPRESENTATION_ITEM ( '' )  );
#45011=CARTESIAN_POINT ( 'NONE',  ( -1.364683531250010740, 9.130208333674731946, 0.7879004041258445001 ) ) ;
#45033=VERTEX_POINT ( 'NONE', #143041 ) ;
#45069=VERTEX_POINT ( 'NONE', #84118 ) ;
#45146=CARTESIAN_POINT ( 'NONE',  ( -2.788906526875773208E-15, 12.43750000000000000, -1.499999999999998446 ) ) ;
#45267=CARTESIAN_POINT ( 'NONE',  ( 0.7500000000000006661, 11.83333333333333393, 1.299038105676657340 ) ) ;
#45272=CARTESIAN_POINT ( 'NONE',  ( -0.6823417656250003738, 8.651041667008065872, 1.181850606188754593 ) ) ;
#45310=CARTESIAN_POINT ( 'NONE',  ( -8.012344526598182026E-15, 11.60937500034139980, -1.575800808251669460 ) ) ;
#45383=CARTESIAN_POINT ( 'NONE',  ( -1.402160292154681736E-14, 13.34375000068279427, 1.732050807568881190 ) ) ;
#45417=CARTESIAN_POINT ( 'NONE',  ( -0.6823417656250039265, 9.317708333674733723, -1.181850606188755259 ) ) ;
#45460=ORIENTED_EDGE ( 'NONE', *, *, #54713, .T. ) ;
#45479=EDGE_LOOP ( 'NONE', ( #135503, #8590, #20684, #186234, #52814, #79126, #97021, #55974 ) ) ;
#45487=VECTOR ( 'NONE', #117022, 1000.000000000000000 ) ;
#45568=CARTESIAN_POINT ( 'NONE',  ( 0.6823417656249969321, 9.088541667008065872, -1.181850606188757036 ) ) ;
#45573=ORIENTED_EDGE ( 'NONE', *, *, #34126, .T. ) ;
#45597=CARTESIAN_POINT ( 'NONE',  ( 0.4019237886466778820, 11.57366454968462932, 1.500000000000001554 ) ) ;
#45674=DIRECTION ( 'NONE',  ( 0.000000000000000000, 1.000000000000000000, 0.000000000000000000 ) ) ;
#45684=CARTESIAN_POINT ( 'NONE',  ( 0.6823417656249969321, 13.02604166700806232, -1.181850606188757036 ) ) ;
#45697=CARTESIAN_POINT ( 'NONE',  ( -1.286956418854592332, 4.047654341997461991, 0.4592741676706398324 ) ) ;
#45752=DIRECTION ( 'NONE',  ( 0.000000000000000000, 0.000000000000000000, -1.000000000000000000 ) ) ;
#45807=CARTESIAN_POINT ( 'NONE',  ( 1.393602545685229011, 3.362046851755900345, 0.1272763605452785218 ) ) ;
#45829=CARTESIAN_POINT ( 'NONE',  ( 1.364683531249997417, 13.54687500034139980, 2.602085213965210642E-15 ) ) ;
#45853=CARTESIAN_POINT ( 'NONE',  ( 0.000000000000000000, -4.517653975874099892, -1.376945625684933061 ) ) ;
#45892=CARTESIAN_POINT ( 'NONE',  ( -8.012344526598182026E-15, 11.35937500034139980, -1.575800808251669460 ) ) ;
#45898=AXIS2_PLACEMENT_3D ( 'NONE', #176578, #76923, #196028 ) ;
#45938=CARTESIAN_POINT ( 'NONE',  ( 1.499999999999997113, 9.427083334016129967, -0.8660254037844378194 ) ) ;
#46016=EDGE_CURVE ( 'NONE', #40283, #202706, #213821, .T. ) ;
#46037=CARTESIAN_POINT ( 'NONE',  ( 0.000000000000000000, -4.517653975874099892, 0.000000000000000000 ) ) ;
#46038=CARTESIAN_POINT ( 'NONE',  ( 1.265299903344048627, 3.779048306927172529, 0.4993168358707211207 ) ) ;
#46056=CARTESIAN_POINT ( 'NONE',  ( -1.430889623655251075, 3.675352821211156140, -0.4691377289697510888 ) ) ;
#46063=VECTOR ( 'NONE', #34706, 1000.000000000000000 ) ;
#46074=CARTESIAN_POINT ( 'NONE',  ( -0.6823417656250039265, 9.817708333674735499, -1.181850606188755259 ) ) ;
#46115=EDGE_CURVE ( 'NONE', #177149, #205543, #189550, .T. ) ;
#46150=CARTESIAN_POINT ( 'NONE',  ( 1.364683531249997417, 15.29687500034139447, 2.602085213965210642E-15 ) ) ;
#46203=VERTEX_POINT ( 'NONE', #156647 ) ;
#46333=CARTESIAN_POINT ( 'NONE',  ( -0.7500000000000179856, 10.79166666666666430, 1.299038105676658228 ) ) ;
#46339=CARTESIAN_POINT ( 'NONE',  ( -0.6823417656250003738, 9.401041667008065872, 1.181850606188754593 ) ) ;
#46371=CARTESIAN_POINT ( 'NONE',  ( 0.6823417656249969321, 11.08854166700806765, -1.181850606188757036 ) ) ;
#46379=ORIENTED_EDGE ( 'NONE', *, *, #38367, .F. ) ;
#46442=CARTESIAN_POINT ( 'NONE',  ( 0.7500000000000006661, 14.11458333401613352, 1.299038105676657340 ) ) ;
#46475=CARTESIAN_POINT ( 'NONE',  ( -1.402160292154681736E-14, 8.921875000341405126, 1.575800808251682339 ) ) ;
#46491=DIRECTION ( 'NONE',  ( 0.000000000000000000, 0.3953086839949069842, 0.9185483353412680074 ) ) ;
#46629=CARTESIAN_POINT ( 'NONE',  ( 1.364683531249996529, 8.526041667008065872, 0.7879004041258405033 ) ) ;
#46636=CARTESIAN_POINT ( 'NONE',  ( -1.434937167926458423, 13.25321981955314143, 0.4065227821781826623 ) ) ;
#46641=CARTESIAN_POINT ( 'NONE',  ( -1.115562610750309283E-14, 9.562500000000000000, 1.500000000000001554 ) ) ;
#46660=CARTESIAN_POINT ( 'NONE',  ( 1.408069224121391017, 4.235466930450527023, -0.5223881139200245993 ) ) ;
#46689=DIRECTION ( 'NONE',  ( 0.000000000000000000, -1.000000000000000000, 0.000000000000000000 ) ) ;
#46732=CARTESIAN_POINT ( 'NONE',  ( -0.7500000000000179856, 9.791666666666671404, 1.299038105676658228 ) ) ;
#46751=CARTESIAN_POINT ( 'NONE',  ( -0.6823417656250039265, 13.31770833367473195, -1.181850606188755259 ) ) ;
#46804=ORIENTED_EDGE ( 'NONE', *, *, #28580, .T. ) ;
#46821=DIRECTION ( 'NONE',  ( 0.000000000000000000, -1.000000000000000000, 0.000000000000000000 ) ) ;
#46825=VECTOR ( 'NONE', #156202, 1000.000000000000114 ) ;
#46877=CARTESIAN_POINT ( 'NONE',  ( -0.4153311931459208184, 3.850000000000006306, -0.4999999999999961142 ) ) ;
#46879=ORIENTED_EDGE ( 'NONE', *, *, #117958, .T. ) ;
#46899=CARTESIAN_POINT ( 'NONE',  ( 1.364683531249997417, 12.04687500034139980, 2.602085213965210642E-15 ) ) ;
#46960=CARTESIAN_POINT ( 'NONE',  ( -1.364683531250010295, 10.19270833367473017, 0.7879004041258445001 ) ) ;
#46969=EDGE_CURVE ( 'NONE', #144059, #39789, #114355, .T. ) ;
#47002=CARTESIAN_POINT ( 'NONE',  ( -6.009258394948636914E-15, 9.468750000682799595, -1.732050807568875195 ) ) ;
#47004=EDGE_LOOP ( 'NONE', ( #88548, #65060, #37529, #107599 ) ) ;
#47127=CARTESIAN_POINT ( 'NONE',  ( -1.467608305004828750, 3.323697079694280632, -0.3199191423968864023 ) ) ;
#47146=CARTESIAN_POINT ( 'NONE',  ( -1.364683531250000748, 9.359375000341396245, 0.000000000000000000 ) ) ;
#47219=CARTESIAN_POINT ( 'NONE',  ( 0.6823417656249969321, 14.08854166700806232, -1.181850606188757036 ) ) ;
#47378=CARTESIAN_POINT ( 'NONE',  ( 4.764381983412778688E-15, 12.93749999999999645, -1.499999999999998446 ) ) ;
#47407=CARTESIAN_POINT ( 'NONE',  ( -1.500000000000015099, 11.22916666666666963, -0.8660254037844309360 ) ) ;
#47412=CARTESIAN_POINT ( 'NONE',  ( -1.364683531250010295, 8.880208333674731946, 0.7879004041258445001 ) ) ;
#47421=CARTESIAN_POINT ( 'NONE',  ( -2.926243505372967280E-18, -4.140708350189166609, -0.9999999999999991118 ) ) ;
#47446=CARTESIAN_POINT ( 'NONE',  ( -1.364683531250000748, 10.17187500034139802, 0.000000000000000000 ) ) ;
#47521=CARTESIAN_POINT ( 'NONE',  ( -6.009258394948636914E-15, 14.46875000068279249, -1.732050807568875195 ) ) ;
#47534=VERTEX_POINT ( 'NONE', #122912 ) ;
#47558=CARTESIAN_POINT ( 'NONE',  ( -8.012344526598182026E-15, 9.296875000341398021, -1.575800808251669460 ) ) ;
#47562=ORIENTED_EDGE ( 'NONE', *, *, #105381, .T. ) ;
#47571=CARTESIAN_POINT ( 'NONE',  ( -1.115562610750309283E-14, 10.84375000068279604, 1.500000000000001554 ) ) ;
#47614=DIRECTION ( 'NONE',  ( 0.000000000000000000, 0.000000000000000000, 1.000000000000000000 ) ) ;
#47647=ADVANCED_FACE ( 'NONE', ( #23147 ), #174790, .T. ) ;
#47666=CARTESIAN_POINT ( 'NONE',  ( 1.364683531249997417, 11.98437500034139980, 2.602085213965210642E-15 ) ) ;
#47683=DIRECTION ( 'NONE',  ( 0.000000000000000000, 1.000000000000000000, 0.000000000000000000 ) ) ;
#47707=CARTESIAN_POINT ( 'NONE',  ( 1.364683531250000303, 8.567708333674730170, -0.7879004041258355073 ) ) ;
#47758=VERTEX_POINT ( 'NONE', #181157 ) ;
#47765=CARTESIAN_POINT ( 'NONE',  ( 0.7500000000000006661, 11.33333333333333393, 1.299038105676657340 ) ) ;
#47766=ADVANCED_FACE ( 'NONE', ( #210448 ), #159579, .T. ) ;
#47767=CARTESIAN_POINT ( 'NONE',  ( 1.836970198721030181E-16, 13.49999999999999822, 1.500000000000000222 ) ) ;
#47787=CARTESIAN_POINT ( 'NONE',  ( -0.7500000000000179856, 9.822916667349467446, 1.299038105676658228 ) ) ;
#47795=CARTESIAN_POINT ( 'NONE',  ( -0.4019237886467001974, 8.332585450998168497, 1.500000000000001998 ) ) ;
#47799=ORIENTED_EDGE ( 'NONE', *, *, #188668, .T. ) ;
#47824=CARTESIAN_POINT ( 'NONE',  ( -8.012344526598182026E-15, 12.54687500034139624, -1.575800808251669460 ) ) ;
#47837=CARTESIAN_POINT ( 'NONE',  ( -1.493932498646918017, 4.331812005461956439, -0.1507059531854464673 ) ) ;
#47895=EDGE_CURVE ( 'NONE', #177149, #104840, #194208, .T. ) ;
#47918=CARTESIAN_POINT ( 'NONE',  ( 1.500000000000001332, 10.12500000000000178, 0.000000000000000000 ) ) ;
#47973=CARTESIAN_POINT ( 'NONE',  ( -1.364683531250014514, 12.40104166700806054, -0.7879004041258335089 ) ) ;
#48036=CARTESIAN_POINT ( 'NONE',  ( -1.364683531250000748, 9.921875000341398021, 0.000000000000000000 ) ) ;
#48078=CARTESIAN_POINT ( 'NONE',  ( 0.7500000000000006661, 9.697916667349467446, -1.299038105676657340 ) ) ;
#48179=CARTESIAN_POINT ( 'NONE',  ( 1.315333408008315441, 4.153791529306043451, 0.4024190470832924582 ) ) ;
#48196=CARTESIAN_POINT ( 'NONE',  ( -1.445243771768972785, 3.563465185575238614, -0.4166150551214558573 ) ) ;
#48215=CARTESIAN_POINT ( 'NONE',  ( -0.6823417656250003738, 8.901041667008065872, 1.181850606188754593 ) ) ;
#48283=CARTESIAN_POINT ( 'NONE',  ( 0.6823417656249934904, 14.75520833367473195, 1.181850606188764807 ) ) ;
#48301=VERTEX_POINT ( 'NONE', #186485 ) ;
#48363=DIRECTION ( 'NONE',  ( 8.659560562354941486E-17, -0.7071067811865469066, 0.7071067811865482389 ) ) ;
#48436=AXIS2_PLACEMENT_3D ( 'NONE', #155352, #70866, #212621 ) ;
#48468=CARTESIAN_POINT ( 'NONE',  ( -1.500000000000008216, 10.74999999999999645, 3.469446951953614189E-15 ) ) ;
#48472=CARTESIAN_POINT ( 'NONE',  ( 1.364683531249996529, 9.213541667008062319, 0.7879004041258405033 ) ) ;
#48481=CARTESIAN_POINT ( 'NONE',  ( -0.3982008013781589417, -4.205834154662571933, -0.9999999999999991118 ) ) ;
#48505=CARTESIAN_POINT ( 'NONE',  ( 1.364683531249997417, 11.29687500034139802, 2.602085213965210642E-15 ) ) ;
#48518=CARTESIAN_POINT ( 'NONE',  ( -2.788906526875773208E-15, 8.687500000000000000, -1.499999999999998446 ) ) ;
#48520=CARTESIAN_POINT ( 'NONE',  ( 0.000000000000000000, 13.49999999999999822, 0.000000000000000000 ) ) ;
#48579=CARTESIAN_POINT ( 'NONE',  ( -1.402160292154681736E-14, 12.34375000068279782, 1.732050807568881190 ) ) ;
#48612=CARTESIAN_POINT ( 'NONE',  ( -1.364683531250010295, 9.630208333674735499, 0.7879004041258445001 ) ) ;
#48632=EDGE_LOOP ( 'NONE', ( #92468, #51733 ) ) ;
#48757=CARTESIAN_POINT ( 'NONE',  ( 1.364683531249996529, 8.776041667008067648, 0.7879004041258405033 ) ) ;
#48810=LINE ( 'NONE', #47767, #8420 ) ;
#48833=LINE ( 'NONE', #147401, #96268 ) ;
#48858=CARTESIAN_POINT ( 'NONE',  ( 0.4839601414735513196, 4.104060063207238152, -0.4353502767700700438 ) ) ;
#48867=CARTESIAN_POINT ( 'NONE',  ( -1.364683531250010295, 12.88020833367473372, 0.7879004041258445001 ) ) ;
#48897=EDGE_CURVE ( 'NONE', #37159, #112702, #26446, .T. ) ;
#48949=EDGE_CURVE ( 'NONE', #73128, #31261, #26490, .T. ) ;
#49018=CARTESIAN_POINT ( 'NONE',  ( -1.364683531250014514, 12.90104166700806232, -0.7879004041258335089 ) ) ;
#49083=CARTESIAN_POINT ( 'NONE',  ( 1.364683531249997417, 10.04687500034139802, 2.602085213965210642E-15 ) ) ;
#49127=CARTESIAN_POINT ( 'NONE',  ( 0.7500000000000006661, 9.364583334016129967, 1.299038105676657340 ) ) ;
#49195=ADVANCED_FACE ( 'NONE', ( #199554 ), #154033, .T. ) ;
#49204=CARTESIAN_POINT ( 'NONE',  ( -0.4019237886466933696, 12.83258545099817027, 1.500000000000005995 ) ) ;
#49264=CARTESIAN_POINT ( 'NONE',  ( -1.402160292154681736E-14, 9.421875000341398021, 1.575800808251682339 ) ) ;
#49335=ADVANCED_FACE ( 'NONE', ( #34923, #170266 ), #1344, .F. ) ;
#49336=CARTESIAN_POINT ( 'NONE',  ( -0.6823417656250039265, 14.13020833367473195, -1.181850606188755259 ) ) ;
#49343=CARTESIAN_POINT ( 'NONE',  ( 0.000000000000000000, 0.000000000000000000, 0.000000000000000000 ) ) ;
#49372=EDGE_CURVE ( 'NONE', #195805, #170920, #21852, .T. ) ;
#49482=CARTESIAN_POINT ( 'NONE',  ( -1.500000000000001110, 13.02083333333333393, 0.8660254037844418162 ) ) ;
#49488=CARTESIAN_POINT ( 'NONE',  ( -3.602337597214539753E-15, 11.84375000068279604, 1.500000000000001554 ) ) ;
#49510=CARTESIAN_POINT ( 'NONE',  ( 1.499999999999997113, 11.64583333333333748, -0.8660254037844378194 ) ) ;
#49515=CARTESIAN_POINT ( 'NONE',  ( -1.364683531250014514, 9.588541667008064096, -0.7879004041258335089 ) ) ;
#49523=CARTESIAN_POINT ( 'NONE',  ( -0.4153311931458959494, 3.850000000000006306, 0.5000000000000064393 ) ) ;
#49549=CARTESIAN_POINT ( 'NONE',  ( 1.364683531249997417, 10.79687500034139802, 2.602085213965210642E-15 ) ) ;
#49564=CARTESIAN_POINT ( 'NONE',  ( 3.834746474454188013E-15, 10.81250000000000355, 1.500000000000001554 ) ) ;
#49574=DIRECTION ( 'NONE',  ( 0.000000000000000000, 0.000000000000000000, -1.000000000000000000 ) ) ;
#49580=EDGE_CURVE ( 'NONE', #190224, #144059, #25186, .T. ) ;
#49624=CARTESIAN_POINT ( 'NONE',  ( -1.500000000000015099, 13.01041666734946567, -0.8660254037844309360 ) ) ;
#49707=ORIENTED_EDGE ( 'NONE', *, *, #42099, .T. ) ;
#49807=CARTESIAN_POINT ( 'NONE',  ( -1.329432108394029477, 13.36331283326043007, 0.3989760537385304007 ) ) ;
#49815=CARTESIAN_POINT ( 'NONE',  ( -0.7500000000000179856, 12.07291666734946389, 1.299038105676658228 ) ) ;
#49874=( BOUNDED_CURVE ( )  B_SPLINE_CURVE ( 2, ( #137698, #107383, #187490, #56437, #152866, #138766, #40190, #170172, #73746 ),
 .UNSPECIFIED., .F., .T. ) 
 B_SPLINE_CURVE_WITH_KNOTS ( ( 3, 2, 2, 2, 3 ),
 ( 0.6339285714285713969, 0.6369047619047618625, 0.6428571428571429047, 0.6488095238095238360, 0.6517857142857143016 ),
 .UNSPECIFIED. ) 
 CURVE ( )  GEOMETRIC_REPRESENTATION_ITEM ( )  RATIONAL_B_SPLINE_CURVE ( ( 0.9330127018922194093, 0.9330127018922194093, 1.000000000000000000, 0.8660254037844387076, 1.000000000000000000, 0.8660254037844387076, 1.000000000000000000, 0.9330127018922194093, 0.9330127018922194093 ) ) 
 REPRESENTATION_ITEM ( '' )  );
#49914=CARTESIAN_POINT ( 'NONE',  ( 0.6383513625407178926, 4.335081533326786918, -0.1381026099400640694 ) ) ;
#49923=CARTESIAN_POINT ( 'NONE',  ( -0.6823417656250003738, 11.15104166700806765, 1.181850606188754593 ) ) ;
#49952=CARTESIAN_POINT ( 'NONE',  ( 1.340960183756584767, 13.31717403215611739, 0.4859952365426111198 ) ) ;
#49982=ORIENTED_EDGE ( 'NONE', *, *, #96366, .F. ) ;
#50065=CARTESIAN_POINT ( 'NONE',  ( 1.836970198721030181E-16, 13.49999999999999822, 1.500000000000000222 ) ) ;
#50077=CARTESIAN_POINT ( 'NONE',  ( -1.364683531250010295, 12.94270833367473550, 0.7879004041258445001 ) ) ;
#50127=CARTESIAN_POINT ( 'NONE',  ( 0.6823417656249934904, 12.69270833367473017, 1.181850606188764807 ) ) ;
#50132=CARTESIAN_POINT ( 'NONE',  ( 1.154700538379228147, -2.500000000000002220, -1.734723475976807094E-15 ) ) ;
#50139=CARTESIAN_POINT ( 'NONE',  ( 0.6823417656249969321, 10.58854166700806587, -1.181850606188757036 ) ) ;
#50182=CARTESIAN_POINT ( 'NONE',  ( -1.364683531250010295, 15.13020833367473017, 0.7879004041258445001 ) ) ;
#50283=CARTESIAN_POINT ( 'NONE',  ( -1.500000000000001110, 9.270833333333332149, 0.8660254037844418162 ) ) ;
#50287=CARTESIAN_POINT ( 'NONE',  ( 1.500000000000001332, 9.406250000682799595, 0.000000000000000000 ) ) ;
#50364=EDGE_LOOP ( 'NONE', ( #155597, #184831, #181326, #169359 ) ) ;
#50388=CARTESIAN_POINT ( 'NONE',  ( -1.402160292154681736E-14, 14.98437500034140157, 1.575800808251682339 ) ) ;
#50469=CARTESIAN_POINT ( 'NONE',  ( -2.788906526875773208E-15, 13.21875000068279604, -1.499999999999998446 ) ) ;
#50500=CARTESIAN_POINT ( 'NONE',  ( 1.499999999999993117, 12.88541666734946567, 0.8660254037844408170 ) ) ;
#50562=CARTESIAN_POINT ( 'NONE',  ( 1.499999999999996891, 13.17708333401612997, -0.8660254037844378194 ) ) ;
#50563=FACE_OUTER_BOUND ( 'NONE', #71758, .T. ) ;
#50574=CARTESIAN_POINT ( 'NONE',  ( -6.009258394948636914E-15, 10.68750000000000355, -1.732050807568875195 ) ) ;
#50579=CARTESIAN_POINT ( 'NONE',  ( 0.6823417656249969321, 8.526041667008064096, -1.181850606188757036 ) ) ;
#50614=EDGE_LOOP ( 'NONE', ( #135576, #25025, #41459, #198299, #16293 ) ) ;
#50619=CARTESIAN_POINT ( 'NONE',  ( -8.012344526598182026E-15, 10.35937500034139624, -1.575800808251669460 ) ) ;
#50675=CARTESIAN_POINT ( 'NONE',  ( 1.500000000000001332, 8.625000000000000000, 0.000000000000000000 ) ) ;
#50693=CARTESIAN_POINT ( 'NONE',  ( -1.500000000000015099, 12.51041666734946212, -0.8660254037844309360 ) ) ;
#50740=CARTESIAN_POINT ( 'NONE',  ( -0.7500000000000179856, 11.32291666734946212, 1.299038105676658228 ) ) ;
#50742=CARTESIAN_POINT ( 'NONE',  ( 0.000000000000000000, -4.500000000000003553, 2.000000000000000000 ) ) ;
#50782=CARTESIAN_POINT ( 'NONE',  ( -8.012344526598182026E-15, 13.29687500034140157, -1.575800808251669460 ) ) ;
#50838=CARTESIAN_POINT ( 'NONE',  ( 0.6823417656249969321, 12.02604166700806054, -1.181850606188757036 ) ) ;
#50876=CARTESIAN_POINT ( 'NONE',  ( 0.6823417656249969321, 8.838541667008065872, -1.181850606188757036 ) ) ;
#50965=FACE_BOUND ( 'NONE', #191319, .T. ) ;
#50990=CARTESIAN_POINT ( 'NONE',  ( -1.364683531250010295, 11.13020833367473372, 0.7879004041258445001 ) ) ;
#50993=CARTESIAN_POINT ( 'NONE',  ( -2.788906526875773208E-15, 12.96875000068279782, -1.499999999999998446 ) ) ;
#51021=CARTESIAN_POINT ( 'NONE',  ( 0.09230638003325472574, 13.28780466659584292, 1.452645848652445171 ) ) ;
#51139=CARTESIAN_POINT ( 'NONE',  ( 0.6823417656249969321, 12.08854166700806765, -1.181850606188757036 ) ) ;
#51208=CARTESIAN_POINT ( 'NONE',  ( -8.012344526598182026E-15, 9.859375000341399797, -1.575800808251669460 ) ) ;
#51249=CARTESIAN_POINT ( 'NONE',  ( -1.402160292154681736E-14, 8.343750000682796042, 1.732050807568881190 ) ) ;
#51390=CARTESIAN_POINT ( 'NONE',  ( -0.5773502691896261751, -2.500000000000002220, -0.9999999999999991118 ) ) ;
#51444=ORIENTED_EDGE ( 'NONE', *, *, #134419, .F. ) ;
#51460=CARTESIAN_POINT ( 'NONE',  ( 1.364683531249997417, 14.54687500034139447, 2.602085213965210642E-15 ) ) ;
#51634=EDGE_CURVE ( 'NONE', #45033, #95692, #190979, .T. ) ;
#51651=CARTESIAN_POINT ( 'NONE',  ( 1.364683531249997417, 11.73437500034139802, 2.602085213965210642E-15 ) ) ;
#51657=CARTESIAN_POINT ( 'NONE',  ( -1.402160292154681736E-14, 9.312500000000005329, 1.732050807568881190 ) ) ;
#51663=VECTOR ( 'NONE', #209932, 1000.000000000000000 ) ;
#51668=VECTOR ( 'NONE', #18155, 1000.000000000000000 ) ;
#51704=CARTESIAN_POINT ( 'NONE',  ( -1.364683531250014514, 9.901041667008064096, -0.7879004041258335089 ) ) ;
#51733=ORIENTED_EDGE ( 'NONE', *, *, #112300, .F. ) ;
#51753=CARTESIAN_POINT ( 'NONE',  ( -0.4019237886467001974, 11.58258545099816494, 1.500000000000001998 ) ) ;
#51763=CARTESIAN_POINT ( 'NONE',  ( 3.834746474454188013E-15, 12.31250000000000178, 1.500000000000001554 ) ) ;
#51778=CARTESIAN_POINT ( 'NONE',  ( -1.500000000000001110, 12.55208333401612641, 0.8660254037844419273 ) ) ;
#51849=CARTESIAN_POINT ( 'NONE',  ( -0.3982008013818653658, -4.205834154663907754, 1.000000000000004663 ) ) ;
#51863=CARTESIAN_POINT ( 'NONE',  ( 1.364683531249997417, 13.73437500034139980, 2.602085213965210642E-15 ) ) ;
#51875=B_SPLINE_CURVE_WITH_KNOTS ( 'NONE', 3,
 ( #120112, #65916, #151484, #85398, #185015, #33448, #69123, #202324, #201258, #102725, #21436, #132063, #84332, #198074 ),
 .UNSPECIFIED., .F., .F.,
 ( 4, 2, 2, 2, 2, 2, 4 ),
 ( 0.003709280639842194114, 0.003956362438780341648, 0.004203444237718488748, 0.004697607835594784682, 0.004944689634532932650, 0.005191771433471080617, 0.005685935031347376552 ),
 .UNSPECIFIED. ) ;
#51914=CARTESIAN_POINT ( 'NONE',  ( -1.364683531250014514, 12.33854166700806054, -0.7879004041258335089 ) ) ;
#51944=CARTESIAN_POINT ( 'NONE',  ( 0.5773502691896124084, -4.295408888568413630, -0.9999999999999991118 ) ) ;
#51962=CARTESIAN_POINT ( 'NONE',  ( -0.5368768833858145184, 13.37576698399828246, -1.254641125003840507 ) ) ;
#51991=FACE_OUTER_BOUND ( 'NONE', #26970, .T. ) ;
#52007=CARTESIAN_POINT ( 'NONE',  ( 3.834746474454188013E-15, 10.56250000000000178, 1.500000000000001554 ) ) ;
#52056=CARTESIAN_POINT ( 'NONE',  ( -1.364683531250010295, 11.63020833367472839, 0.7879004041258445001 ) ) ;
#52086=CARTESIAN_POINT ( 'NONE',  ( 1.344440581753393538, 13.33325798258003481, -0.4256415601542729021 ) ) ;
#52109=PRODUCT_DEFINITION ( 'UNKNOWN', '', #79968, #182500 ) ;
#52184=ORIENTED_EDGE ( 'NONE', *, *, #55165, .F. ) ;
#52205=CARTESIAN_POINT ( 'NONE',  ( -1.364683531250000748, 11.42187500034139802, 0.000000000000000000 ) ) ;
#52247=ORIENTED_EDGE ( 'NONE', *, *, #9604, .T. ) ;
#52272=CARTESIAN_POINT ( 'NONE',  ( -0.6823417656250039265, 9.130208333674726617, -1.181850606188755259 ) ) ;
#52276=B_SPLINE_CURVE_WITH_KNOTS ( 'NONE', 3,
 ( #171719, #107863, #75293, #173889, #73133, #103530, #72063, #170651, #5992, #138173 ),
 .UNSPECIFIED., .F., .F.,
 ( 4, 2, 2, 2, 4 ),
 ( 0.001822879634083279061, 0.002175306537177320535, 0.002527733440271361792, 0.002880160343365403049, 0.003232587246459444306 ),
 .UNSPECIFIED. ) ;
#52312=CARTESIAN_POINT ( 'NONE',  ( -8.012344526598182026E-15, 15.29687500034140157, -1.575800808251669460 ) ) ;
#52316=VECTOR ( 'NONE', #147861, 1000.000000000000000 ) ;
#52386=CARTESIAN_POINT ( 'NONE',  ( 1.499999999999993117, 10.60416666666666607, 0.8660254037844408170 ) ) ;
#52513=CARTESIAN_POINT ( 'NONE',  ( 1.364683531249996529, 13.52604166700806587, 0.7879004041258405033 ) ) ;
#52555=ORIENTED_EDGE ( 'NONE', *, *, #61890, .T. ) ;
#52599=CARTESIAN_POINT ( 'NONE',  ( -1.500000000000008216, 11.03125000068279427, 3.469446951953614189E-15 ) ) ;
#52654=CARTESIAN_POINT ( 'NONE',  ( 1.836970198721030181E-16, 13.49999999999999822, 1.500000000000000222 ) ) ;
#52679=CARTESIAN_POINT ( 'NONE',  ( -1.432341765625004593, 8.460937500170699010, 8.673617379884035472E-16 ) ) ;
#52698=CARTESIAN_POINT ( 'NONE',  ( 0.6823417656249934904, 12.19270833367473017, 1.181850606188764807 ) ) ;
#52704=CARTESIAN_POINT ( 'NONE',  ( -6.009258394948636914E-15, 9.937500000000000000, -1.732050807568875195 ) ) ;
#52751=CARTESIAN_POINT ( 'NONE',  ( 1.364683531250000748, 9.567708333674735499, -0.7879004041258355073 ) ) ;
#52766=CARTESIAN_POINT ( 'NONE',  ( -2.788906526875773208E-15, 12.46875000068279782, -1.499999999999998446 ) ) ;
#52812=CARTESIAN_POINT ( 'NONE',  ( -1.500000000000008216, 9.281250000682799595, 3.469446951953614189E-15 ) ) ;
#52814=ORIENTED_EDGE ( 'NONE', *, *, #98379, .T. ) ;
#52825=CARTESIAN_POINT ( 'NONE',  ( 1.499999999999993117, 12.13541666734946212, 0.8660254037844409281 ) ) ;
#52835=CARTESIAN_POINT ( 'NONE',  ( -3.602337597214539753E-15, 12.81249999999999822, 1.500000000000001554 ) ) ;
#52875=CARTESIAN_POINT ( 'NONE',  ( 1.264911064067348656, 3.849999999999994316, 0.5000000000000064393 ) ) ;
#52914=CARTESIAN_POINT ( 'NONE',  ( 1.364683531249997417, 12.73437500034139980, 2.602085213965210642E-15 ) ) ;
#52925=CARTESIAN_POINT ( 'NONE',  ( -2.788906526875773208E-15, 12.21875000068279782, -1.499999999999998446 ) ) ;
#52935=CARTESIAN_POINT ( 'NONE',  ( 1.309956906536929200, 3.548345970690609974, 0.4145166106152374796 ) ) ;
#52956=CARTESIAN_POINT ( 'NONE',  ( -1.402160292154681736E-14, 13.56250000000000000, 1.732050807568881190 ) ) ;
#52962=CARTESIAN_POINT ( 'NONE',  ( -1.364683531250010295, 12.38020833367473372, 0.7879004041258445001 ) ) ;
#53011=CARTESIAN_POINT ( 'NONE',  ( 1.364683531249996529, 13.27604166700806765, 0.7879004041258403923 ) ) ;
#53094=CARTESIAN_POINT ( 'NONE',  ( 0.000000000000000000, 13.49999999999999822, -1.500000000000000222 ) ) ;
#53112=CARTESIAN_POINT ( 'NONE',  ( -1.364683531250010295, 11.38020833367473728, 0.7879004041258445001 ) ) ;
#53209=( BOUNDED_CURVE ( )  B_SPLINE_CURVE ( 2, ( #172382, #156136, #7718, #139896, #27176, #62876, #79129, #177716, #109582 ),
 .UNSPECIFIED., .F., .T. ) 
 B_SPLINE_CURVE_WITH_KNOTS ( ( 3, 2, 2, 2, 3 ),
 ( 0.8660714285714286031, 0.8690476190476190688, 0.8750000000000000000, 0.8809523809523809312, 0.8839285714285713969 ),
 .UNSPECIFIED. ) 
 CURVE ( )  GEOMETRIC_REPRESENTATION_ITEM ( )  RATIONAL_B_SPLINE_CURVE ( ( 0.9330127018922194093, 0.9330127018922194093, 1.000000000000000000, 0.8660254037844387076, 1.000000000000000000, 0.8660254037844387076, 1.000000000000000000, 0.9330127018922194093, 0.9330127018922194093 ) ) 
 REPRESENTATION_ITEM ( '' )  );
#53267=CARTESIAN_POINT ( 'NONE',  ( -1.364683531250010295, 11.44270833367472662, 0.7879004041258445001 ) ) ;
#53291=CARTESIAN_POINT ( 'NONE',  ( -0.6823417656250039265, 15.31770833367473372, -1.181850606188755259 ) ) ;
#53332=CARTESIAN_POINT ( 'NONE',  ( 1.364683531250000303, 9.567708333674735499, -0.7879004041258355073 ) ) ;
#53373=CARTESIAN_POINT ( 'NONE',  ( -1.500000000000008216, 9.031250000682797818, 3.469446951953614189E-15 ) ) ;
#53502=VECTOR ( 'NONE', #172165, 1000.000000000000000 ) ;
#53521=CYLINDRICAL_SURFACE ( 'NONE', #163548, 1.500000000000000222 ) ;
#53581=CARTESIAN_POINT ( 'NONE',  ( -0.6823417656250003738, 12.96354166700806942, 1.181850606188754593 ) ) ;
#53600=( BOUNDED_CURVE ( )  B_SPLINE_CURVE ( 2, ( #153524, #85309, #134099, #2965, #50675, #83163, #102636, #184926, #168693 ),
 .UNSPECIFIED., .F., .T. ) 
 B_SPLINE_CURVE_WITH_KNOTS ( ( 3, 2, 2, 2, 3 ),
 ( 0.9732142857142856984, 0.9761904761904761640, 0.9821428571428570953, 0.9880952380952381375, 0.9910714285714286031 ),
 .UNSPECIFIED. ) 
 CURVE ( )  GEOMETRIC_REPRESENTATION_ITEM ( )  RATIONAL_B_SPLINE_CURVE ( ( 0.9330127018922194093, 0.9330127018922194093, 1.000000000000000000, 0.8660254037844387076, 1.000000000000000000, 0.8660254037844387076, 1.000000000000000000, 0.9330127018922194093, 0.9330127018922194093 ) ) 
 REPRESENTATION_ITEM ( '' )  );
#53775=CARTESIAN_POINT ( 'NONE',  ( 1.364683531249996529, 12.21354166700805877, 0.7879004041258403923 ) ) ;
#53780=CARTESIAN_POINT ( 'NONE',  ( -6.009258394948636914E-15, 9.437499999999996447, -1.732050807568875195 ) ) ;
#53832=CARTESIAN_POINT ( 'NONE',  ( 1.364683531250000748, 8.817708333674731946, -0.7879004041258355073 ) ) ;
#53901=CARTESIAN_POINT ( 'NONE',  ( -6.009258394948636914E-15, 10.96875000068279249, -1.732050807568875195 ) ) ;
#53964=ORIENTED_EDGE ( 'NONE', *, *, #84877, .T. ) ;
#53976=FACE_OUTER_BOUND ( 'NONE', #117626, .T. ) ;
#53988=CARTESIAN_POINT ( 'NONE',  ( -1.364683531250010295, 13.13020833367472839, 0.7879004041258445001 ) ) ;
#53998=CARTESIAN_POINT ( 'NONE',  ( -1.115562610750309283E-14, 11.59375000068279604, 1.500000000000001554 ) ) ;
#54034=CARTESIAN_POINT ( 'NONE',  ( -0.7500000000000179856, 13.29166666666666607, 1.299038105676658228 ) ) ;
#54042=CARTESIAN_POINT ( 'NONE',  ( -1.364683531250000748, 11.85937500034139802, 0.000000000000000000 ) ) ;
#54096=CARTESIAN_POINT ( 'NONE',  ( -0.7500000000000006661, 12.23958333401613174, -1.299038105676657340 ) ) ;
#54131=DIRECTION ( 'NONE',  ( 0.000000000000000000, 1.000000000000000000, 0.000000000000000000 ) ) ;
#54155=CARTESIAN_POINT ( 'NONE',  ( -1.500000000000001110, 14.80208333401612997, 0.8660254037844419273 ) ) ;
#54163=EDGE_LOOP ( 'NONE', ( #108356, #145038, #171104, #152327 ) ) ;
#54185=CARTESIAN_POINT ( 'NONE',  ( -1.364683531250014514, 11.33854166700806410, -0.7879004041258335089 ) ) ;
#54197=EDGE_CURVE ( 'NONE', #179060, #14542, #3016, .T. ) ;
#54270=ORIENTED_EDGE ( 'NONE', *, *, #104314, .T. ) ;
#54296=CARTESIAN_POINT ( 'NONE',  ( -1.350866880800077663, 3.446184751535887436, 0.3155278943301856320 ) ) ;
#54324=B_SPLINE_CURVE_WITH_KNOTS ( 'NONE', 3,
 ( #32442, #109771, #175778, #140090, #11110, #209298, #143307, #60946, #206115, #127102, #193067, #44719, #81191, #35622 ),
 .UNSPECIFIED., .F., .F.,
 ( 4, 2, 2, 2, 2, 2, 4 ),
 ( 0.001731424703407325729, 0.001978656695461683979, 0.002225888687516043747, 0.002720352671624761548, 0.002967584663679120015, 0.003214816655733478482, 0.003709280639842196282 ),
 .UNSPECIFIED. ) ;
#54342=CARTESIAN_POINT ( 'NONE',  ( 1.364683531250000303, 11.31770833367473550, -0.7879004041258355073 ) ) ;
#54367=FACE_OUTER_BOUND ( 'NONE', #50364, .T. ) ;
#54401=VECTOR ( 'NONE', #160936, 1000.000000000000000 ) ;
#54408=CARTESIAN_POINT ( 'NONE',  ( -0.6823417656250003738, 8.963541667008065872, 1.181850606188754593 ) ) ;
#54421=CARTESIAN_POINT ( 'NONE',  ( 0.4019237886466778820, 9.604914550367428916, 1.500000000000001554 ) ) ;
#54450=CARTESIAN_POINT ( 'NONE',  ( -1.500000000000001110, 9.052083334016126415, 0.8660254037844419273 ) ) ;
#54461=LINE ( 'NONE', #206027, #14505 ) ;
#54483=CARTESIAN_POINT ( 'NONE',  ( 1.063464886906835938, -4.211945764156021177, -0.1580247838118454540 ) ) ;
#54588=CARTESIAN_POINT ( 'NONE',  ( -1.364683531250014514, 8.588541667008067648, -0.7879004041258335089 ) ) ;
#54598=ORIENTED_EDGE ( 'NONE', *, *, #96366, .T. ) ;
#54635=CARTESIAN_POINT ( 'NONE',  ( -0.7500000000000179856, 8.791666666666669627, 1.299038105676658228 ) ) ;
#54647=CARTESIAN_POINT ( 'NONE',  ( -1.364683531250014514, 12.65104166700806232, -0.7879004041258335089 ) ) ;
#54692=VECTOR ( 'NONE', #209657, 1000.000000000000000 ) ;
#54695=CARTESIAN_POINT ( 'NONE',  ( -1.154700538379266339, -4.295408888568413630, 2.602085213965210642E-15 ) ) ;
#54713=EDGE_CURVE ( 'NONE', #162878, #147411, #114263, .T. ) ;
#54781=ORIENTED_EDGE ( 'NONE', *, *, #160757, .T. ) ;
#54842=CARTESIAN_POINT ( 'NONE',  ( 1.364683531249996529, 12.46354166700806232, 0.7879004041258403923 ) ) ;
#54848=CARTESIAN_POINT ( 'NONE',  ( -1.500000000000001110, 10.02083333333333393, 0.8660254037844419273 ) ) ;
#54865=CARTESIAN_POINT ( 'NONE',  ( 1.499999999999993117, 9.604166666666669627, 0.8660254037844408170 ) ) ;
#54895=CARTESIAN_POINT ( 'NONE',  ( -1.402160292154681736E-14, 8.734375000341403350, 1.575800808251682339 ) ) ;
#55056=CARTESIAN_POINT ( 'NONE',  ( -0.4019237886466933696, 12.55133545031537246, 1.500000000000005995 ) ) ;
#55057=CARTESIAN_POINT ( 'NONE',  ( 0.6823417656249969321, 13.02604166700806232, -1.181850606188757036 ) ) ;
#55081=CARTESIAN_POINT ( 'NONE',  ( 1.264911064067342217, 3.732455999420146053, -0.4999999999999988343 ) ) ;
#55103=CARTESIAN_POINT ( 'NONE',  ( 1.499999999999993117, 13.85416666666666430, 0.8660254037844409281 ) ) ;
#55110=CARTESIAN_POINT ( 'NONE',  ( 1.364683531249996529, 12.21354166700805877, 0.7879004041258405033 ) ) ;
#55154=CARTESIAN_POINT ( 'NONE',  ( -0.6823417656250039265, 12.88020833367473017, -1.181850606188755259 ) ) ;
#55165=EDGE_CURVE ( 'NONE', #173308, #42462, #44149, .T. ) ;
#55194=DIRECTION ( 'NONE',  ( 0.000000000000000000, 0.000000000000000000, -1.000000000000000000 ) ) ;
#55221=CARTESIAN_POINT ( 'NONE',  ( -1.402160292154681736E-14, 14.59375000068279249, 1.732050807568881190 ) ) ;
#55229=CARTESIAN_POINT ( 'NONE',  ( 0.000000000000000000, 13.49999999999999822, 0.000000000000000000 ) ) ;
#55232=EDGE_CURVE ( 'NONE', #8253, #147564, #32148, .T. ) ;
#55256=CARTESIAN_POINT ( 'NONE',  ( 1.364683531249996529, 10.71354166700806942, 0.7879004041258405033 ) ) ;
#55327=CARTESIAN_POINT ( 'NONE',  ( 3.834746474454188013E-15, 12.84375000068279782, 1.500000000000001554 ) ) ;
#55399=CARTESIAN_POINT ( 'NONE',  ( -1.402160292154681736E-14, 10.98437500034139802, 1.575800808251682339 ) ) ;
#55420=CARTESIAN_POINT ( 'NONE',  ( 0.4153311931458959494, 3.850000000000006306, 0.5000000000000064393 ) ) ;
#55425=CARTESIAN_POINT ( 'NONE',  ( 1.364683531249996529, 13.96354166700806765, 0.7879004041258405033 ) ) ;
#55458=CARTESIAN_POINT ( 'NONE',  ( -0.7500000000000179856, 13.07291666734946389, 1.299038105676658228 ) ) ;
#55466=CARTESIAN_POINT ( 'NONE',  ( -1.402160292154681736E-14, 8.484375000341403350, 1.575800808251682339 ) ) ;
#55474=ORIENTED_EDGE ( 'NONE', *, *, #165357, .F. ) ;
#55512=CARTESIAN_POINT ( 'NONE',  ( -1.364683531250000748, 14.10937500034140157, 0.000000000000000000 ) ) ;
#55524=CARTESIAN_POINT ( 'NONE',  ( -1.390311220213877652, 4.148202468850559654, -0.5641062960582055030 ) ) ;
#55549=CARTESIAN_POINT ( 'NONE',  ( 0.5773502691896124084, -4.295408888568413630, -0.9999999999999991118 ) ) ;
#55651=CARTESIAN_POINT ( 'NONE',  ( 0.6823417656249934904, 8.442708333674733723, 1.181850606188764807 ) ) ;
#55713=CARTESIAN_POINT ( 'NONE',  ( -1.402160292154681736E-14, 13.23437500034139980, 1.575800808251682339 ) ) ;
#55904=CARTESIAN_POINT ( 'NONE',  ( 0.6823417656249934904, 10.94270833367473550, 1.181850606188764807 ) ) ;
#55910=CARTESIAN_POINT ( 'NONE',  ( -1.500000000000001110, 9.520833333333333925, 0.8660254037844419273 ) ) ;
#55934=CARTESIAN_POINT ( 'NONE',  ( 3.834746474454188013E-15, 8.593750000682796042, 1.500000000000001554 ) ) ;
#55948=ORIENTED_EDGE ( 'NONE', *, *, #115096, .F. ) ;
#55966=CARTESIAN_POINT ( 'NONE',  ( 1.364683531249996529, 9.026041667008060543, 0.7879004041258403923 ) ) ;
#55974=ORIENTED_EDGE ( 'NONE', *, *, #98818, .T. ) ;
#55983=ADVANCED_FACE ( 'NONE', ( #11364 ), #4642, .F. ) ;
#56166=CARTESIAN_POINT ( 'NONE',  ( -1.500000000000008216, 13.24999999999999822, 3.469446951953614189E-15 ) ) ;
#56175=CARTESIAN_POINT ( 'NONE',  ( -1.364683531250000748, 11.10937500034139802, 0.000000000000000000 ) ) ;
#56179=CARTESIAN_POINT ( 'NONE',  ( 2.449293598294706414E-16, -1.500000000000001332, -2.000000000000000000 ) ) ;
#56199=LINE ( 'NONE', #169938, #93384 ) ;
#56220=CARTESIAN_POINT ( 'NONE',  ( -1.402160292154681736E-14, 13.23437500034139980, 1.575800808251682339 ) ) ;
#56238=EDGE_CURVE ( 'NONE', #78671, #42462, #91647, .T. ) ;
#56288=CARTESIAN_POINT ( 'NONE',  ( -1.500000000000015099, 15.26041666734946745, -0.8660254037844309360 ) ) ;
#56318=AXIS2_PLACEMENT_3D ( 'NONE', #100769, #70377, #151675 ) ;
#56321=CARTESIAN_POINT ( 'NONE',  ( -1.364683531250010295, 10.38020833367473195, 0.7879004041258445001 ) ) ;
#56376=ORIENTED_EDGE ( 'NONE', *, *, #108076, .T. ) ;
#56401=DIRECTION ( 'NONE',  ( 0.000000000000000000, -1.000000000000000000, 0.000000000000000000 ) ) ;
#56427=CARTESIAN_POINT ( 'NONE',  ( 1.220146605508150803E-14, 11.43749999999999822, -1.499999999999998446 ) ) ;
#56429=CARTESIAN_POINT ( 'NONE',  ( -1.115562610750309283E-14, 9.312500000000001776, 1.500000000000001554 ) ) ;
#56437=CARTESIAN_POINT ( 'NONE',  ( -1.500000000000001110, 11.02083333333333393, 0.8660254037844418162 ) ) ;
#56470=CARTESIAN_POINT ( 'NONE',  ( 1.364683531249997417, 11.54687500034139802, 2.602085213965210642E-15 ) ) ;
#56483=CARTESIAN_POINT ( 'NONE',  ( -0.7500000000000006661, 10.70833333333333393, -1.299038105676657340 ) ) ;
#56498=CARTESIAN_POINT ( 'NONE',  ( 1.364683531249997417, 14.48437500034140157, 2.602085213965210642E-15 ) ) ;
#56515=CARTESIAN_POINT ( 'NONE',  ( 1.500000000000001332, 10.37499999999999467, 0.000000000000000000 ) ) ;
#56540=CARTESIAN_POINT ( 'NONE',  ( -1.364683531250014514, 9.401041667008062319, -0.7879004041258335089 ) ) ;
#56588=CARTESIAN_POINT ( 'NONE',  ( -1.402160292154681736E-14, 14.67187500034139980, 1.575800808251682339 ) ) ;
#56597=CARTESIAN_POINT ( 'NONE',  ( -1.378728738066232307, 3.613591550242559070, -0.5908528300941753297 ) ) ;
#56615=PRESENTATION_STYLE_ASSIGNMENT (( #173596 ) ) ;
#56651=VECTOR ( 'NONE', #35831, 1000.000000000000000 ) ;
#56681=CARTESIAN_POINT ( 'NONE',  ( 0.7500000000000006661, 8.364583334016128191, 1.299038105676657340 ) ) ;
#56702=CARTESIAN_POINT ( 'NONE',  ( 1.430889623655247744, 4.024647178788855584, -0.4691377289697504227 ) ) ;
#56725=CARTESIAN_POINT ( 'NONE',  ( -0.6823417656250003738, 14.71354166700806410, 1.181850606188754593 ) ) ;
#56746=( BOUNDED_CURVE ( )  B_SPLINE_CURVE ( 2, ( #205179, #124048, #126173, #11260, #25380, #155387, #142379, #10196, #190014 ),
 .UNSPECIFIED., .F., .T. ) 
 B_SPLINE_CURVE_WITH_KNOTS ( ( 3, 2, 2, 2, 3 ),
 ( 0.5982142857142856984, 0.6011904761904761640, 0.6071428571428570953, 0.6130952380952381375, 0.6160714285714286031 ),
 .UNSPECIFIED. ) 
 CURVE ( )  GEOMETRIC_REPRESENTATION_ITEM ( )  RATIONAL_B_SPLINE_CURVE ( ( 0.9330127018922194093, 0.9330127018922194093, 1.000000000000000000, 0.8660254037844387076, 1.000000000000000000, 0.8660254037844387076, 1.000000000000000000, 0.9330127018922194093, 0.9330127018922194093 ) ) 
 REPRESENTATION_ITEM ( '' )  );
#56784=CARTESIAN_POINT ( 'NONE',  ( -1.364683531250014514, 12.40104166700806054, -0.7879004041258335089 ) ) ;
#56833=CARTESIAN_POINT ( 'NONE',  ( -0.5773502691960585853, -4.295408888567775918, 1.000000000000000888 ) ) ;
#56870=CARTESIAN_POINT ( 'NONE',  ( -0.4019237886467001974, 9.582585450998170273, 1.500000000000001998 ) ) ;
#56900=CARTESIAN_POINT ( 'NONE',  ( -2.788906526875773208E-15, 10.71875000068279604, -1.499999999999998446 ) ) ;
#56934=LINE ( 'NONE', #184779, #177314 ) ;
#56952=CARTESIAN_POINT ( 'NONE',  ( -2.788906526875773208E-15, 8.968750000682797818, -1.499999999999998446 ) ) ;
#56957=CARTESIAN_POINT ( 'NONE',  ( 1.310129046446480094, 4.152766000979581484, -0.4142140226951018245 ) ) ;
#56964=EDGE_CURVE ( 'NONE', #96430, #33125, #54324, .T. ) ;
#56974=CARTESIAN_POINT ( 'NONE',  ( 0.6823417656249934904, 10.69270833367473550, 1.181850606188764807 ) ) ;
#57058=AXIS2_PLACEMENT_3D ( 'NONE', #101806, #103952, #55194 ) ;
#57072=DIRECTION ( 'NONE',  ( 1.000000000000000000, 0.000000000000000000, 0.000000000000000000 ) ) ;
#57143=UNCERTAINTY_MEASURE_WITH_UNIT (LENGTH_MEASURE( 1.000000000000000082E-05 ), #178346, 'distance_accuracy_value', 'NONE');
#57173=ORIENTED_EDGE ( 'NONE', *, *, #135275, .F. ) ;
#57187=B_SPLINE_CURVE_WITH_KNOTS ( 'NONE', 3,
 ( #33694, #51021, #182062, #133369, #201501, #16360, #68306, #82438, #15299, #117143, #148528, #49952, #99770, #165836, #134437, #34750, #84580, #200440, #52086, #101900, #140839, #36886, #5428, #205786, #86713, #203634, #206851, #185262 ),
 .UNSPECIFIED., .F., .F.,
 ( 4, 2, 2, 2, 2, 2, 2, 2, 2, 2, 2, 2, 2, 4 ),
 ( 0.002695587478349080121, 0.002974090769189313352, 0.003252594060029546583, 0.003531097350869780247, 0.003809600641710013478, 0.004366607223390480373, 0.004645110514230714471, 0.004923613805070947702, 0.005202117095911182668, 0.005480620386751415031, 0.006037626968431882360, 0.006594633550112348822, 0.006873136840952582052, 0.007151640131792815283 ),
 .UNSPECIFIED. ) ;
#57238=CARTESIAN_POINT ( 'NONE',  ( 1.499999999999993117, 14.10416666666666607, 0.8660254037844409281 ) ) ;
#57243=CARTESIAN_POINT ( 'NONE',  ( -1.364683531250010295, 10.63020833367473195, 0.7879004041258445001 ) ) ;
#57287=CARTESIAN_POINT ( 'NONE',  ( 1.364683531249997417, 12.54687500034139980, 2.602085213965210642E-15 ) ) ;
#57292=CARTESIAN_POINT ( 'NONE',  ( -0.4019237886466933696, 12.33258545099817205, 1.500000000000005995 ) ) ;
#57314=CARTESIAN_POINT ( 'NONE',  ( -1.364683531250014514, 13.08854166700806410, -0.7879004041258335089 ) ) ;
#57383=CARTESIAN_POINT ( 'NONE',  ( 1.364683531249997417, 9.734375000341396245, 2.602085213965210642E-15 ) ) ;
#57528=CARTESIAN_POINT ( 'NONE',  ( -0.4019237886467001974, 11.80133545031536890, 1.500000000000001998 ) ) ;
#57539=CARTESIAN_POINT ( 'NONE',  ( -1.364683531250014514, 10.15104166700806587, -0.7879004041258335089 ) ) ;
#57563=CARTESIAN_POINT ( 'NONE',  ( -1.364683531250000748, 14.60937500034140157, 0.000000000000000000 ) ) ;
#57605=CARTESIAN_POINT ( 'NONE',  ( -0.7500000000000006661, 15.20833333333333748, -1.299038105676657340 ) ) ;
#57617=VERTEX_POINT ( 'NONE', #162200 ) ;
#57626=ORIENTED_EDGE ( 'NONE', *, *, #48949, .T. ) ;
#57628=ORIENTED_EDGE ( 'NONE', *, *, #18034, .T. ) ;
#57652=CARTESIAN_POINT ( 'NONE',  ( 1.364683531249996529, 14.71354166700806410, 0.7879004041258405033 ) ) ;
#57789=CARTESIAN_POINT ( 'NONE',  ( -8.012344526598182026E-15, 13.35937500034140157, -1.575800808251669460 ) ) ;
#57798=CARTESIAN_POINT ( 'NONE',  ( 1.500000000000001332, 12.40625000068279427, 0.000000000000000000 ) ) ;
#57849=CARTESIAN_POINT ( 'NONE',  ( -0.6823417656250003738, 11.21354166700806765, 1.181850606188754593 ) ) ;
#57890=CARTESIAN_POINT ( 'NONE',  ( -0.7500000000000006661, 10.98958333401613174, -1.299038105676657340 ) ) ;
#58035=CARTESIAN_POINT ( 'NONE',  ( 1.364683531250000748, 10.75520833367473195, -0.7879004041258355073 ) ) ;
#58055=ORIENTED_EDGE ( 'NONE', *, *, #104082, .F. ) ;
#58078=EDGE_LOOP ( 'NONE', ( #41981, #125831, #152772, #27462 ) ) ;
#58083=ORIENTED_EDGE ( 'NONE', *, *, #38859, .T. ) ;
#58168=ORIENTED_EDGE ( 'NONE', *, *, #27925, .F. ) ;
#58217=CARTESIAN_POINT ( 'NONE',  ( 1.499999999999996891, 11.89583333333333570, -0.8660254037844378194 ) ) ;
#58260=CARTESIAN_POINT ( 'NONE',  ( -0.4019237886466871523, 10.44866454968463110, -1.499999999999998668 ) ) ;
#58303=CARTESIAN_POINT ( 'NONE',  ( -1.500000000000015099, 11.72916666666666252, -0.8660254037844309360 ) ) ;
#58308=CARTESIAN_POINT ( 'NONE',  ( -0.6823417656250003738, 11.15104166700806765, 1.181850606188754593 ) ) ;
#58349=CARTESIAN_POINT ( 'NONE',  ( -1.364683531250014514, 11.65104166700806587, -0.7879004041258335089 ) ) ;
#58398=CARTESIAN_POINT ( 'NONE',  ( -2.788906526875773208E-15, 12.21875000068279782, -1.499999999999998446 ) ) ;
#58405=DIRECTION ( 'NONE',  ( 0.000000000000000000, -1.000000000000000000, 0.000000000000000000 ) ) ;
#58453=CARTESIAN_POINT ( 'NONE',  ( -8.012344526598182026E-15, 10.54687500034139624, -1.575800808251669460 ) ) ;
#58456=CARTESIAN_POINT ( 'NONE',  ( -1.115562610750309283E-14, 11.06250000000000178, 1.500000000000001554 ) ) ;
#58473=ORIENTED_EDGE ( 'NONE', *, *, #28769, .F. ) ;
#58548=CYLINDRICAL_SURFACE ( 'NONE', #189579, 1.500000000000000222 ) ;
#58577=FACE_BOUND ( 'NONE', #109527, .T. ) ;
#58601=CARTESIAN_POINT ( 'NONE',  ( -0.6823417656250039265, 9.380208333674728394, -1.181850606188755259 ) ) ;
#58615=ORIENTED_EDGE ( 'NONE', *, *, #186000, .F. ) ;
#58626=CARTESIAN_POINT ( 'NONE',  ( -1.402160292154681736E-14, 14.17187500034139624, 1.575800808251682339 ) ) ;
#58644=CARTESIAN_POINT ( 'NONE',  ( -1.115562610750309283E-14, 9.843750000682801371, 1.500000000000001554 ) ) ;
#58670=CARTESIAN_POINT ( 'NONE',  ( 1.499999999999997113, 15.14583333333333570, -0.8660254037844378194 ) ) ;
#58714=CARTESIAN_POINT ( 'NONE',  ( -1.364683531250000748, 14.35937500034140157, 0.000000000000000000 ) ) ;
#58777=CARTESIAN_POINT ( 'NONE',  ( 0.4019237886466778820, 11.35491455036742536, 1.500000000000001554 ) ) ;
#58855=CARTESIAN_POINT ( 'NONE',  ( -1.364683531250010295, 14.19270833367473195, 0.7879004041258445001 ) ) ;
#58887=EDGE_CURVE ( 'NONE', #8679, #47758, #69750, .T. ) ;
#58919=CARTESIAN_POINT ( 'NONE',  ( -8.012344526598182026E-15, 11.85937500034140157, -1.575800808251669460 ) ) ;
#58957=DIRECTION ( 'NONE',  ( 0.000000000000000000, 0.000000000000000000, -1.000000000000000000 ) ) ;
#58962=CARTESIAN_POINT ( 'NONE',  ( -0.7500000000000179856, 10.57291666734946212, 1.299038105676658228 ) ) ;
#59098=CARTESIAN_POINT ( 'NONE',  ( -8.012344526598182026E-15, 11.04687500034139624, -1.575800808251669460 ) ) ;
#59104=CARTESIAN_POINT ( 'NONE',  ( -6.009258394948636914E-15, 8.937500000000001776, -1.732050807568875195 ) ) ;
#59146=EDGE_LOOP ( 'NONE', ( #189951, #92646, #9762, #12088 ) ) ;
#59155=LINE ( 'NONE', #190212, #54401 ) ;
#59263=ORIENTED_EDGE ( 'NONE', *, *, #124881, .F. ) ;
#59276=CARTESIAN_POINT ( 'NONE',  ( 7.960204194457795477E-17, 13.49999999999999822, 0.6500000000000000222 ) ) ;
#59329=EDGE_CURVE ( 'NONE', #81332, #57617, #150018, .T. ) ;
#59364=CARTESIAN_POINT ( 'NONE',  ( 0.7500000000000006661, 12.16666666666666607, -1.299038105676657340 ) ) ;
#59370=CARTESIAN_POINT ( 'NONE',  ( -1.402160292154681736E-14, 11.17187500034139802, 1.575800808251682339 ) ) ;
#59386=LINE ( 'NONE', #174237, #128586 ) ;
#59409=CARTESIAN_POINT ( 'NONE',  ( 1.364683531250000748, 12.06770833367473195, -0.7879004041258355073 ) ) ;
#59463=LINE ( 'NONE', #211025, #141697 ) ;
#59477=CARTESIAN_POINT ( 'NONE',  ( -6.009258394948636914E-15, 13.46875000068279604, -1.732050807568875195 ) ) ;
#59508=CARTESIAN_POINT ( 'NONE',  ( 1.364683531249997417, 10.23437500034139802, 2.602085213965210642E-15 ) ) ;
#59513=LINE ( 'NONE', #191632, #94901 ) ;
#59656=DIRECTION ( 'NONE',  ( 0.000000000000000000, -1.000000000000000000, 0.000000000000000000 ) ) ;
#59662=CARTESIAN_POINT ( 'NONE',  ( 1.364683531250000303, 9.817708333674735499, -0.7879004041258355073 ) ) ;
#59674=CARTESIAN_POINT ( 'NONE',  ( 1.266973501737285845, 3.918521279025124482, -0.4964169966120777766 ) ) ;
#59688=CARTESIAN_POINT ( 'NONE',  ( -0.4019237886467001974, 8.551335450315372455, 1.500000000000001998 ) ) ;
#59732=CARTESIAN_POINT ( 'NONE',  ( -1.500000000000001110, 15.02083333333333570, 0.8660254037844419273 ) ) ;
#59776=CARTESIAN_POINT ( 'NONE',  ( 1.364683531250000303, 14.75520833367472839, -0.7879004041258355073 ) ) ;
#59814=ORIENTED_EDGE ( 'NONE', *, *, #107076, .T. ) ;
#59864=CARTESIAN_POINT ( 'NONE',  ( -1.115562610750309283E-14, 10.09375000068279782, 1.500000000000001554 ) ) ;
#59895=CARTESIAN_POINT ( 'NONE',  ( 1.500389033793473992, 3.249152749159987419, 0.07878897303667579954 ) ) ;
#59916=CARTESIAN_POINT ( 'NONE',  ( 1.364683531250000303, 13.31770833367472839, -0.7879004041258355073 ) ) ;
#59983=CARTESIAN_POINT ( 'NONE',  ( 1.364683531250000303, 11.81770833367472839, -0.7879004041258355073 ) ) ;
#60009=CARTESIAN_POINT ( 'NONE',  ( 1.836970198721030181E-16, 13.49999999999999822, 1.500000000000000222 ) ) ;
#60027=CARTESIAN_POINT ( 'NONE',  ( 1.500000000000001332, 11.65625000068279427, 0.000000000000000000 ) ) ;
#60127=CARTESIAN_POINT ( 'NONE',  ( 1.392249819062528537, 4.335314676365917386, 0.1369250707804057221 ) ) ;
#60146=CARTESIAN_POINT ( 'NONE',  ( -1.500236433942644609, 3.349270317293938870, -0.06629318219674300294 ) ) ;
#60165=CARTESIAN_POINT ( 'NONE',  ( -0.6823417656250039265, 10.06770833367473550, -1.181850606188755259 ) ) ;
#60235=CARTESIAN_POINT ( 'NONE',  ( 1.364683531250000303, 15.06770833367473017, -0.7879004041258355073 ) ) ;
#60246=CARTESIAN_POINT ( 'NONE',  ( 1.499999999999996891, 13.14583333333333393, -0.8660254037844378194 ) ) ;
#60315=EDGE_CURVE ( 'NONE', #127879, #183272, #2477, .T. ) ;
#60352=VERTEX_POINT ( 'NONE', #180764 ) ;
#60368=ORIENTED_EDGE ( 'NONE', *, *, #140315, .F. ) ;
#60426=CARTESIAN_POINT ( 'NONE',  ( 0.7500000000000006661, 12.33333333333333570, 1.299038105676657340 ) ) ;
#60431=CARTESIAN_POINT ( 'NONE',  ( 0.6823417656249934904, 10.69270833367473550, 1.181850606188764807 ) ) ;
#60441=CARTESIAN_POINT ( 'NONE',  ( -2.788906526875773208E-15, 10.71875000068279604, -1.499999999999998446 ) ) ;
#60470=CARTESIAN_POINT ( 'NONE',  ( -0.6823417656250003738, 12.21354166700806765, 1.181850606188754593 ) ) ;
#60494=DIRECTION ( 'NONE',  ( 0.000000000000000000, -1.000000000000000000, 0.000000000000000000 ) ) ;
#60540=CARTESIAN_POINT ( 'NONE',  ( -6.009258394948636914E-15, 13.96875000068279782, -1.732050807568875195 ) ) ;
#60575=CARTESIAN_POINT ( 'NONE',  ( -0.6823417656250003738, 9.651041667008065872, 1.181850606188754593 ) ) ;
#60619=VERTEX_POINT ( 'NONE', #21437 ) ;
#60671=LINE ( 'NONE', #77991, #168638 ) ;
#60712=CARTESIAN_POINT ( 'NONE',  ( -0.7500000000000006661, 11.70833333333333393, -1.299038105676657340 ) ) ;
#60724=CARTESIAN_POINT ( 'NONE',  ( -1.364683531250000748, 9.421875000341396245, 0.000000000000000000 ) ) ;
#60736=CARTESIAN_POINT ( 'NONE',  ( 1.286813488861806354, 4.047007041464545374, -0.4595522011843541366 ) ) ;
#60800=CARTESIAN_POINT ( 'NONE',  ( -6.009258394948636914E-15, 15.43750000000000178, -1.732050807568875195 ) ) ;
#60843=CARTESIAN_POINT ( 'NONE',  ( -1.364683531250010295, 13.13020833367472839, 0.7879004041258445001 ) ) ;
#60946=CARTESIAN_POINT ( 'NONE',  ( -1.493107181547909557, 3.264587186353522519, 0.1630395111544278020 ) ) ;
#60965=CARTESIAN_POINT ( 'NONE',  ( 1.392149563160024694, 3.364880846494863853, -0.1376214334732262790 ) ) ;
#60991=CARTESIAN_POINT ( 'NONE',  ( 1.364683531249997417, 13.79687500034139980, 2.602085213965210642E-15 ) ) ;
#61038=FACE_OUTER_BOUND ( 'NONE', #206890, .T. ) ;
#61054=CARTESIAN_POINT ( 'NONE',  ( 1.364683531250000303, 11.31770833367473550, -0.7879004041258355073 ) ) ;
#61097=CARTESIAN_POINT ( 'NONE',  ( -1.500000000000001110, 11.80208333401613352, 0.8660254037844419273 ) ) ;
#61151=CARTESIAN_POINT ( 'NONE',  ( 1.063950011417321484, -4.204658361605590144, 0.1571845235116707262 ) ) ;
#61168=EDGE_CURVE ( 'NONE', #104840, #133306, #180619, .T. ) ;
#61199=CARTESIAN_POINT ( 'NONE',  ( 1.435188857121525441, 4.071834925727953802, 0.4528096192972438927 ) ) ;
#61219=CARTESIAN_POINT ( 'NONE',  ( -1.491696246971095041, 3.267622381768281681, 0.1760465247046025805 ) ) ;
#61238=CARTESIAN_POINT ( 'NONE',  ( -1.364683531250000748, 9.109375000341396245, 0.000000000000000000 ) ) ;
#61249=( BOUNDED_CURVE ( )  B_SPLINE_CURVE ( 2, ( #112607, #128869, #78960, #208948, #146134, #94185, #80031, #176478, #113677 ),
 .UNSPECIFIED., .F., .T. ) 
 B_SPLINE_CURVE_WITH_KNOTS ( ( 3, 2, 2, 2, 3 ),
 ( 0.5803571428571429047, 0.5833333333333333703, 0.5892857142857143016, 0.5952380952380952328, 0.5982142857142856984 ),
 .UNSPECIFIED. ) 
 CURVE ( )  GEOMETRIC_REPRESENTATION_ITEM ( )  RATIONAL_B_SPLINE_CURVE ( ( 0.9330127018922194093, 0.9330127018922206306, 1.000000000000000000, 0.8660254037844387076, 1.000000000000000000, 0.8660254037844387076, 1.000000000000000000, 0.9330127018922194093, 0.9330127018922194093 ) ) 
 REPRESENTATION_ITEM ( '' )  );
#61496=CARTESIAN_POINT ( 'NONE',  ( 1.499999999999993117, 12.10416666666666430, 0.8660254037844409281 ) ) ;
#61502=CARTESIAN_POINT ( 'NONE',  ( -1.402160292154681736E-14, 8.671875000341403350, 1.575800808251682339 ) ) ;
#61540=CARTESIAN_POINT ( 'NONE',  ( -1.364683531250014514, 12.40104166700806054, -0.7879004041258335089 ) ) ;
#61612=CARTESIAN_POINT ( 'NONE',  ( -1.500000000000015099, 14.01041666734946212, -0.8660254037844309360 ) ) ;
#61649=CARTESIAN_POINT ( 'NONE',  ( 1.364683531250000303, 9.505208333674735499, -0.7879004041258355073 ) ) ;
#61668=DIRECTION ( 'NONE',  ( 1.000000000000000000, 0.000000000000000000, -1.665334536937734811E-16 ) ) ;
#61801=CARTESIAN_POINT ( 'NONE',  ( -8.012344526598182026E-15, 9.609375000341399797, -1.575800808251669460 ) ) ;
#61890=EDGE_CURVE ( 'NONE', #116561, #11879, #61249, .T. ) ;
#61917=CARTESIAN_POINT ( 'NONE',  ( -0.6823417656250003738, 13.65104166700806232, 1.181850606188754593 ) ) ;
#61930=AXIS2_PLACEMENT_3D ( 'NONE', #158597, #74145, #58957 ) ;
#61944=CARTESIAN_POINT ( 'NONE',  ( 0.5773502691896192918, -4.295408888568413630, 1.000000000000004441 ) ) ;
#62032=ADVANCED_FACE ( 'NONE', ( #11824 ), #163433, .T. ) ;
#62045=CARTESIAN_POINT ( 'NONE',  ( 1.436299488671524571, 3.619978527027484905, 0.4486666144298699366 ) ) ;
#62047=ORIENTED_EDGE ( 'NONE', *, *, #146436, .T. ) ;
#62067=CARTESIAN_POINT ( 'NONE',  ( -0.6823417656250003738, 13.21354166700806942, 1.181850606188754593 ) ) ;
#62075=ORIENTED_EDGE ( 'NONE', *, *, #191014, .F. ) ;
#62126=CARTESIAN_POINT ( 'NONE',  ( 1.364683531250000303, 11.56770833367472839, -0.7879004041258355073 ) ) ;
#62155=EDGE_CURVE ( 'NONE', #18633, #169050, #83369, .T. ) ;
#62171=CARTESIAN_POINT ( 'NONE',  ( -1.402160292154681736E-14, 10.34375000068279782, 1.732050807568881190 ) ) ;
#62268=CARTESIAN_POINT ( 'NONE',  ( 1.362971619486228025, 4.002954933304044616, 0.6272962186313684185 ) ) ;
#62276=EDGE_CURVE ( 'NONE', #11879, #114519, #15676, .T. ) ;
#62287=CARTESIAN_POINT ( 'NONE',  ( -1.317902950743175872, 3.538712461327640391, -0.3966175983076866696 ) ) ;
#62306=CARTESIAN_POINT ( 'NONE',  ( -1.402160292154681736E-14, 8.921875000341405126, 1.575800808251682339 ) ) ;
#62441=FILL_AREA_STYLE_COLOUR ( '', #124461 ) ;
#62556=CARTESIAN_POINT ( 'NONE',  ( -1.500000000000015099, 12.22916666666666607, -0.8660254037844309360 ) ) ;
#62561=CARTESIAN_POINT ( 'NONE',  ( -1.364683531250014514, 9.838541667008064096, -0.7879004041258335089 ) ) ;
#62597=CARTESIAN_POINT ( 'NONE',  ( 0.6823417656249934904, 11.25520833367473017, 1.181850606188764807 ) ) ;
#62665=CARTESIAN_POINT ( 'NONE',  ( -0.7500000000000006661, 13.73958333401613352, -1.299038105676657340 ) ) ;
#62679=( BOUNDED_CURVE ( )  B_SPLINE_CURVE ( 2, ( #51962, #21544, #171028, #19432, #201371, #53011, #203501, #56220, #153724, #118084, #202435, #5293, #4233, #72447, #167833, #71371, #70303, #119146, #155858, #85512, #151598, #137487, #39979, #86583, #55154, #152648, #136419, #121301, #6377, #106087, #187275, #38903, #104987, #22623, #88734, #208840, #111428, #125566, #8522, #160112, #57287, #124505, #95133, #205650, #75667, #173188, #156933, #61540, #76717, #161182, #141775, #93004, #9591, #191526, #174260, #108236, #60470, #190464, #193667, #159049, #41054, #123450, #107163, #59409, #175313, #139627, #143909, #207782, #176371, #42123, #43191, #189412, #25832, #94071, #24768, #91941, #29050, #73525, #158002, #110366, #177433, #11714, #109304, #58349, #126627, #45310, #26900, #10641, #142834, #192590, #140707, #206721, #77788, #90871, #74603, #27978, #127706, #44245, #209902, #31186, #48505, #212032, #62597, #63674, #79913, #762, #132972, #96201, #131912, #78843, #46371, #34362, #165433, #100435, #196867, #164375, #82043, #194733, #128759, #99380, #162250, #66829, #144963, #114625, #49549, #112490, #13837, #146020, #148137, #17029, #180615, #12768, #80989, #147078, #97259, #83106, #210969, #213099, #163313, #129828, #116744, #113562, #198974, #32240, #149187, #50619, #98311, #195810, #178500, #64729, #33296, #182744, #30110, #15960, #47446, #179565, #214138, #65766, #14895, #130872, #197921, #115674, #181669, #2906, #188083, #84185, #168635, #51704, #35427, #154535, #169704, #37573, #101505, #134045, #72185, #187016, #21294, #5038, #6115, #200055, #184871, #102575, #70041, #52751, #201111, #87399, #68978, #138293, #185938, #117827, #135097, #67901, #167575, #71114, #136157, #202174, #119963, #103653, #183817, #122118, #38649, #118885, #104727, #19174, #36497, #39712, #166506, #20238, #203252, #55966, #86323, #152395, #85248, #18097, #150273, #151337, #1842, #3974, #204309, #53832, #153465, #170775, #137231, #54895, #121049, #22364, #88476, #41875, #124257, #141530, #74353, #90620, #24509, #8270, #205395, #171847, #139364, #206469, #156677 ),
 .UNSPECIFIED., .F., .T. ) 
 B_SPLINE_CURVE_WITH_KNOTS ( ( 3, 2, 2, 2, 2, 2, 2, 2, 2, 2, 2, 2, 2, 2, 2, 2, 2, 2, 2, 2, 2, 2, 2, 2, 2, 2, 2, 2, 2, 2, 2, 2, 2, 2, 2, 2, 2, 2, 2, 2, 2, 2, 2, 2, 2, 2, 2, 2, 2, 2, 2, 2, 2, 2, 2, 2, 2, 2, 2, 2, 2, 2, 2, 2, 2, 2, 2, 2, 2, 2, 2, 2, 2, 2, 2, 2, 2, 2, 2, 2, 2, 2, 2, 2, 2, 2, 2, 2, 2, 2, 2, 2, 2, 2, 2, 2, 2, 2, 2, 2, 2, 2, 2, 2, 2, 2, 2, 2, 2, 2, 2, 2, 2, 2, 2, 2, 2, 2, 2, 3 ),
 ( 0.2923662209080201690, 0.2976190476190476164, 0.3035714285714285476, 0.3095238095238095344, 0.3154761904761904656, 0.3214285714285714524, 0.3273809523809523836, 0.3333333333333333148, 0.3392857142857143016, 0.3452380952380952328, 0.3511904761904761640, 0.3571428571428571508, 0.3630952380952380820, 0.3690476190476190688, 0.3750000000000000000, 0.3809523809523809312, 0.3869047619047619180, 0.3928571428571428492, 0.3988095238095238360, 0.4047619047619047672, 0.4107142857142856984, 0.4166666666666666852, 0.4226190476190476164, 0.4285714285714285476, 0.4345238095238095344, 0.4404761904761904656, 0.4464285714285714524, 0.4523809523809523836, 0.4583333333333333148, 0.4642857142857143016, 0.4702380952380952328, 0.4761904761904761640, 0.4821428571428571508, 0.4880952380952380820, 0.4940476190476190688, 0.5000000000000000000, 0.5059523809523809312, 0.5119047619047618625, 0.5178571428571429047, 0.5238095238095238360, 0.5297619047619047672, 0.5357142857142856984, 0.5416666666666666297, 0.5476190476190476719, 0.5535714285714286031, 0.5595238095238095344, 0.5654761904761904656, 0.5714285714285713969, 0.5773809523809523281, 0.5833333333333333703, 0.5892857142857143016, 0.5952380952380952328, 0.6011904761904761640, 0.6071428571428570953, 0.6130952380952381375, 0.6190476190476190688, 0.6250000000000000000, 0.6309523809523809312, 0.6369047619047618625, 0.6428571428571429047, 0.6488095238095238360, 0.6547619047619047672, 0.6607142857142856984, 0.6666666666666666297, 0.6726190476190476719, 0.6785714285714286031, 0.6845238095238095344, 0.6904761904761904656, 0.6964285714285713969, 0.7023809523809523281, 0.7083333333333333703, 0.7142857142857143016, 0.7202380952380953438, 0.7261904761904761640, 0.7321428571428570953, 0.7380952380952381375, 0.7440476190476190688, 0.7500000000000000000, 0.7559523809523809312, 0.7619047619047618625, 0.7678571428571430157, 0.7738095238095238360, 0.7797619047619047672, 0.7857142857142856984, 0.7916666666666666297, 0.7976190476190476719, 0.8035714285714286031, 0.8095238095238095344, 0.8154761904761904656, 0.8214285714285713969, 0.8273809523809523281, 0.8333333333333334814, 0.8392857142857144126, 0.8452380952380953438, 0.8511904761904762751, 0.8571428571428572063, 0.8630952380952381375, 0.8690476190476190688, 0.8750000000000000000, 0.8809523809523809312, 0.8869047619047618625, 0.8928571428571430157, 0.8988095238095239470, 0.9047619047619048782, 0.9107142857142858094, 0.9166666666666667407, 0.9226190476190476719, 0.9285714285714286031, 0.9345238095238095344, 0.9404761904761904656, 0.9464285714285713969, 0.9523809523809523281, 0.9583333333333334814, 0.9642857142857144126, 0.9702380952380953438, 0.9761904761904762751, 0.9821428571428572063, 0.9880952380952381375, 0.9940476190476190688, 1.000000000000000000 ),
 .UNSPECIFIED. ) 
 CURVE ( )  GEOMETRIC_REPRESENTATION_ITEM ( )  RATIONAL_B_SPLINE_CURVE ( ( 0.9722101959979289054, 0.8817707832831631620, 1.000000000000000000, 0.8660254037844387076, 1.000000000000000000, 0.8660254037844387076, 1.000000000000000000, 0.8660254037844387076, 1.000000000000000000, 0.8660254037844387076, 1.000000000000000000, 0.8660254037844387076, 1.000000000000000000, 0.8660254037844387076, 1.000000000000000000, 0.8660254037844387076, 1.000000000000000000, 0.8660254037844387076, 1.000000000000000000, 0.8660254037844387076, 1.000000000000000000, 0.8660254037844387076, 1.000000000000000000, 0.8660254037844387076, 1.000000000000000000, 0.8660254037844387076, 1.000000000000000000, 0.8660254037844387076, 1.000000000000000000, 0.8660254037844387076, 1.000000000000000000, 0.8660254037844387076, 1.000000000000000000, 0.8660254037844387076, 1.000000000000000000, 0.8660254037844387076, 1.000000000000000000, 0.8660254037844387076, 1.000000000000000000, 0.8660254037844387076, 1.000000000000000000, 0.8660254037844387076, 1.000000000000000000, 0.8660254037844387076, 1.000000000000000000, 0.8660254037844387076, 1.000000000000000000, 0.8660254037844387076, 1.000000000000000000, 0.8660254037844387076, 1.000000000000000000, 0.8660254037844387076, 1.000000000000000000, 0.8660254037844387076, 1.000000000000000000, 0.8660254037844387076, 1.000000000000000000, 0.8660254037844387076, 1.000000000000000000, 0.8660254037844387076, 1.000000000000000000, 0.8660254037844387076, 1.000000000000000000, 0.8660254037844387076, 1.000000000000000000, 0.8660254037844387076, 1.000000000000000000, 0.8660254037844387076, 1.000000000000000000, 0.8660254037844387076, 1.000000000000000000, 0.8660254037844387076, 1.000000000000000000, 0.8660254037844387076, 1.000000000000000000, 0.8660254037844387076, 1.000000000000000000, 0.8660254037844387076, 1.000000000000000000, 0.8660254037844387076, 1.000000000000000000, 0.8660254037844387076, 1.000000000000000000, 0.8660254037844387076, 1.000000000000000000, 0.8660254037844387076, 1.000000000000000000, 0.8660254037844387076, 1.000000000000000000, 0.8660254037844387076, 1.000000000000000000, 0.8660254037844387076, 1.000000000000000000, 0.8660254037844387076, 1.000000000000000000, 0.8660254037844387076, 1.000000000000000000, 0.8660254037844387076, 1.000000000000000000, 0.8660254037844387076, 1.000000000000000000, 0.8660254037844387076, 1.000000000000000000, 0.8660254037844387076, 1.000000000000000000, 0.8660254037844387076, 1.000000000000000000, 0.8660254037844387076, 1.000000000000000000, 0.8660254037844387076, 1.000000000000000000, 0.8660254037844387076, 1.000000000000000000, 0.8660254037844387076, 1.000000000000000000, 0.8660254037844387076, 1.000000000000000000, 0.8660254037844387076, 1.000000000000000000, 0.8660254037844387076, 1.000000000000000000, 0.8660254037844387076, 1.000000000000000000, 0.8660254037844387076, 1.000000000000000000, 0.8660254037844387076, 1.000000000000000000, 0.8660254037844387076, 1.000000000000000000, 0.8660254037844387076, 1.000000000000000000, 0.8660254037844387076, 1.000000000000000000, 0.8660254037844387076, 1.000000000000000000, 0.8660254037844387076, 1.000000000000000000, 0.8660254037844387076, 1.000000000000000000, 0.8660254037844387076, 1.000000000000000000, 0.8660254037844387076, 1.000000000000000000, 0.8660254037844387076, 1.000000000000000000, 0.8660254037844387076, 1.000000000000000000, 0.8660254037844387076, 1.000000000000000000, 0.8660254037844387076, 1.000000000000000000, 0.8660254037844387076, 1.000000000000000000, 0.8660254037844387076, 1.000000000000000000, 0.8660254037844387076, 1.000000000000000000, 0.8660254037844387076, 1.000000000000000000, 0.8660254037844387076, 1.000000000000000000, 0.8660254037844387076, 1.000000000000000000, 0.8660254037844387076, 1.000000000000000000, 0.8660254037844387076, 1.000000000000000000, 0.8660254037844387076, 1.000000000000000000, 0.8660254037844387076, 1.000000000000000000, 0.8660254037844387076, 1.000000000000000000, 0.8660254037844387076, 1.000000000000000000, 0.8660254037844387076, 1.000000000000000000, 0.8660254037844387076, 1.000000000000000000, 0.8660254037844387076, 1.000000000000000000, 0.8660254037844387076, 1.000000000000000000, 0.8660254037844387076, 1.000000000000000000, 0.8660254037844387076, 1.000000000000000000, 0.8660254037844387076, 1.000000000000000000, 0.8660254037844387076, 1.000000000000000000, 0.8660254037844387076, 1.000000000000000000, 0.8660254037844387076, 1.000000000000000000, 0.8660254037844387076, 1.000000000000000000, 0.8660254037844387076, 1.000000000000000000, 0.8660254037844387076, 1.000000000000000000, 0.8660254037844387076, 1.000000000000000000, 0.8660254037844387076, 1.000000000000000000, 0.8660254037844387076, 1.000000000000000000, 0.8660254037844387076, 1.000000000000000000, 0.8660254037844387076, 1.000000000000000000, 0.8660254037844387076, 1.000000000000000000, 0.8660254037844387076, 1.000000000000000000, 0.8660254037844387076, 1.000000000000000000, 0.8660254037844387076, 1.000000000000000000, 0.8660254037844387076, 1.000000000000000000, 0.8660254037844387076, 1.000000000000000000, 0.8660254037844387076, 1.000000000000000000, 0.8660254037844387076, 1.000000000000000000, 0.8660254037844387076, 1.000000000000000000, 0.8660254037844387076, 1.000000000000000000, 0.8660254037844387076, 1.000000000000000000, 0.8660254037844387076, 1.000000000000000000, 0.8660254037844387076, 1.000000000000000000, 0.8660254037844387076, 1.000000000000000000 ) ) 
 REPRESENTATION_ITEM ( '' )  );
#62699=CARTESIAN_POINT ( 'NONE',  ( -1.364683531250000748, 8.609375000341396245, 0.000000000000000000 ) ) ;
#62875=CARTESIAN_POINT ( 'NONE',  ( 0.4340096093344653627, 3.713252088577059684, -0.4851708347456812898 ) ) ;
#62876=CARTESIAN_POINT ( 'NONE',  ( 1.499999999999993117, 9.135416667349462116, 0.8660254037844408170 ) ) ;
#62882=CARTESIAN_POINT ( 'NONE',  ( 1.492698588115513703, 4.434522803406307112, -0.1666886929329614297 ) ) ;
#62893=CARTESIAN_POINT ( 'NONE',  ( -2.788906526875773208E-15, 9.968750000682797818, -1.499999999999998446 ) ) ;
#62949=CARTESIAN_POINT ( 'NONE',  ( 0.4019237886466778820, 11.07366454968463110, 1.500000000000001554 ) ) ;
#62969=CARTESIAN_POINT ( 'NONE',  ( 0.6823417656249934904, 12.94270833367473017, 1.181850606188764807 ) ) ;
#62982=CARTESIAN_POINT ( 'NONE',  ( -1.300105796840246519, 4.107110749520949788, 0.4336863642760122040 ) ) ;
#63070=CARTESIAN_POINT ( 'NONE',  ( -1.500000000000008216, 12.24999999999999645, 3.469446951953614189E-15 ) ) ;
#63099=CARTESIAN_POINT ( 'NONE',  ( 1.430949710260811969, 3.674736480791923388, 0.4689103363401325164 ) ) ;
#63110=B_SPLINE_CURVE_WITH_KNOTS ( 'NONE', 3,
 ( #94741, #80601, #112109, #147745, #129444, #29728, #127308, #179176, #30800, #180239, #63281, #130500, #195426, #12380, #96879, #109972, #78460, #175983 ),
 .UNSPECIFIED., .F., .F.,
 ( 4, 2, 2, 2, 2, 2, 2, 2, 4 ),
 ( 0.001640627021451598498, 0.001845642838648688241, 0.002050658655845778201, 0.002255674473042867945, 0.002460690290239957688, 0.002665706107437047431, 0.002870721924634137175, 0.003075737741831227352, 0.003280753559028317095 ),
 .UNSPECIFIED. ) ;
#63125=CARTESIAN_POINT ( 'NONE',  ( -1.364683531250000748, 12.17187500034139980, 0.000000000000000000 ) ) ;
#63174=VECTOR ( 'NONE', #166798, 1000.000000000000114 ) ;
#63185=CARTESIAN_POINT ( 'NONE',  ( 1.364683531250000303, 9.817708333674735499, -0.7879004041258355073 ) ) ;
#63214=CARTESIAN_POINT ( 'NONE',  ( 0.4153311931458959494, 3.850000000000006306, 0.5000000000000064393 ) ) ;
#63228=CARTESIAN_POINT ( 'NONE',  ( 1.499999999999997113, 9.677083334016129967, -0.8660254037844378194 ) ) ;
#63281=CARTESIAN_POINT ( 'NONE',  ( -0.6386894617478927616, 4.335523901721595408, -0.1366332986426508633 ) ) ;
#63334=FACE_OUTER_BOUND ( 'NONE', #86548, .T. ) ;
#63353=CARTESIAN_POINT ( 'NONE',  ( -1.476571758179682670, 3.427372387846666424, 0.2774774824061063128 ) ) ;
#63373=CARTESIAN_POINT ( 'NONE',  ( 1.364683531249996529, 8.963541667008069425, 0.7879004041258403923 ) ) ;
#63445=CARTESIAN_POINT ( 'NONE',  ( -8.012344526598182026E-15, 14.10937500034139802, -1.575800808251669460 ) ) ;
#63478=DIRECTION ( 'NONE',  ( 0.000000000000000000, -1.000000000000000000, 0.000000000000000000 ) ) ;
#63576=ORIENTED_EDGE ( 'NONE', *, *, #154299, .F. ) ;
#63602=CARTESIAN_POINT ( 'NONE',  ( -0.7500000000000179856, 13.04166666666666607, 1.299038105676658228 ) ) ;
#63633=CARTESIAN_POINT ( 'NONE',  ( 1.500000000000001332, 10.37499999999999467, 0.000000000000000000 ) ) ;
#63638=CARTESIAN_POINT ( 'NONE',  ( 0.6823417656249969321, 9.026041667008065872, -1.181850606188757036 ) ) ;
#63674=CARTESIAN_POINT ( 'NONE',  ( -1.402160292154681736E-14, 11.23437500034139624, 1.575800808251682339 ) ) ;
#63733=EDGE_CURVE ( 'NONE', #179825, #183713, #102994, .T. ) ;
#63740=CARTESIAN_POINT ( 'NONE',  ( 1.499999999999997113, 13.92708333401613352, -0.8660254037844378194 ) ) ;
#63774=CARTESIAN_POINT ( 'NONE',  ( -0.6823417656250039265, 8.567708333674733723, -1.181850606188755259 ) ) ;
#63778=ORIENTED_EDGE ( 'NONE', *, *, #173881, .T. ) ;
#63790=DIRECTION ( 'NONE',  ( -0.1669130127894878912, 0.9056625952363902554, -0.3897631457067520788 ) ) ;
#63925=CARTESIAN_POINT ( 'NONE',  ( 0.6823417656249934904, 9.005208333674726617, 1.181850606188764807 ) ) ;
#64006=CARTESIAN_POINT ( 'NONE',  ( -1.500000000000008216, 9.781250000682799595, 3.469446951953614189E-15 ) ) ;
#64027=CARTESIAN_POINT ( 'NONE',  ( 1.220146605508150803E-14, 9.687500000000000000, -1.499999999999998446 ) ) ;
#64044=CARTESIAN_POINT ( 'NONE',  ( -8.012344526598182026E-15, 13.54687500034139269, -1.575800808251669460 ) ) ;
#64199=CARTESIAN_POINT ( 'NONE',  ( -1.364683531250000748, 12.42187500034139980, 0.000000000000000000 ) ) ;
#64210=ORIENTED_EDGE ( 'NONE', *, *, #175320, .F. ) ;
#64212=CARTESIAN_POINT ( 'NONE',  ( 3.834746474454188013E-15, 12.34375000068279959, 1.500000000000001554 ) ) ;
#64260=CARTESIAN_POINT ( 'NONE',  ( -1.364683531250014514, 10.90104166700806942, -0.7879004041258335089 ) ) ;
#64301=CARTESIAN_POINT ( 'NONE',  ( -1.500000000000008216, 9.531250000682799595, 3.469446951953614189E-15 ) ) ;
#64368=PLANE ( 'NONE',  #86113 ) ;
#64402=CARTESIAN_POINT ( 'NONE',  ( 1.445243771768980556, 4.136534814424732254, -0.4166150551214564679 ) ) ;
#64439=CARTESIAN_POINT ( 'NONE',  ( 1.364683531250000748, 10.00520833367473017, -0.7879004041258355073 ) ) ;
#64508=CARTESIAN_POINT ( 'NONE',  ( -1.364683531250000748, 14.92187500034139447, 0.000000000000000000 ) ) ;
#64689=CARTESIAN_POINT ( 'NONE',  ( -0.7500000000000179856, 10.54166666666667140, 1.299038105676658228 ) ) ;
#64694=CARTESIAN_POINT ( 'NONE',  ( 1.364683531249997417, 9.234375000341396245, 2.602085213965210642E-15 ) ) ;
#64703=CARTESIAN_POINT ( 'NONE',  ( -0.5773502691896261751, -4.295408888568413630, -0.9999999999999991118 ) ) ;
#64729=CARTESIAN_POINT ( 'NONE',  ( 1.364683531249996529, 10.27604166700806410, 0.7879004041258403923 ) ) ;
#64755=VECTOR ( 'NONE', #178583, 1000.000000000000114 ) ;
#64802=CARTESIAN_POINT ( 'NONE',  ( -1.500000000000008216, 13.03125000068279604, 3.469446951953614189E-15 ) ) ;
#64836=CARTESIAN_POINT ( 'NONE',  ( -1.364683531250000748, 9.609375000341396245, 0.000000000000000000 ) ) ;
#64994=CARTESIAN_POINT ( 'NONE',  ( -2.788906526875773208E-15, 9.187500000000001776, -1.499999999999998446 ) ) ;
#65060=ORIENTED_EDGE ( 'NONE', *, *, #114249, .T. ) ;
#65084=CARTESIAN_POINT ( 'NONE',  ( 1.364683531249996529, 12.46354166700806054, 0.7879004041258405033 ) ) ;
#65095=CARTESIAN_POINT ( 'NONE',  ( -1.392969482149210014, 4.158527933356495510, 0.5575990067801558370 ) ) ;
#65099=ADVANCED_FACE ( 'NONE', ( #153798, #50965 ), #167913, .T. ) ;
#65230=CARTESIAN_POINT ( 'NONE',  ( 1.364683531250000303, 12.81770833367473372, -0.7879004041258355073 ) ) ;
#65231=VECTOR ( 'NONE', #68391, 1000.000000000000000 ) ;
#65269=VERTEX_POINT ( 'NONE', #93083 ) ;
#65276=FACE_OUTER_BOUND ( 'NONE', #107686, .T. ) ;
#65291=CARTESIAN_POINT ( 'NONE',  ( 1.364683531250000303, 10.81770833367473195, -0.7879004041258355073 ) ) ;
#65333=CARTESIAN_POINT ( 'NONE',  ( 1.499999999999997113, 9.927083334016131744, -0.8660254037844378194 ) ) ;
#65410=CARTESIAN_POINT ( 'NONE',  ( 4.764381983412778688E-15, 12.71875000068279782, -1.499999999999998446 ) ) ;
#65470=CARTESIAN_POINT ( 'NONE',  ( 0.6823417656249934904, 9.942708333674735499, 1.181850606188764807 ) ) ;
#65516=CARTESIAN_POINT ( 'NONE',  ( -1.115562610750309283E-14, 9.343750000682799595, 1.500000000000001554 ) ) ;
#65542=CARTESIAN_POINT ( 'NONE',  ( -8.012344526598182026E-15, 14.60937500034139980, -1.575800808251669460 ) ) ;
#65558=ORIENTED_EDGE ( 'NONE', *, *, #139460, .T. ) ;
#65597=CARTESIAN_POINT ( 'NONE',  ( 0.4019237886466816012, 8.707585450998170273, -1.499999999999998668 ) ) ;
#65723=CARTESIAN_POINT ( 'NONE',  ( 0.7500000000000006661, 10.66666666666666430, -1.299038105676657340 ) ) ;
#65729=CARTESIAN_POINT ( 'NONE',  ( -1.402160292154681736E-14, 8.921875000341405126, 1.575800808251682339 ) ) ;
#65738=CARTESIAN_POINT ( 'NONE',  ( -0.4842345852037238663, 3.595399794601802146, 0.4350569428522566007 ) ) ;
#65766=CARTESIAN_POINT ( 'NONE',  ( -8.012344526598182026E-15, 10.10937500034140335, -1.575800808251669460 ) ) ;
#65790=CYLINDRICAL_SURFACE ( 'NONE', #179843, 1.500000000000000222 ) ;
#65828=B_SPLINE_CURVE_WITH_KNOTS ( 'NONE', 3,
 ( #97242, #115657, #147061, #213081, #164358, #15942 ),
 .UNSPECIFIED., .F., .F.,
 ( 4, 2, 4 ),
 ( 0.000000000000000000, 0.0001030949158708163878, 0.0002061898317416328299 ),
 .UNSPECIFIED. ) ;
#65840=CARTESIAN_POINT ( 'NONE',  ( -1.402160292154681736E-14, 12.84375000068279959, 1.732050807568881190 ) ) ;
#65879=ORIENTED_EDGE ( 'NONE', *, *, #120622, .T. ) ;
#65881=CARTESIAN_POINT ( 'NONE',  ( 1.220146605508150803E-14, 11.21875000068279249, -1.499999999999998446 ) ) ;
#65897=CYLINDRICAL_SURFACE ( 'NONE', #8340, 1.500000000000000222 ) ;
#65916=CARTESIAN_POINT ( 'NONE',  ( 1.364067407192349757, 4.011924485828274101, -0.6250643920678818910 ) ) ;
#65922=EDGE_LOOP ( 'NONE', ( #6460, #112769, #199085, #70004, #90614 ) ) ;
#65993=CARTESIAN_POINT ( 'NONE',  ( 0.000000000000000000, -4.500000000000003553, 0.000000000000000000 ) ) ;
#66019=CARTESIAN_POINT ( 'NONE',  ( 1.364683531249997417, 8.546875000341403350, 2.602085213965210642E-15 ) ) ;
#66026=CARTESIAN_POINT ( 'NONE',  ( -1.500000000000015099, 12.01041666734946212, -0.8660254037844309360 ) ) ;
#66068=VERTEX_POINT ( 'NONE', #168446 ) ;
#66130=CARTESIAN_POINT ( 'NONE',  ( 1.364683531250000303, 11.50520833367472839, -0.7879004041258355073 ) ) ;
#66189=VECTOR ( 'NONE', #18916, 1000.000000000000000 ) ;
#66221=EDGE_CURVE ( 'NONE', #161998, #127879, #190438, .T. ) ;
#66247=LINE ( 'NONE', #84664, #65231 ) ;
#66269=EDGE_LOOP ( 'NONE', ( #11860, #102884, #135565, #7699 ) ) ;
#66283=CARTESIAN_POINT ( 'NONE',  ( -1.402160292154681736E-14, 12.23437500034140335, 1.575800808251682339 ) ) ;
#66296=( BOUNDED_CURVE ( )  B_SPLINE_CURVE ( 2, ( #134795, #116440, #37265, #20983, #167276 ),
 .UNSPECIFIED., .F., .T. ) 
 B_SPLINE_CURVE_WITH_KNOTS ( ( 3, 2, 3 ),
 ( 0.3228721300350675949, 0.3273809523809523836, 0.3303571428571428492 ),
 .UNSPECIFIED. ) 
 CURVE ( )  GEOMETRIC_REPRESENTATION_ITEM ( )  RATIONAL_B_SPLINE_CURVE ( ( 0.9507769454952199606, 0.8985166342628003733, 1.000000000000000000, 0.9330127018922194093, 0.9330127018922194093 ) ) 
 REPRESENTATION_ITEM ( '' )  );
#66350=CARTESIAN_POINT ( 'NONE',  ( 1.364683531249997417, 10.29687500034139802, 2.602085213965210642E-15 ) ) ;
#66390=CARTESIAN_POINT ( 'NONE',  ( -1.500000000000008216, 9.281250000682799595, 3.469446951953614189E-15 ) ) ;
#66474=( BOUNDED_CURVE ( )  B_SPLINE_CURVE ( 2, ( #112844, #210258, #46732, #32587, #178860, #98664, #176710, #212385, #64027 ),
 .UNSPECIFIED., .F., .T. ) 
 B_SPLINE_CURVE_WITH_KNOTS ( ( 3, 2, 2, 2, 3 ),
 ( 0.8125000000000000000, 0.8154761904761904656, 0.8214285714285713969, 0.8273809523809523281, 0.8303571428571429047 ),
 .UNSPECIFIED. ) 
 CURVE ( )  GEOMETRIC_REPRESENTATION_ITEM ( )  RATIONAL_B_SPLINE_CURVE ( ( 0.9330127018922194093, 0.9330127018922194093, 1.000000000000000000, 0.8660254037844387076, 1.000000000000000000, 0.8660254037844387076, 1.000000000000000000, 0.9330127018922180770, 0.9330127018922194093 ) ) 
 REPRESENTATION_ITEM ( '' )  );
#66594=CARTESIAN_POINT ( 'NONE',  ( -0.6823417656250003738, 13.96354166700806942, 1.181850606188754593 ) ) ;
#66728=ORIENTED_EDGE ( 'NONE', *, *, #146061, .F. ) ;
#66783=CARTESIAN_POINT ( 'NONE',  ( 1.500000000000001332, 10.87499999999999645, 0.000000000000000000 ) ) ;
#66789=CARTESIAN_POINT ( 'NONE',  ( -0.6823417656250003738, 8.401041667008064096, 1.181850606188754593 ) ) ;
#66829=CARTESIAN_POINT ( 'NONE',  ( -8.012344526598182026E-15, 10.85937500034139624, -1.575800808251669460 ) ) ;
#66866=CARTESIAN_POINT ( 'NONE',  ( -0.4019237886466802689, 9.948664549684631098, -1.500000000000002887 ) ) ;
#66884=( BOUNDED_CURVE ( )  B_SPLINE_CURVE ( 2, ( #52925, #205565, #23617, #204484, #22539, #36665, #189329, #187188, #40970 ),
 .UNSPECIFIED., .F., .T. ) 
 B_SPLINE_CURVE_WITH_KNOTS ( ( 3, 2, 2, 2, 3 ),
 ( 0.4375000000000000000, 0.4404761904761904656, 0.4464285714285714524, 0.4523809523809523836, 0.4553571428571427937 ),
 .UNSPECIFIED. ) 
 CURVE ( )  GEOMETRIC_REPRESENTATION_ITEM ( )  RATIONAL_B_SPLINE_CURVE ( ( 0.9330127018922194093, 0.9330127018922194093, 1.000000000000000000, 0.8660254037844387076, 1.000000000000000000, 0.8660254037844387076, 1.000000000000000000, 0.9330127018922206306, 0.9330127018922194093 ) ) 
 REPRESENTATION_ITEM ( '' )  );
#66894=EDGE_CURVE ( 'NONE', #95692, #60619, #11826, .T. ) ;
#66905=CARTESIAN_POINT ( 'NONE',  ( 1.499999999999993117, 12.38541666734946212, 0.8660254037844409281 ) ) ;
#66919=EDGE_CURVE ( 'NONE', #114519, #8253, #29622, .T. ) ;
#67000=CARTESIAN_POINT ( 'NONE',  ( -0.6823417656250003738, 13.65104166700806232, 1.181850606188754593 ) ) ;
#67053=CARTESIAN_POINT ( 'NONE',  ( -0.6823417656250003738, 12.40104166700806232, 1.181850606188754593 ) ) ;
#67094=VERTEX_POINT ( 'NONE', #1960 ) ;
#67112=EDGE_CURVE ( 'NONE', #47534, #116561, #154233, .T. ) ;
#67135=CYLINDRICAL_SURFACE ( 'NONE', #183069, 1.500000000000000222 ) ;
#67137=CARTESIAN_POINT ( 'NONE',  ( 1.499999999999993117, 10.63541666734946212, 0.8660254037844408170 ) ) ;
#67138=ORIENTED_EDGE ( 'NONE', *, *, #104977, .T. ) ;
#67202=CARTESIAN_POINT ( 'NONE',  ( 1.364683531250000303, 12.25520833367473195, -0.7879004041258355073 ) ) ;
#67247=ORIENTED_EDGE ( 'NONE', *, *, #103483, .T. ) ;
#67258=ORIENTED_EDGE ( 'NONE', *, *, #129790, .F. ) ;
#67283=DIRECTION ( 'NONE',  ( 0.000000000000000000, -1.000000000000000000, 0.000000000000000000 ) ) ;
#67347=CARTESIAN_POINT ( 'NONE',  ( -0.6823417656250003738, 12.46354166700806765, 1.181850606188754593 ) ) ;
#67371=EDGE_CURVE ( 'NONE', #98728, #115710, #169328, .T. ) ;
#67401=ORIENTED_EDGE ( 'NONE', *, *, #162793, .T. ) ;
#67414=CARTESIAN_POINT ( 'NONE',  ( -1.364683531250000748, 10.92187500034139802, 0.000000000000000000 ) ) ;
#67455=CARTESIAN_POINT ( 'NONE',  ( 1.499999999999997113, 9.177083334016128191, -0.8660254037844378194 ) ) ;
#67506=( BOUNDED_CURVE ( )  B_SPLINE_CURVE ( 2, ( #197850, #211963, #63602, #49482, #115602, #129756, #177360, #195741, #47378 ),
 .UNSPECIFIED., .F., .T. ) 
 B_SPLINE_CURVE_WITH_KNOTS ( ( 3, 2, 2, 2, 3 ),
 ( 0.3482142857142856429, 0.3511904761904761640, 0.3571428571428571508, 0.3630952380952380820, 0.3660714285714286031 ),
 .UNSPECIFIED. ) 
 CURVE ( )  GEOMETRIC_REPRESENTATION_ITEM ( )  RATIONAL_B_SPLINE_CURVE ( ( 0.9330127018922194093, 0.9330127018922180770, 1.000000000000000000, 0.8660254037844387076, 1.000000000000000000, 0.8660254037844387076, 1.000000000000000000, 0.9330127018922187432, 0.9330127018922194093 ) ) 
 REPRESENTATION_ITEM ( '' )  );
#67594=CARTESIAN_POINT ( 'NONE',  ( 0.6823417656249934904, 8.442708333674733723, 1.181850606188764807 ) ) ;
#67647=DIRECTION ( 'NONE',  ( 0.000000000000000000, 1.000000000000000000, 0.000000000000000000 ) ) ;
#67660=CARTESIAN_POINT ( 'NONE',  ( -0.6823417656250003738, 14.46354166700806410, 1.181850606188754593 ) ) ;
#67821=CARTESIAN_POINT ( 'NONE',  ( 1.836970198721030181E-16, 0.000000000000000000, 1.500000000000000222 ) ) ;
#67827=CARTESIAN_POINT ( 'NONE',  ( 0.7500000000000006661, 11.94791666734946389, -1.299038105676657340 ) ) ;
#67848=CARTESIAN_POINT ( 'NONE',  ( -0.6823417656250039265, 11.81770833367473017, -1.181850606188755259 ) ) ;
#67853=CARTESIAN_POINT ( 'NONE',  ( 0.7500000000000006661, 10.41666666666667140, -1.299038105676657340 ) ) ;
#67884=VECTOR ( 'NONE', #80709, 1000.000000000000114 ) ;
#67901=CARTESIAN_POINT ( 'NONE',  ( -1.364683531250014514, 9.401041667008062319, -0.7879004041258335089 ) ) ;
#67959=CARTESIAN_POINT ( 'NONE',  ( 0.7500000000000006661, 12.41666666666666607, -1.299038105676657340 ) ) ;
#67972=CARTESIAN_POINT ( 'NONE',  ( -0.7500000000000179856, 12.32291666734946389, 1.299038105676658228 ) ) ;
#67983=CARTESIAN_POINT ( 'NONE',  ( -2.788906526875773208E-15, 12.68749999999999822, -1.499999999999998446 ) ) ;
#68065=CARTESIAN_POINT ( 'NONE',  ( -1.364683531250000748, 13.10937500034139980, 0.000000000000000000 ) ) ;
#68075=EDGE_CURVE ( 'NONE', #122713, #46203, #86864, .T. ) ;
#68120=CARTESIAN_POINT ( 'NONE',  ( -8.012344526598182026E-15, 12.29687500034140513, -1.575800808251669460 ) ) ;
#68206=CARTESIAN_POINT ( 'NONE',  ( 3.834746474454188013E-15, 10.59375000068279604, 1.500000000000001554 ) ) ;
#68256=LINE ( 'NONE', #53094, #46063 ) ;
#68274=CARTESIAN_POINT ( 'NONE',  ( 1.364683531250000303, 11.00520833367473550, -0.7879004041258355073 ) ) ;
#68306=CARTESIAN_POINT ( 'NONE',  ( 0.7080714767514932895, 13.29905055995279106, 1.258874868610346809 ) ) ;
#68356=DIRECTION ( 'NONE',  ( 0.000000000000000000, 0.000000000000000000, -1.000000000000000000 ) ) ;
#68372=CARTESIAN_POINT ( 'NONE',  ( 0.000000000000000000, 13.49999999999999822, -0.6500000000000000222 ) ) ;
#68391=DIRECTION ( 'NONE',  ( 0.000000000000000000, -1.000000000000000000, 0.000000000000000000 ) ) ;
#68413=EDGE_CURVE ( 'NONE', #72363, #166249, #169409, .T. ) ;
#68426=CARTESIAN_POINT ( 'NONE',  ( -0.6823417656250003738, 10.71354166700806765, 1.181850606188754593 ) ) ;
#68493=CARTESIAN_POINT ( 'NONE',  ( 1.364683531249996529, 8.776041667008067648, 0.7879004041258405033 ) ) ;
#68505=CARTESIAN_POINT ( 'NONE',  ( 0.7500000000000006661, 9.697916667349467446, -1.299038105676657340 ) ) ;
#68532=CARTESIAN_POINT ( 'NONE',  ( -1.402160292154681736E-14, 8.593750000682796042, 1.732050807568881190 ) ) ;
#68596=EDGE_CURVE ( 'NONE', #94456, #32497, #163741, .T. ) ;
#68640=AXIS2_PLACEMENT_3D ( 'NONE', #10846, #23901, #139831 ) ;
#68722=ORIENTED_EDGE ( 'NONE', *, *, #40853, .F. ) ;
#68740=CARTESIAN_POINT ( 'NONE',  ( -0.6823417656250039265, 13.13020833367473017, -1.181850606188755259 ) ) ;
#68923=CARTESIAN_POINT ( 'NONE',  ( 0.6823417656249969321, 11.52604166700806765, -1.181850606188757036 ) ) ;
#68929=CARTESIAN_POINT ( 'NONE',  ( -6.009258394948636914E-15, 9.187500000000003553, -1.732050807568875195 ) ) ;
#68961=ORIENTED_EDGE ( 'NONE', *, *, #157657, .T. ) ;
#68968=ORIENTED_EDGE ( 'NONE', *, *, #61168, .F. ) ;
#68978=CARTESIAN_POINT ( 'NONE',  ( 0.6823417656249934904, 9.505208333674728394, 1.181850606188764807 ) ) ;
#69051=CARTESIAN_POINT ( 'NONE',  ( 1.499999999999997113, 12.17708333401613352, -0.8660254037844378194 ) ) ;
#69123=CARTESIAN_POINT ( 'NONE',  ( 1.456019627564700825, 3.350498733230925286, -0.3924612876561414665 ) ) ;
#69138=CARTESIAN_POINT ( 'NONE',  ( -1.364683531250010295, 13.88020833367473195, 0.7879004041258445001 ) ) ;
#69140=STYLED_ITEM ( 'NONE', ( #127541 ), #176823 ) ;
#69182=CARTESIAN_POINT ( 'NONE',  ( 0.7500000000000006661, 14.08333333333333570, 1.299038105676657340 ) ) ;
#69189=CARTESIAN_POINT ( 'NONE',  ( -1.364683531250014514, 11.83854166700806587, -0.7879004041258335089 ) ) ;
#69259=CARTESIAN_POINT ( 'NONE',  ( -1.115562610750309283E-14, 9.812500000000000000, 1.500000000000001554 ) ) ;
#69336=CARTESIAN_POINT ( 'NONE',  ( 1.364683531249997417, 11.98437500034139980, 2.602085213965210642E-15 ) ) ;
#69405=CARTESIAN_POINT ( 'NONE',  ( -0.8145602173408781344, -4.140925090156072130, -0.5891403177412749548 ) ) ;
#69489=CARTESIAN_POINT ( 'NONE',  ( -8.012344526598182026E-15, 10.85937500034139624, -1.575800808251669460 ) ) ;
#69498=CARTESIAN_POINT ( 'NONE',  ( 1.530808498934191324E-16, -0.5000000000000004441, -1.249999999999999778 ) ) ;
#69500=LINE ( 'NONE', #34873, #105461 ) ;
#69554=CARTESIAN_POINT ( 'NONE',  ( 1.364683531249997417, 9.296875000341403350, 2.602085213965210642E-15 ) ) ;
#69568=CARTESIAN_POINT ( 'NONE',  ( 1.499999999999996891, 9.677083334016129967, -0.8660254037844378194 ) ) ;
#69578=CARTESIAN_POINT ( 'NONE',  ( 0.000000000000000000, 13.49999999999999822, -1.500000000000000222 ) ) ;
#69598=CARTESIAN_POINT ( 'NONE',  ( 1.499999999999993117, 8.635416667349460340, 0.8660254037844409281 ) ) ;
#69600=EDGE_LOOP ( 'NONE', ( #76078, #165591 ) ) ;
#69673=CARTESIAN_POINT ( 'NONE',  ( -1.115562610750309283E-14, 9.093750000682799595, 1.500000000000001554 ) ) ;
#69750=CIRCLE ( 'NONE', #125219, 2.000000000000000000 ) ;
#69801=CARTESIAN_POINT ( 'NONE',  ( -1.364683531250014514, 13.65104166700806765, -0.7879004041258335089 ) ) ;
#69987=CARTESIAN_POINT ( 'NONE',  ( -1.402160292154681736E-14, 11.42187500034139980, 1.575800808251682339 ) ) ;
#69991=CARTESIAN_POINT ( 'NONE',  ( 0.4019237886466816012, 9.426335450315370679, -1.499999999999998668 ) ) ;
#69993=CARTESIAN_POINT ( 'NONE',  ( 0.7500000000000006661, 9.083333333333332149, 1.299038105676657340 ) ) ;
#70004=ORIENTED_EDGE ( 'NONE', *, *, #184537, .F. ) ;
#70036=VERTEX_POINT ( 'NONE', #34776 ) ;
#70041=CARTESIAN_POINT ( 'NONE',  ( 0.6823417656249969321, 9.588541667008065872, -1.181850606188757036 ) ) ;
#70049=CARTESIAN_POINT ( 'NONE',  ( -2.788906526875773208E-15, 10.21875000068279782, -1.499999999999998446 ) ) ;
#70069=CARTESIAN_POINT ( 'NONE',  ( 3.834746474454188013E-15, 13.09375000068279959, 1.500000000000001554 ) ) ;
#70102=CARTESIAN_POINT ( 'NONE',  ( -0.7500000000000006661, 9.239583334016129967, -1.299038105676657340 ) ) ;
#70115=AXIS2_PLACEMENT_3D ( 'NONE', #103555, #36405, #102483 ) ;
#70117=CARTESIAN_POINT ( 'NONE',  ( 1.499999999999993117, 11.63541666734946745, 0.8660254037844409281 ) ) ;
#70205=CARTESIAN_POINT ( 'NONE',  ( -8.012344526598182026E-15, 13.79687500034139624, -1.575800808251669460 ) ) ;
#70251=CARTESIAN_POINT ( 'NONE',  ( 1.499999999999993117, 13.35416666666667140, 0.8660254037844409281 ) ) ;
#70257=CARTESIAN_POINT ( 'NONE',  ( -1.364683531250000748, 12.35937500034139980, 0.000000000000000000 ) ) ;
#70300=CARTESIAN_POINT ( 'NONE',  ( -2.788906526875773208E-15, 11.96875000068279604, -1.499999999999998446 ) ) ;
#70303=CARTESIAN_POINT ( 'NONE',  ( 1.364683531249997417, 13.04687500034139980, 2.602085213965210642E-15 ) ) ;
#70331=DIRECTION ( 'NONE',  ( 0.000000000000000000, -1.000000000000000000, 0.000000000000000000 ) ) ;
#70341=CARTESIAN_POINT ( 'NONE',  ( -0.4019237886466802689, 11.44866454968463110, -1.500000000000002887 ) ) ;
#70377=DIRECTION ( 'NONE',  ( 0.000000000000000000, -1.000000000000000000, 0.000000000000000000 ) ) ;
#70390=CARTESIAN_POINT ( 'NONE',  ( 0.4339420102923677303, 3.986509213895420345, -0.4852232617283462335 ) ) ;
#70399=CARTESIAN_POINT ( 'NONE',  ( 1.364683531250000303, 11.75520833367473017, -0.7879004041258355073 ) ) ;
#70406=CARTESIAN_POINT ( 'NONE',  ( -0.7500000000000006661, 8.989583334016129967, -1.299038105676657340 ) ) ;
#70548=CARTESIAN_POINT ( 'NONE',  ( -1.364683531250000748, 10.92187500034139802, 0.000000000000000000 ) ) ;
#70561=ORIENTED_EDGE ( 'NONE', *, *, #109845, .F. ) ;
#70583=CYLINDRICAL_SURFACE ( 'NONE', #204205, 1.500000000000000222 ) ;
#70596=ORIENTED_EDGE ( 'NONE', *, *, #40853, .T. ) ;
#70617=CARTESIAN_POINT ( 'NONE',  ( -8.012344526598182026E-15, 8.859375000341405126, -1.575800808251669460 ) ) ;
#70652=B_SPLINE_CURVE_WITH_KNOTS ( 'NONE', 3,
 ( #129027, #196081, #126895, #46636, #30383, #96469, #80181, #31447, #97525, #142027, #143103, #208041, #109569, #175573 ),
 .UNSPECIFIED., .F., .F.,
 ( 4, 2, 2, 2, 2, 2, 4 ),
 ( 0.000000000000000000, 0.0006738968695872706808, 0.001010845304380905913, 0.001347793739174541362, 0.001684742173968175943, 0.002021690608761810524, 0.002695587478349080121 ),
 .UNSPECIFIED. ) ;
#70654=CARTESIAN_POINT ( 'NONE',  ( 0.000000000000000000, 0.000000000000000000, -1.500000000000000222 ) ) ;
#70662=CARTESIAN_POINT ( 'NONE',  ( -1.500000000000001110, 8.802083334016133520, 0.8660254037844419273 ) ) ;
#70708=ORIENTED_EDGE ( 'NONE', *, *, #178139, .T. ) ;
#70723=CARTESIAN_POINT ( 'NONE',  ( 0.000000000000000000, -0.5000000000000004441, 0.000000000000000000 ) ) ;
#70804=CARTESIAN_POINT ( 'NONE',  ( 1.364683531249996529, 15.27604166700806587, 0.7879004041258405033 ) ) ;
#70839=DIRECTION ( 'NONE',  ( 0.000000000000000000, -1.000000000000000000, 0.000000000000000000 ) ) ;
#70862=CARTESIAN_POINT ( 'NONE',  ( -2.788906526875773208E-15, 11.18749999999999822, -1.499999999999998446 ) ) ;
#70865=CARTESIAN_POINT ( 'NONE',  ( 0.6823417656249969321, 12.58854166700806942, -1.181850606188757036 ) ) ;
#70866=DIRECTION ( 'NONE',  ( -0.000000000000000000, 1.000000000000000000, -0.000000000000000000 ) ) ;
#71016=DIRECTION ( 'NONE',  ( 0.000000000000000000, 1.000000000000000000, 0.000000000000000000 ) ) ;
#71056=CARTESIAN_POINT ( 'NONE',  ( 1.364683531250000748, 12.50520833367473550, -0.7879004041258355073 ) ) ;
#71061=CARTESIAN_POINT ( 'NONE',  ( -1.500000000000008216, 10.25000000000000178, 3.469446951953614189E-15 ) ) ;
#71114=CARTESIAN_POINT ( 'NONE',  ( -8.012344526598182026E-15, 9.359375000341396245, -1.575800808251669460 ) ) ;
#71115=EDGE_CURVE ( 'NONE', #128668, #86318, #41982, .T. ) ;
#71182=DIRECTION ( 'NONE',  ( 0.000000000000000000, -1.000000000000000000, 0.000000000000000000 ) ) ;
#71273=CARTESIAN_POINT ( 'NONE',  ( -0.7500000000000179856, 12.54166666666666607, 1.299038105676658228 ) ) ;
#71274=CARTESIAN_POINT ( 'NONE',  ( -1.364683531250010295, 12.63020833367473372, 0.7879004041258445001 ) ) ;
#71318=CARTESIAN_POINT ( 'NONE',  ( 1.500000000000001332, 13.87499999999999822, 0.000000000000000000 ) ) ;
#71324=CARTESIAN_POINT ( 'NONE',  ( 1.364683531249996529, 12.46354166700806054, 0.7879004041258405033 ) ) ;
#71371=CARTESIAN_POINT ( 'NONE',  ( 1.364683531250000748, 13.06770833367473372, -0.7879004041258355073 ) ) ;
#71375=( BOUNDED_SURFACE ( )  B_SPLINE_SURFACE ( 3, 2, ( 
 ( #93745, #76395, #77463 ),
 ( #13527, #192263, #44992 ),
 ( #10321, #79599, #29797 ),
 ( #126304, #145718, #212783 ),
 ( #129511, #158724, #142504 ),
 ( #208512, #112177, #211716 ),
 ( #12450, #11385, #143581 ),
 ( #180307, #28723, #176052 ),
 ( #159783, #63353, #43925 ),
 ( #177107, #195492, #61219 ),
 ( #210661, #127376, #160858 ),
 ( #130564, #60146, #110040 ),
 ( #27645, #209574, #193348 ),
 ( #14579, #111101, #47127 ),
 ( #94809, #78528, #144645 ),
 ( #62287, #48196, #128447 ),
 ( #162998, #179247, #178182 ),
 ( #194414, #46056, #95881 ) ),
 .UNSPECIFIED., .F., .F., .T. ) 
 B_SPLINE_SURFACE_WITH_KNOTS ( ( 4, 2, 2, 2, 2, 2, 2, 2, 4 ),
 ( 3, 3 ),
 ( 0.001893572594152293821, 0.002130269168421383350, 0.002366965742690472444, 0.002603662316959561539, 0.002840358891228651067, 0.003077055465497740595, 0.003313752039766830124, 0.003550448614035919652, 0.003787145188305008747 ),
 ( 0.000000000000000000, 1.000000000000000000 ),
 .UNSPECIFIED. ) 
 GEOMETRIC_REPRESENTATION_ITEM ( )  RATIONAL_B_SPLINE_SURFACE ( (
 ( 1.000000000000000000, 0.5649783097559765155, 1.000000000000000000),
 ( 1.000000000000000000, 0.5467450299869772712, 1.000000000000000000),
 ( 1.000000000000000000, 0.5350701846666650052, 1.000000000000000000),
 ( 1.000000000000000000, 0.5340147030925761484, 1.000000000000000000),
 ( 1.000000000000000000, 0.5447811154896697872, 1.000000000000000000),
 ( 1.000000000000000000, 0.5795975317820121209, 1.000000000000000000),
 ( 1.000000000000000000, 0.6028840214606389081, 1.000000000000000000),
 ( 1.000000000000000000, 0.6474634991924413940, 1.000000000000000000),
 ( 1.000000000000000000, 0.6683065367292350123, 1.000000000000000000),
 ( 1.000000000000000000, 0.6980320384851331772, 1.000000000000000000),
 ( 1.000000000000000000, 0.7066998895408397319, 1.000000000000000000),
 ( 1.000000000000000000, 0.7074845257686436240, 1.000000000000000000),
 ( 1.000000000000000000, 0.6995439292594691771, 1.000000000000000000),
 ( 1.000000000000000000, 0.6710262760327128095, 1.000000000000000000),
 ( 1.000000000000000000, 0.6504357685074378947, 1.000000000000000000),
 ( 1.000000000000000000, 0.6062099919889085697, 1.000000000000000000),
 ( 1.000000000000000000, 0.5828135443829817186, 1.000000000000000000),
 ( 1.000000000000000000, 0.5647844906712726765, 1.000000000000000000) ) ) 
 REPRESENTATION_ITEM ( '' )  SURFACE ( )  );
#71392=CARTESIAN_POINT ( 'NONE',  ( -1.500000000000001110, 10.27083333333332860, 0.8660254037844418162 ) ) ;
#71400=CARTESIAN_POINT ( 'NONE',  ( 1.364683531250000748, 13.25520833367473017, -0.7879004041258355073 ) ) ;
#71440=CARTESIAN_POINT ( 'NONE',  ( 0.7500000000000006661, 14.61458333401613530, 1.299038105676657340 ) ) ;
#71474=CARTESIAN_POINT ( 'NONE',  ( -1.402160292154681736E-14, 10.42187500034139447, 1.575800808251682339 ) ) ;
#71476=CARTESIAN_POINT ( 'NONE',  ( -0.7807912181424305764, 13.24045051524828942, -1.280767376876722041 ) ) ;
#71561=DIRECTION ( 'NONE',  ( 0.000000000000000000, 1.000000000000000000, 0.000000000000000000 ) ) ;
#71573=DIRECTION ( 'NONE',  ( 0.000000000000000000, -1.000000000000000000, 0.000000000000000000 ) ) ;
#71623=CARTESIAN_POINT ( 'NONE',  ( 0.6823417656249934904, 11.25520833367473017, 1.181850606188764807 ) ) ;
#71647=CARTESIAN_POINT ( 'NONE',  ( 1.364683531250000303, 14.00520833367473195, -0.7879004041258355073 ) ) ;
#71671=CARTESIAN_POINT ( 'NONE',  ( 1.836970198721030181E-16, 13.49999999999999822, 1.500000000000000222 ) ) ;
#71690=CARTESIAN_POINT ( 'NONE',  ( 0.6823417656249969321, 8.588541667008065872, -1.181850606188757036 ) ) ;
#71725=DIRECTION ( 'NONE',  ( 0.5000000000000001110, 0.000000000000000000, -0.8660254037844385966 ) ) ;
#71733=CARTESIAN_POINT ( 'NONE',  ( 0.6823417656249934904, 15.19270833367473372, 1.181850606188764807 ) ) ;
#71758=EDGE_LOOP ( 'NONE', ( #125060, #102993, #172363, #8330, #84491 ) ) ;
#71771=CARTESIAN_POINT ( 'NONE',  ( -1.364683531250000748, 8.390625000341399797, 0.000000000000000000 ) ) ;
#71800=EDGE_CURVE ( 'NONE', #32497, #143111, #140351, .T. ) ;
#71829=CARTESIAN_POINT ( 'NONE',  ( 1.499999999999993117, 8.385416667349467446, 0.8660254037844408170 ) ) ;
#71875=CARTESIAN_POINT ( 'NONE',  ( 1.364683531249996529, 15.02604166700806587, 0.7879004041258405033 ) ) ;
#71879=CARTESIAN_POINT ( 'NONE',  ( -0.7500000000000006661, 10.48958333401613174, -1.299038105676657340 ) ) ;
#71911=ORIENTED_EDGE ( 'NONE', *, *, #181109, .T. ) ;
#71937=CARTESIAN_POINT ( 'NONE',  ( -1.364683531250000748, 12.92187500034139980, 0.000000000000000000 ) ) ;
#72023=AXIS2_PLACEMENT_3D ( 'NONE', #77722, #158982, #110299 ) ;
#72063=CARTESIAN_POINT ( 'NONE',  ( -1.350829346764931271, 4.253646974019544835, -0.3155766437963781201 ) ) ;
#72131=CARTESIAN_POINT ( 'NONE',  ( 0.6823417656249969321, 11.27604166700806765, -1.181850606188757036 ) ) ;
#72137=CARTESIAN_POINT ( 'NONE',  ( -0.7500000000000006661, 10.20833333333333393, -1.299038105676657340 ) ) ;
#72156=CARTESIAN_POINT ( 'NONE',  ( -0.7500000000000006661, 8.739583334016129967, -1.299038105676657340 ) ) ;
#72185=CARTESIAN_POINT ( 'NONE',  ( 0.6823417656249934904, 9.755208333674728394, 1.181850606188764807 ) ) ;
#72199=CARTESIAN_POINT ( 'NONE',  ( -1.500000000000001110, 12.55208333401612819, 0.8660254037844418162 ) ) ;
#72243=CARTESIAN_POINT ( 'NONE',  ( -0.7500000000000179856, 9.322916667349467446, 1.299038105676658228 ) ) ;
#72326=ORIENTED_EDGE ( 'NONE', *, *, #58887, .T. ) ;
#72363=VERTEX_POINT ( 'NONE', #44152 ) ;
#72395=DIRECTION ( 'NONE',  ( 1.000000000000000000, 0.000000000000000000, 0.000000000000000000 ) ) ;
#72397=CARTESIAN_POINT ( 'NONE',  ( -0.7500000000000006661, 13.45833333333333570, -1.299038105676657340 ) ) ;
#72402=CARTESIAN_POINT ( 'NONE',  ( -1.402160292154681736E-14, 10.42187500034139447, 1.575800808251682339 ) ) ;
#72447=CARTESIAN_POINT ( 'NONE',  ( -8.012344526598182026E-15, 13.10937500034139980, -1.575800808251669460 ) ) ;
#72486=CARTESIAN_POINT ( 'NONE',  ( -0.4019237886467001974, 11.55133545031536713, 1.500000000000001998 ) ) ;
#72495=DIRECTION ( 'NONE',  ( 0.8660254037844388186, 0.000000000000000000, -0.4999999999999997780 ) ) ;
#72518=CARTESIAN_POINT ( 'NONE',  ( 1.500000000000001332, 15.15625000068279782, 0.000000000000000000 ) ) ;
#72552=CARTESIAN_POINT ( 'NONE',  ( -8.012344526598182026E-15, 10.79687500034139624, -1.575800808251669460 ) ) ;
#72704=CARTESIAN_POINT ( 'NONE',  ( -0.6823417656250039265, 10.63020833367472839, -1.181850606188755259 ) ) ;
#72726=CARTESIAN_POINT ( 'NONE',  ( 0.4339943706424725378, 3.713305424705313218, 0.4851827343914862922 ) ) ;
#72730=CARTESIAN_POINT ( 'NONE',  ( -1.364683531250000748, 14.85937500034140157, 0.000000000000000000 ) ) ;
#72735=CARTESIAN_POINT ( 'NONE',  ( -1.500000000000008216, 8.500000000000000000, 3.469446951953614189E-15 ) ) ;
#72772=CARTESIAN_POINT ( 'NONE',  ( -1.364683531250000748, 9.671875000341396245, 0.000000000000000000 ) ) ;
#72797=DIRECTION ( 'NONE',  ( 0.000000000000000000, -1.000000000000000000, 0.000000000000000000 ) ) ;
#72806=FACE_OUTER_BOUND ( 'NONE', #10001, .T. ) ;
#72816=CARTESIAN_POINT ( 'NONE',  ( -0.6823417656250039265, 14.81770833367473195, -1.181850606188755259 ) ) ;
#72930=FACE_OUTER_BOUND ( 'NONE', #65922, .T. ) ;
#72954=CARTESIAN_POINT ( 'NONE',  ( 1.364683531249997417, 14.79687500034139447, 2.602085213965210642E-15 ) ) ;
#73017=CARTESIAN_POINT ( 'NONE',  ( -0.6823417656250003738, 13.46354166700806942, 1.181850606188754593 ) ) ;
#73063=CARTESIAN_POINT ( 'NONE',  ( -0.7662865668244825956, -4.140281660848354583, 0.6727527331025086044 ) ) ;
#73128=VERTEX_POINT ( 'NONE', #191977 ) ;
#73133=CARTESIAN_POINT ( 'NONE',  ( -1.406470046317634059, 4.362887876502464124, 0.01120553378793602735 ) ) ;
#73177=( BOUNDED_CURVE ( )  B_SPLINE_CURVE ( 2, ( #132797, #65597, #131746, #179403, #15794, #16854, #115509, #31023, #197751 ),
 .UNSPECIFIED., .F., .T. ) 
 B_SPLINE_CURVE_WITH_KNOTS ( ( 3, 2, 2, 2, 3 ),
 ( 0.9375000000000000000, 0.9404761904761904656, 0.9464285714285713969, 0.9523809523809523281, 0.9553571428571427937 ),
 .UNSPECIFIED. ) 
 CURVE ( )  GEOMETRIC_REPRESENTATION_ITEM ( )  RATIONAL_B_SPLINE_CURVE ( ( 0.9330127018922194093, 0.9330127018922194093, 1.000000000000000000, 0.8660254037844387076, 1.000000000000000000, 0.8660254037844387076, 1.000000000000000000, 0.9330127018922206306, 0.9330127018922194093 ) ) 
 REPRESENTATION_ITEM ( '' )  );
#73201=CARTESIAN_POINT ( 'NONE',  ( 1.364683531250000748, 10.25520833367473017, -0.7879004041258355073 ) ) ;
#73207=CARTESIAN_POINT ( 'NONE',  ( 1.499999999999993117, 9.354166666666667851, 0.8660254037844409281 ) ) ;
#73383=CARTESIAN_POINT ( 'NONE',  ( 0.4019237886466816012, 11.92633545031536890, -1.499999999999998668 ) ) ;
#73406=ORIENTED_EDGE ( 'NONE', *, *, #55165, .T. ) ;
#73447=CARTESIAN_POINT ( 'NONE',  ( 1.396038594575822023, 3.355321791732675418, 0.1345620919992574216 ) ) ;
#73472=CARTESIAN_POINT ( 'NONE',  ( -0.7500000000000179856, 13.04166666666666607, 1.299038105676658228 ) ) ;
#73479=CARTESIAN_POINT ( 'NONE',  ( 0.6823417656249969321, 10.77604166700806765, -1.181850606188757036 ) ) ;
#73506=DIRECTION ( 'NONE',  ( 0.000000000000000000, -1.000000000000000000, 0.000000000000000000 ) ) ;
#73525=CARTESIAN_POINT ( 'NONE',  ( 1.364683531249996529, 11.77604166700806765, 0.7879004041258403923 ) ) ;
#73554=CARTESIAN_POINT ( 'NONE',  ( 0.6823417656249969321, 12.77604166700806232, -1.181850606188757036 ) ) ;
#73593=CARTESIAN_POINT ( 'NONE',  ( 0.7500000000000006661, 14.94791666734946567, -1.299038105676657340 ) ) ;
#73630=CARTESIAN_POINT ( 'NONE',  ( 1.364683531249997417, 9.984375000341398021, 2.602085213965210642E-15 ) ) ;
#73639=CARTESIAN_POINT ( 'NONE',  ( -0.7500000000000179856, 9.072916667349467446, 1.299038105676658228 ) ) ;
#73718=VECTOR ( 'NONE', #12066, 1000.000000000000000 ) ;
#73746=CARTESIAN_POINT ( 'NONE',  ( -2.788906526875773208E-15, 10.93750000000000178, -1.499999999999998446 ) ) ;
#73765=CARTESIAN_POINT ( 'NONE',  ( 1.499999999999993117, 10.38541666734946212, 0.8660254037844408170 ) ) ;
#73778=CARTESIAN_POINT ( 'NONE',  ( -1.364683531250010295, 9.692708333674737275, 0.7879004041258445001 ) ) ;
#73786=CARTESIAN_POINT ( 'NONE',  ( -1.247849810309911600, 13.37576698399836594, 0.5524780460566154350 ) ) ;
#73805=CARTESIAN_POINT ( 'NONE',  ( -8.012344526598182026E-15, 14.04687500034139624, -1.575800808251669460 ) ) ;
#73845=CARTESIAN_POINT ( 'NONE',  ( -2.788906526875773208E-15, 12.96875000068279782, -1.499999999999998446 ) ) ;
#73852=CARTESIAN_POINT ( 'NONE',  ( -1.500000000000008216, 15.25000000000000000, 3.469446951953614189E-15 ) ) ;
#73902=CARTESIAN_POINT ( 'NONE',  ( -0.6823417656250039265, 14.31770833367473195, -1.181850606188755259 ) ) ;
#74016=VECTOR ( 'NONE', #124866, 1000.000000000000000 ) ;
#74045=CARTESIAN_POINT ( 'NONE',  ( 1.364683531249997417, 14.54687500034139447, 2.602085213965210642E-15 ) ) ;
#74076=( BOUNDED_CURVE ( )  B_SPLINE_CURVE ( 2, ( #120333, #154900, #73639, #169003, #137592, #172220, #70406, #136525, #88843 ),
 .UNSPECIFIED., .F., .T. ) 
 B_SPLINE_CURVE_WITH_KNOTS ( ( 3, 2, 2, 2, 3 ),
 ( 0.8839285714285713969, 0.8869047619047618625, 0.8928571428571429047, 0.8988095238095238360, 0.9017857142857143016 ),
 .UNSPECIFIED. ) 
 CURVE ( )  GEOMETRIC_REPRESENTATION_ITEM ( )  RATIONAL_B_SPLINE_CURVE ( ( 0.9330127018922194093, 0.9330127018922194093, 1.000000000000000000, 0.8660254037844387076, 1.000000000000000000, 0.8660254037844387076, 1.000000000000000000, 0.9330127018922194093, 0.9330127018922194093 ) ) 
 REPRESENTATION_ITEM ( '' )  );
#74108=CARTESIAN_POINT ( 'NONE',  ( -1.364683531250014514, 11.90104166700806587, -0.7879004041258335089 ) ) ;
#74145=DIRECTION ( 'NONE',  ( 0.000000000000000000, -1.000000000000000000, 0.000000000000000000 ) ) ;
#74150=CARTESIAN_POINT ( 'NONE',  ( -1.500000000000015099, 11.26041666734946567, -0.8660254037844309360 ) ) ;
#74296=CARTESIAN_POINT ( 'NONE',  ( -1.364683531250014514, 11.08854166700806054, -0.7879004041258335089 ) ) ;
#74302=CARTESIAN_POINT ( 'NONE',  ( 1.499999999999993117, 8.604166666666664298, 0.8660254037844409281 ) ) ;
#74353=CARTESIAN_POINT ( 'NONE',  ( 0.6823417656249969321, 8.588541667008065872, -1.181850606188757036 ) ) ;
#74470=CARTESIAN_POINT ( 'NONE',  ( -2.788906526875773208E-15, 11.93750000000000000, -1.499999999999998446 ) ) ;
#74508=( BOUNDED_CURVE ( )  B_SPLINE_CURVE ( 2, ( #23710, #57292, #88739, #123456, #189418, #5298, #54096, #188345, #39984 ),
 .UNSPECIFIED., .F., .T. ) 
 B_SPLINE_CURVE_WITH_KNOTS ( ( 3, 2, 2, 2, 3 ),
 ( 0.4196428571428570953, 0.4226190476190476164, 0.4285714285714285476, 0.4345238095238095344, 0.4375000000000000000 ),
 .UNSPECIFIED. ) 
 CURVE ( )  GEOMETRIC_REPRESENTATION_ITEM ( )  RATIONAL_B_SPLINE_CURVE ( ( 0.9330127018922194093, 0.9330127018922180770, 1.000000000000000000, 0.8660254037844387076, 1.000000000000000000, 0.8660254037844387076, 1.000000000000000000, 0.9330127018922194093, 0.9330127018922194093 ) ) 
 REPRESENTATION_ITEM ( '' )  );
#74513=CARTESIAN_POINT ( 'NONE',  ( -0.7500000000000006661, 10.45833333333333393, -1.299038105676657340 ) ) ;
#74556=CARTESIAN_POINT ( 'NONE',  ( 1.499999999999997113, 12.89583333333333215, -0.8660254037844378194 ) ) ;
#74562=CARTESIAN_POINT ( 'NONE',  ( 0.6823417656249969321, 11.27604166700806765, -1.181850606188757036 ) ) ;
#74579=DIRECTION ( 'NONE',  ( 0.000000000000000000, -1.000000000000000000, 0.000000000000000000 ) ) ;
#74584=FACE_OUTER_BOUND ( 'NONE', #110491, .T. ) ;
#74603=CARTESIAN_POINT ( 'NONE',  ( -1.364683531250000748, 11.42187500034139802, 0.000000000000000000 ) ) ;
#74629=LINE ( 'NONE', #140734, #131487 ) ;
#74670=CARTESIAN_POINT ( 'NONE',  ( -0.7500000000000179856, 14.82291666734946567, 1.299038105676658228 ) ) ;
#74678=CARTESIAN_POINT ( 'NONE',  ( 0.000000000000000000, 13.49999999999999822, 0.000000000000000000 ) ) ;
#74703=CARTESIAN_POINT ( 'NONE',  ( -1.402160292154681736E-14, 9.921875000341401574, 1.575800808251682339 ) ) ;
#74805=FACE_OUTER_BOUND ( 'NONE', #186012, .T. ) ;
#74858=CARTESIAN_POINT ( 'NONE',  ( 0.6823417656249969321, 9.838541667008065872, -1.181850606188757036 ) ) ;
#74879=CARTESIAN_POINT ( 'NONE',  ( 1.364683531249997417, 14.23437500034140157, 2.602085213965210642E-15 ) ) ;
#74891=DIRECTION ( 'NONE',  ( 0.000000000000000000, -1.000000000000000000, 0.000000000000000000 ) ) ;
#74897=CARTESIAN_POINT ( 'NONE',  ( -2.788906526875773208E-15, 9.968750000682797818, -1.499999999999998446 ) ) ;
#74921=CARTESIAN_POINT ( 'NONE',  ( -1.402160292154681736E-14, 14.56249999999999645, 1.732050807568881190 ) ) ;
#74935=CARTESIAN_POINT ( 'NONE',  ( -2.788906526875773208E-15, 10.96875000068279427, -1.499999999999998446 ) ) ;
#74956=PLANE ( 'NONE',  #93693 ) ;
#74965=CARTESIAN_POINT ( 'NONE',  ( 1.364683531250000303, 14.25520833367473372, -0.7879004041258355073 ) ) ;
#74999=( NAMED_UNIT ( * ) SI_UNIT ( $, .STERADIAN. ) SOLID_ANGLE_UNIT ( ) );
#75058=CARTESIAN_POINT ( 'NONE',  ( -2.788906526875773208E-15, 10.43750000000000000, -1.499999999999998446 ) ) ;
#75110=CARTESIAN_POINT ( 'NONE',  ( -1.364683531250010295, 13.94270833367473195, 0.7879004041258445001 ) ) ;
#75176=CARTESIAN_POINT ( 'NONE',  ( -1.402160292154681736E-14, 11.73437500034140335, 1.575800808251682339 ) ) ;
#75216=CARTESIAN_POINT ( 'NONE',  ( -1.500000000000015099, 10.76041666734946389, -0.8660254037844309360 ) ) ;
#75222=ADVANCED_FACE ( 'NONE', ( #102928 ), #1134, .T. ) ;
#75271=CARTESIAN_POINT ( 'NONE',  ( 0.6224592253955643084, -4.250299932362443300, 0.9218689959748729290 ) ) ;
#75293=CARTESIAN_POINT ( 'NONE',  ( -1.346800533732415817, 4.238484701306172830, 0.3345042947240802755 ) ) ;
#75359=CARTESIAN_POINT ( 'NONE',  ( 1.364683531249996529, 10.46354166700806765, 0.7879004041258403923 ) ) ;
#75365=CARTESIAN_POINT ( 'NONE',  ( -1.500000000000008216, 8.750000000000000000, 3.469446951953614189E-15 ) ) ;
#75389=AXIS2_PLACEMENT_3D ( 'NONE', #124009, #90364, #8016 ) ;
#75430=CARTESIAN_POINT ( 'NONE',  ( -8.012344526598182026E-15, 15.10937500034140157, -1.575800808251669460 ) ) ;
#75586=VECTOR ( 'NONE', #67647, 1000.000000000000000 ) ;
#75612=EDGE_CURVE ( 'NONE', #46203, #79633, #52276, .T. ) ;
#75622=CARTESIAN_POINT ( 'NONE',  ( -1.500000000000001110, 12.02083333333333748, 0.8660254037844419273 ) ) ;
#75627=CARTESIAN_POINT ( 'NONE',  ( -1.364683531250000748, 10.85937500034139802, 0.000000000000000000 ) ) ;
#75667=CARTESIAN_POINT ( 'NONE',  ( -0.6823417656250003738, 12.46354166700806765, 1.181850606188754593 ) ) ;
#75675=VERTEX_POINT ( 'NONE', #137104 ) ;
#75678=CARTESIAN_POINT ( 'NONE',  ( 0.000000000000000000, -0.5000000000000004441, 0.000000000000000000 ) ) ;
#75717=CARTESIAN_POINT ( 'NONE',  ( 0.000000000000000000, 13.49999999999999822, 0.000000000000000000 ) ) ;
#75733=CARTESIAN_POINT ( 'NONE',  ( 1.500000000000001332, 13.90625000068279604, 0.000000000000000000 ) ) ;
#75741=DIRECTION ( 'NONE',  ( 0.000000000000000000, -1.000000000000000000, 0.000000000000000000 ) ) ;
#75768=CARTESIAN_POINT ( 'NONE',  ( 1.364683531250000303, 10.25520833367473017, -0.7879004041258355073 ) ) ;
#75892=CYLINDRICAL_SURFACE ( 'NONE', #79294, 1.500000000000000222 ) ;
#75917=CARTESIAN_POINT ( 'NONE',  ( 1.364683531249996529, 9.776041667008064096, 0.7879004041258405033 ) ) ;
#75976=CARTESIAN_POINT ( 'NONE',  ( 0.5773502691896192918, -4.295408888568413630, 1.000000000000004441 ) ) ;
#75985=CARTESIAN_POINT ( 'NONE',  ( -0.7500000000000179856, 15.04166666666666785, 1.299038105676658228 ) ) ;
#76006=ORIENTED_EDGE ( 'NONE', *, *, #7130, .F. ) ;
#76029=CARTESIAN_POINT ( 'NONE',  ( 1.364683531249996529, 14.46354166700806410, 0.7879004041258405033 ) ) ;
#76078=ORIENTED_EDGE ( 'NONE', *, *, #113661, .T. ) ;
#76146=CARTESIAN_POINT ( 'NONE',  ( 1.412279214364694946, 3.475718376301037527, 0.5092244867763745519 ) ) ;
#76169=CARTESIAN_POINT ( 'NONE',  ( -0.6823417656250039265, 13.63020833367473195, -1.181850606188755259 ) ) ;
#76177=CARTESIAN_POINT ( 'NONE',  ( -2.788906526875773208E-15, 8.718750000682796042, -1.499999999999998446 ) ) ;
#76234=CARTESIAN_POINT ( 'NONE',  ( -1.364683531250000748, 11.92187500034139980, 0.000000000000000000 ) ) ;
#76276=CARTESIAN_POINT ( 'NONE',  ( 1.500000000000001332, 11.15625000068279427, 0.000000000000000000 ) ) ;
#76376=CARTESIAN_POINT ( 'NONE',  ( 1.478132491927091063, 4.278202457637306999, -0.2687277897297863372 ) ) ;
#76395=CARTESIAN_POINT ( 'NONE',  ( -1.430949710260827068, 4.025263519208237106, 0.4689103363400777824 ) ) ;
#76410=CARTESIAN_POINT ( 'NONE',  ( 1.364683531249996529, 11.21354166700806410, 0.7879004041258403923 ) ) ;
#76416=EDGE_CURVE ( 'NONE', #156928, #124391, #104263, .T. ) ;
#76417=CARTESIAN_POINT ( 'NONE',  ( -6.009258394948636914E-15, 8.687500000000001776, -1.732050807568875195 ) ) ;
#76446=CARTESIAN_POINT ( 'NONE',  ( -1.500000000000001110, 8.802083334016133520, 0.8660254037844418162 ) ) ;
#76617=CARTESIAN_POINT ( 'NONE',  ( 4.764381983412778688E-15, 12.71875000068279782, -1.499999999999998446 ) ) ;
#76676=CARTESIAN_POINT ( 'NONE',  ( 0.7500000000000006661, 12.91666666666666607, -1.299038105676657340 ) ) ;
#76681=CARTESIAN_POINT ( 'NONE',  ( 1.364683531249996529, 10.46354166700806765, 0.7879004041258405033 ) ) ;
#76717=CARTESIAN_POINT ( 'NONE',  ( -0.6823417656250039265, 12.38020833367473017, -1.181850606188755259 ) ) ;
#76785=CARTESIAN_POINT ( 'NONE',  ( 1.499999999999997113, 14.42708333401612819, -0.8660254037844378194 ) ) ;
#76820=CARTESIAN_POINT ( 'NONE',  ( -1.364683531250010295, 8.880208333674731946, 0.7879004041258445001 ) ) ;
#76923=DIRECTION ( 'NONE',  ( 0.000000000000000000, -1.000000000000000000, 0.000000000000000000 ) ) ;
#76956=CARTESIAN_POINT ( 'NONE',  ( -1.500000000000008216, 11.74999999999999645, 3.469446951953614189E-15 ) ) ;
#76969=CARTESIAN_POINT ( 'NONE',  ( 1.364683531249996529, 9.526041667008062319, 0.7879004041258405033 ) ) ;
#76982=CARTESIAN_POINT ( 'NONE',  ( 1.264911064067342439, 3.884384971023816746, -0.4999999999999986122 ) ) ;
#77039=CARTESIAN_POINT ( 'NONE',  ( 1.499999999999993117, 14.60416666666666963, 0.8660254037844409281 ) ) ;
#77086=CARTESIAN_POINT ( 'NONE',  ( -0.6823417656250003738, 13.90104166700806232, 1.181850606188754593 ) ) ;
#77177=CARTESIAN_POINT ( 'NONE',  ( 3.834746474454188013E-15, 12.31250000000000178, 1.500000000000001554 ) ) ;
#77189=VECTOR ( 'NONE', #15870, 1000.000000000000000 ) ;
#77206=CARTESIAN_POINT ( 'NONE',  ( 1.467639082483200630, 3.323620087475168905, 0.3198401300024580896 ) ) ;
#77229=CARTESIAN_POINT ( 'NONE',  ( -0.6823417656250003738, 13.96354166700806942, 1.181850606188754593 ) ) ;
#77301=CARTESIAN_POINT ( 'NONE',  ( 1.364683531249996529, 11.27604166700806410, 0.7879004041258405033 ) ) ;
#77343=CARTESIAN_POINT ( 'NONE',  ( -1.500000000000008216, 11.03125000068279427, 3.469446951953614189E-15 ) ) ;
#77353=DIRECTION ( 'NONE',  ( 0.000000000000000000, -1.000000000000000000, 0.000000000000000000 ) ) ;
#77393=CARTESIAN_POINT ( 'NONE',  ( 0.5773502691896192918, -2.500000000000002220, 1.000000000000004441 ) ) ;
#77398=CARTESIAN_POINT ( 'NONE',  ( 0.6685859206620029527, -4.211945764156018512, 0.8419752161881538521 ) ) ;
#77463=CARTESIAN_POINT ( 'NONE',  ( -1.378881877344243723, 4.087185210397143109, 0.5904953584335904671 ) ) ;
#77481=CARTESIAN_POINT ( 'NONE',  ( 1.364683531250000748, 9.755208333674737275, -0.7879004041258355073 ) ) ;
#77538=CARTESIAN_POINT ( 'NONE',  ( -1.154700538379266339, -2.500000000000002220, 2.602085213965210642E-15 ) ) ;
#77541=LINE ( 'NONE', #174013, #54692 ) ;
#77553=CARTESIAN_POINT ( 'NONE',  ( -0.6823417656250039265, 15.38020833367473372, -1.181850606188755259 ) ) ;
#77565=CARTESIAN_POINT ( 'NONE',  ( 1.500000000000001332, 13.12499999999999822, 0.000000000000000000 ) ) ;
#77682=CARTESIAN_POINT ( 'NONE',  ( -1.500000000000008216, 9.000000000000001776, 3.469446951953614189E-15 ) ) ;
#77722=CARTESIAN_POINT ( 'NONE',  ( 0.000000000000000000, 13.49999999999999822, 0.000000000000000000 ) ) ;
#77744=CARTESIAN_POINT ( 'NONE',  ( -0.7500000000000006661, 12.45833333333333570, -1.299038105676657340 ) ) ;
#77750=CARTESIAN_POINT ( 'NONE',  ( 0.6823417656249934904, 9.192708333674733723, 1.181850606188764807 ) ) ;
#77783=ORIENTED_EDGE ( 'NONE', *, *, #46115, .T. ) ;
#77788=CARTESIAN_POINT ( 'NONE',  ( -0.6823417656250003738, 11.46354166700806765, 1.181850606188754593 ) ) ;
#77835=CARTESIAN_POINT ( 'NONE',  ( 0.000000000000000000, -0.5000000000000004441, 0.000000000000000000 ) ) ;
#77856=CARTESIAN_POINT ( 'NONE',  ( -0.7500000000000179856, 13.82291666734946567, 1.299038105676658228 ) ) ;
#77893=CARTESIAN_POINT ( 'NONE',  ( -1.364683531250000748, 8.359375000341396245, 0.000000000000000000 ) ) ;
#77991=CARTESIAN_POINT ( 'NONE',  ( 1.530808498934191324E-16, 6.161115872820241535, -1.249999999999999778 ) ) ;
#78044=CARTESIAN_POINT ( 'NONE',  ( -0.6823417656250039265, 9.130208333674726617, -1.181850606188755259 ) ) ;
#78153=CARTESIAN_POINT ( 'NONE',  ( -1.364683531250000748, 12.35937500034139980, 0.000000000000000000 ) ) ;
#78227=ORIENTED_EDGE ( 'NONE', *, *, #155474, .T. ) ;
#78245=CARTESIAN_POINT ( 'NONE',  ( -1.115562610750309283E-14, 10.06250000000000000, 1.500000000000001554 ) ) ;
#78250=DIRECTION ( 'NONE',  ( 0.000000000000000000, 0.000000000000000000, 1.000000000000000000 ) ) ;
#78274=CARTESIAN_POINT ( 'NONE',  ( 1.495015925693002234, 3.364811783656424637, 0.1395187543289240772 ) ) ;
#78298=CARTESIAN_POINT ( 'NONE',  ( -1.402160292154681736E-14, 13.23437500034139980, 1.575800808251682339 ) ) ;
#78364=CARTESIAN_POINT ( 'NONE',  ( 1.364683531249997417, 11.29687500034139802, 2.602085213965210642E-15 ) ) ;
#78407=CARTESIAN_POINT ( 'NONE',  ( 0.7500000000000006661, 9.864583334016129967, 1.299038105676657340 ) ) ;
#78417=CARTESIAN_POINT ( 'NONE',  ( 1.836970198721030181E-16, 13.49999999999999822, 1.500000000000000222 ) ) ;
#78460=CARTESIAN_POINT ( 'NONE',  ( -0.4153311931459070516, 3.919822700377107783, -0.4999999999999988343 ) ) ;
#78509=CARTESIAN_POINT ( 'NONE',  ( 1.500343415223059917, 4.450747917682662980, -0.07855322731631581012 ) ) ;
#78528=CARTESIAN_POINT ( 'NONE',  ( -1.466385641617019342, 3.464586277566083172, -0.3259940066991236507 ) ) ;
#78546=CARTESIAN_POINT ( 'NONE',  ( -0.6823417656250003738, 9.151041667008065872, 1.181850606188754593 ) ) ;
#78562=VERTEX_POINT ( 'NONE', #53998 ) ;
#78568=ORIENTED_EDGE ( 'NONE', *, *, #196068, .F. ) ;
#78658=EDGE_CURVE ( 'NONE', #180856, #178226, #66884, .T. ) ;
#78671=VERTEX_POINT ( 'NONE', #56429 ) ;
#78717=EDGE_CURVE ( 'NONE', #120384, #122713, #212463, .T. ) ;
#78731=CARTESIAN_POINT ( 'NONE',  ( 0.000000000000000000, -1.500000000000001332, 2.000000000000000000 ) ) ;
#78774=CIRCLE ( 'NONE', #75389, 2.000000000000000000 ) ;
#78800=CARTESIAN_POINT ( 'NONE',  ( 1.500000000000001332, 12.62499999999999645, 0.000000000000000000 ) ) ;
#78806=CARTESIAN_POINT ( 'NONE',  ( -0.6823417656250039265, 9.817708333674735499, -1.181850606188755259 ) ) ;
#78843=CARTESIAN_POINT ( 'NONE',  ( -8.012344526598182026E-15, 11.10937500034139802, -1.575800808251669460 ) ) ;
#78890=ADVANCED_FACE ( 'NONE', ( #80127 ), #15113, .T. ) ;
#78914=CARTESIAN_POINT ( 'NONE',  ( -1.500000000000008216, 14.28125000068279604, 3.469446951953614189E-15 ) ) ;
#78923=CARTESIAN_POINT ( 'NONE',  ( 0.000000000000000000, 13.20000000000000284, -1.540450515248283025 ) ) ;
#78951=CARTESIAN_POINT ( 'NONE',  ( -1.364683531250014514, 9.088541667008060543, -0.7879004041258335089 ) ) ;
#78960=CARTESIAN_POINT ( 'NONE',  ( 0.7500000000000006661, 11.19791666734946212, -1.299038105676657340 ) ) ;
#78978=ADVANCED_FACE ( 'NONE', ( #168343 ), #53521, .T. ) ;
#79094=CARTESIAN_POINT ( 'NONE',  ( -1.115562610750309283E-14, 11.81249999999999822, 1.500000000000001554 ) ) ;
#79106=CARTESIAN_POINT ( 'NONE',  ( 0.6823417656249969321, 8.588541667008065872, -1.181850606188757036 ) ) ;
#79126=ORIENTED_EDGE ( 'NONE', *, *, #26279, .T. ) ;
#79129=CARTESIAN_POINT ( 'NONE',  ( 0.7500000000000006661, 9.114583334016129967, 1.299038105676657340 ) ) ;
#79137=CARTESIAN_POINT ( 'NONE',  ( 1.378881877344245277, 3.612814789602863730, 0.5904953584335879135 ) ) ;
#79206=CARTESIAN_POINT ( 'NONE',  ( 0.4019237886466816012, 11.17633545031536713, -1.499999999999998668 ) ) ;
#79219=EDGE_CURVE ( 'NONE', #35502, #179060, #204152, .T. ) ;
#79226=CARTESIAN_POINT ( 'NONE',  ( -1.364683531250000748, 12.60937500034139980, 0.000000000000000000 ) ) ;
#79238=CARTESIAN_POINT ( 'NONE',  ( -1.443845971921561722, 4.128618707767023999, -0.4218533236949579268 ) ) ;
#79294=AXIS2_PLACEMENT_3D ( 'NONE', #26063, #161423, #208013 ) ;
#79343=ORIENTED_EDGE ( 'NONE', *, *, #158993, .F. ) ;
#79352=CARTESIAN_POINT ( 'NONE',  ( 1.286956418854593220, 3.652345658002546624, 0.4592741676706378895 ) ) ;
#79362=ORIENTED_EDGE ( 'NONE', *, *, #30637, .F. ) ;
#79374=CARTESIAN_POINT ( 'NONE',  ( -8.012344526598182026E-15, 14.35937500034139802, -1.575800808251669460 ) ) ;
#79396=CARTESIAN_POINT ( 'NONE',  ( 0.000000000000000000, 13.49999999999999822, 0.000000000000000000 ) ) ;
#79436=CARTESIAN_POINT ( 'NONE',  ( 0.6823417656249969321, 10.83854166700806765, -1.181850606188757036 ) ) ;
#79478=CARTESIAN_POINT ( 'NONE',  ( -6.009258394948636914E-15, 10.46875000068279604, -1.732050807568875195 ) ) ;
#79487=CARTESIAN_POINT ( 'NONE',  ( 1.499999999999993117, 10.13541666734946922, 0.8660254037844408170 ) ) ;
#79549=EDGE_CURVE ( 'NONE', #1432, #177149, #191739, .T. ) ;
#79567=ORIENTED_EDGE ( 'NONE', *, *, #134419, .T. ) ;
#79573=CARTESIAN_POINT ( 'NONE',  ( -2.788906526875773208E-15, 9.968750000682797818, -1.499999999999998446 ) ) ;
#79580=CARTESIAN_POINT ( 'NONE',  ( 1.499745039105476296, 4.349213141111352599, 0.07702037080406516634 ) ) ;
#79599=CARTESIAN_POINT ( 'NONE',  ( -1.423138288543982055, 3.910258984626137746, 0.4995221786828126787 ) ) ;
#79616=CARTESIAN_POINT ( 'NONE',  ( 0.6823417656249934904, 9.692708333674735499, 1.181850606188764807 ) ) ;
#79633=VERTEX_POINT ( 'NONE', #98560 ) ;
#79665=ORIENTED_EDGE ( 'NONE', *, *, #99125, .F. ) ;
#79697=DIRECTION ( 'NONE',  ( 0.000000000000000000, 0.000000000000000000, -1.000000000000000000 ) ) ;
#79715=CARTESIAN_POINT ( 'NONE',  ( -2.788906526875773208E-15, 9.437499999999998224, -1.499999999999998446 ) ) ;
#79763=ADVANCED_FACE ( 'NONE', ( #199223 ), #186182, .T. ) ;
#79764=B_SPLINE_CURVE_WITH_KNOTS ( 'NONE', 3,
 ( #208046, #76982, #59674, #28245, #13040, #60736 ),
 .UNSPECIFIED., .F., .F.,
 ( 4, 2, 4 ),
 ( 0.000000000000000000, 0.0001030949158708173365, 0.0002061898317416346730 ),
 .UNSPECIFIED. ) ;
#79871=CARTESIAN_POINT ( 'NONE',  ( -0.7500000000000179856, 11.04166666666666430, 1.299038105676658228 ) ) ;
#79876=CARTESIAN_POINT ( 'NONE',  ( 0.6823417656249934904, 9.692708333674735499, 1.181850606188764807 ) ) ;
#79913=CARTESIAN_POINT ( 'NONE',  ( -0.6823417656250003738, 11.21354166700806765, 1.181850606188754593 ) ) ;
#79920=CARTESIAN_POINT ( 'NONE',  ( 1.499999999999993117, 9.854166666666671404, 0.8660254037844408170 ) ) ;
#79968=PRODUCT_DEFINITION_FORMATION_WITH_SPECIFIED_SOURCE ( 'ANY', '', #14337, .NOT_KNOWN. ) ;
#79988=CARTESIAN_POINT ( 'NONE',  ( -1.500000000000008216, 13.53125000068279604, 3.469446951953614189E-15 ) ) ;
#80022=CARTESIAN_POINT ( 'NONE',  ( 0.6823417656249969321, 9.276041667008065872, -1.181850606188757036 ) ) ;
#80031=CARTESIAN_POINT ( 'NONE',  ( 0.7500000000000006661, 11.11458333401613174, 1.299038105676657340 ) ) ;
#80036=CARTESIAN_POINT ( 'NONE',  ( -2.788906526875773208E-15, 10.96875000068279427, -1.499999999999998446 ) ) ;
#80044=VERTEX_POINT ( 'NONE', #50742 ) ;
#80064=LINE ( 'NONE', #211116, #131105 ) ;
#80127=FACE_OUTER_BOUND ( 'NONE', #32580, .T. ) ;
#80174=CARTESIAN_POINT ( 'NONE',  ( 1.364683531249996529, 9.026041667008060543, 0.7879004041258405033 ) ) ;
#80181=CARTESIAN_POINT ( 'NONE',  ( -1.242505562683348774, 13.26115344136356455, 0.8107168586029942503 ) ) ;
#80203=AXIS2_PLACEMENT_3D ( 'NONE', #158096, #154885, #122475 ) ;
#80209=EDGE_CURVE ( 'NONE', #46203, #96430, #212045, .T. ) ;
#80290=CARTESIAN_POINT ( 'NONE',  ( -1.364683531250014514, 12.83854166700806232, -0.7879004041258335089 ) ) ;
#80442=CARTESIAN_POINT ( 'NONE',  ( -1.364683531250010295, 12.44270833367473372, 0.7879004041258445001 ) ) ;
#80493=VECTOR ( 'NONE', #178248, 1000.000000000000000 ) ;
#80504=CARTESIAN_POINT ( 'NONE',  ( -1.364683531250000748, 10.67187500034139802, 0.000000000000000000 ) ) ;
#80547=CARTESIAN_POINT ( 'NONE',  ( -6.009258394948636914E-15, 9.718750000682803147, -1.732050807568875195 ) ) ;
#80601=CARTESIAN_POINT ( 'NONE',  ( -0.4153311931459124362, 3.919672248384428404, 0.5000000000000073275 ) ) ;
#80657=CARTESIAN_POINT ( 'NONE',  ( 1.449495214452817038, 4.332601206217148615, -0.3909641857570877455 ) ) ;
#80695=CARTESIAN_POINT ( 'NONE',  ( 0.6823417656249969321, 9.526041667008065872, -1.181850606188757036 ) ) ;
#80696=CARTESIAN_POINT ( 'NONE',  ( 0.000000000000000000, 13.49999999999999822, -1.500000000000000222 ) ) ;
#80709=DIRECTION ( 'NONE',  ( -0.8660254037844411501, -0.4999999999999956146, 5.551115123125779621E-17 ) ) ;
#80766=CARTESIAN_POINT ( 'NONE',  ( 1.364683531250000303, 14.31770833367473372, -0.7879004041258355073 ) ) ;
#80770=EDGE_CURVE ( 'NONE', #175679, #140850, #123955, .T. ) ;
#80945=CARTESIAN_POINT ( 'NONE',  ( 1.499999999999997113, 10.64583333333333037, -0.8660254037844378194 ) ) ;
#80950=CARTESIAN_POINT ( 'NONE',  ( -0.6823417656250003738, 9.151041667008065872, 1.181850606188754593 ) ) ;
#80954=VERTEX_POINT ( 'NONE', #59276 ) ;
#80958=CARTESIAN_POINT ( 'NONE',  ( -0.5993518605652793374, 3.417525394178890785, -0.2595036419143044726 ) ) ;
#80989=CARTESIAN_POINT ( 'NONE',  ( -0.6823417656250039265, 10.63020833367472839, -1.181850606188755259 ) ) ;
#81003=CARTESIAN_POINT ( 'NONE',  ( -5.000000000000009770, 3.850000000000006306, 6.071532165918824830E-15 ) ) ;
#81062=CARTESIAN_POINT ( 'NONE',  ( -6.009258394948636914E-15, 11.96875000068279604, -1.732050807568875195 ) ) ;
#81093=CARTESIAN_POINT ( 'NONE',  ( -0.6823417656250003738, 9.151041667008065872, 1.181850606188754593 ) ) ;
#81191=CARTESIAN_POINT ( 'NONE',  ( -1.408069224121404561, 3.464533069549484701, -0.5223881139200234891 ) ) ;
#81332=VERTEX_POINT ( 'NONE', #79573 ) ;
#81356=CARTESIAN_POINT ( 'NONE',  ( 1.364683531250000303, 12.50520833367473195, -0.7879004041258355073 ) ) ;
#81458=CYLINDRICAL_SURFACE ( 'NONE', #165305, 1.249999999999999778 ) ;
#81479=CARTESIAN_POINT ( 'NONE',  ( 3.834746474454188013E-15, 12.31250000000000178, 1.500000000000001554 ) ) ;
#81507=CARTESIAN_POINT ( 'NONE',  ( -1.364683531250000748, 11.92187500034139980, 0.000000000000000000 ) ) ;
#81549=DIRECTION ( 'NONE',  ( 0.000000000000000000, 0.000000000000000000, -1.000000000000000000 ) ) ;
#81565=CARTESIAN_POINT ( 'NONE',  ( 1.364683531249996529, 10.02604166700806587, 0.7879004041258405033 ) ) ;
#81571=CIRCLE ( 'NONE', #29793, 2.000000000000000000 ) ;
#81608=CARTESIAN_POINT ( 'NONE',  ( 0.7500000000000006661, 10.44791666734946212, -1.299038105676657340 ) ) ;
#81610=ORIENTED_EDGE ( 'NONE', *, *, #79549, .T. ) ;
#81632=CIRCLE ( 'NONE', #175043, 0.1000000000000001027 ) ;
#81751=CARTESIAN_POINT ( 'NONE',  ( -8.012344526598182026E-15, 8.796875000341403350, -1.575800808251669460 ) ) ;
#81821=CARTESIAN_POINT ( 'NONE',  ( -1.364683531250000748, 14.67187500034139447, 0.000000000000000000 ) ) ;
#81874=ORIENTED_EDGE ( 'NONE', *, *, #112471, .T. ) ;
#81951=VERTEX_POINT ( 'NONE', #75058 ) ;
#82003=CARTESIAN_POINT ( 'NONE',  ( -0.7500000000000179856, 11.29166666666666430, 1.299038105676658228 ) ) ;
#82007=CARTESIAN_POINT ( 'NONE',  ( -1.402160292154681736E-14, 9.921875000341401574, 1.575800808251682339 ) ) ;
#82017=CARTESIAN_POINT ( 'NONE',  ( -0.5998553420608248032, 3.416832205580481840, 0.2583637543479647691 ) ) ;
#82043=CARTESIAN_POINT ( 'NONE',  ( -0.6823417656250003738, 10.96354166700806765, 1.181850606188754593 ) ) ;
#82059=CARTESIAN_POINT ( 'NONE',  ( 1.499999999999996891, 10.89583333333333215, -0.8660254037844378194 ) ) ;
#82116=CARTESIAN_POINT ( 'NONE',  ( 1.499999999999997113, 11.92708333401613174, -0.8660254037844378194 ) ) ;
#82208=VECTOR ( 'NONE', #35574, 1000.000000000000114 ) ;
#82289=CARTESIAN_POINT ( 'NONE',  ( 0.2026985623078847998, -4.140708350189159503, -0.9999999999999991118 ) ) ;
#82296=CARTESIAN_POINT ( 'NONE',  ( -1.364683531250010295, 8.692708333674730170, 0.7879004041258445001 ) ) ;
#82409=CARTESIAN_POINT ( 'NONE',  ( 0.6823417656249934904, 11.19270833367473550, 1.181850606188764807 ) ) ;
#82438=CARTESIAN_POINT ( 'NONE',  ( 0.8610211112611746431, 13.30206454917688497, 1.155895390264894518 ) ) ;
#82449=ORIENTED_EDGE ( 'NONE', *, *, #29537, .F. ) ;
#82466=AXIS2_PLACEMENT_3D ( 'NONE', #6165, #187067, #38699 ) ;
#82506=FACE_OUTER_BOUND ( 'NONE', #142539, .T. ) ;
#82559=CARTESIAN_POINT ( 'NONE',  ( 0.6823417656249934904, 12.50520833367473017, 1.181850606188764807 ) ) ;
#82586=CARTESIAN_POINT ( 'NONE',  ( -0.4019237886466871523, 11.94866454968463110, -1.499999999999998668 ) ) ;
#82623=CARTESIAN_POINT ( 'NONE',  ( -1.364683531250010295, 10.69270833367473372, 0.7879004041258445001 ) ) ;
#82638=DIRECTION ( 'NONE',  ( -0.000000000000000000, 1.000000000000000000, -0.000000000000000000 ) ) ;
#82666=CARTESIAN_POINT ( 'NONE',  ( -0.7500000000000179856, 9.322916667349467446, 1.299038105676658228 ) ) ;
#82877=CARTESIAN_POINT ( 'NONE',  ( 1.364683531250000303, 14.06770833367473550, -0.7879004041258355073 ) ) ;
#82985=CARTESIAN_POINT ( 'NONE',  ( 0.7500000000000006661, 12.94791666734946389, -1.299038105676657340 ) ) ;
#83061=CARTESIAN_POINT ( 'NONE',  ( -1.500000000000001110, 11.52083333333333393, 0.8660254037844419273 ) ) ;
#83066=CARTESIAN_POINT ( 'NONE',  ( -0.6823417656250039265, 15.38020833367473372, -1.181850606188755259 ) ) ;
#83106=CARTESIAN_POINT ( 'NONE',  ( 1.364683531250000748, 10.56770833367473195, -0.7879004041258355073 ) ) ;
#83117=VERTEX_POINT ( 'NONE', #106288 ) ;
#83163=CARTESIAN_POINT ( 'NONE',  ( 1.499999999999993117, 8.604166666666664298, 0.8660254037844408170 ) ) ;
#83178=CARTESIAN_POINT ( 'NONE',  ( 0.7500000000000006661, 12.94791666734946389, -1.299038105676657340 ) ) ;
#83245=CARTESIAN_POINT ( 'NONE',  ( 3.834746474454188013E-15, 10.81250000000000355, 1.500000000000001554 ) ) ;
#83319=CARTESIAN_POINT ( 'NONE',  ( 0.6823417656249969321, 11.77604166700806054, -1.181850606188757036 ) ) ;
#83357=CARTESIAN_POINT ( 'NONE',  ( -1.364683531250000748, 8.421875000341403350, 0.000000000000000000 ) ) ;
#83369=( BOUNDED_CURVE ( )  B_SPLINE_CURVE ( 2, ( #205229, #56870, #3811, #123046, #119800, #188997, #16075, #164489, #137064 ),
 .UNSPECIFIED., .F., .T. ) 
 B_SPLINE_CURVE_WITH_KNOTS ( ( 3, 2, 2, 2, 3 ),
 ( 0.8125000000000000000, 0.8154761904761904656, 0.8214285714285713969, 0.8273809523809523281, 0.8303571428571429047 ),
 .UNSPECIFIED. ) 
 CURVE ( )  GEOMETRIC_REPRESENTATION_ITEM ( )  RATIONAL_B_SPLINE_CURVE ( ( 0.9330127018922194093, 0.9330127018922194093, 1.000000000000000000, 0.8660254037844387076, 1.000000000000000000, 0.8660254037844387076, 1.000000000000000000, 0.9330127018922180770, 0.9330127018922194093 ) ) 
 REPRESENTATION_ITEM ( '' )  );
#83415=CARTESIAN_POINT ( 'NONE',  ( 0.4019237886466778820, 11.32366454968462932, 1.500000000000001554 ) ) ;
#83416=EDGE_CURVE ( 'NONE', #169050, #137942, #156466, .T. ) ;
#83474=CARTESIAN_POINT ( 'NONE',  ( 1.364683531249997417, 11.48437500034139802, 2.602085213965210642E-15 ) ) ;
#83493=ORIENTED_EDGE ( 'NONE', *, *, #68596, .F. ) ;
#83540=CARTESIAN_POINT ( 'NONE',  ( -1.063950011417350128, -4.204658361605618566, -0.1571845235116862138 ) ) ;
#83626=CARTESIAN_POINT ( 'NONE',  ( -0.6823417656250003738, 11.96354166700806765, 1.181850606188754593 ) ) ;
#83689=CARTESIAN_POINT ( 'NONE',  ( -0.6823417656250003738, 9.963541667008065872, 1.181850606188754593 ) ) ;
#83732=CARTESIAN_POINT ( 'NONE',  ( 1.500000000000001332, 9.156250000682799595, 0.000000000000000000 ) ) ;
#83940=CARTESIAN_POINT ( 'NONE',  ( 1.364683531249996529, 14.77604166700806410, 0.7879004041258405033 ) ) ;
#84118=CARTESIAN_POINT ( 'NONE',  ( -1.115562610750309283E-14, 10.31250000000000000, 1.500000000000001554 ) ) ;
#84133=CARTESIAN_POINT ( 'NONE',  ( -1.364683531250010740, 12.63020833367473372, 0.7879004041258445001 ) ) ;
#84138=CARTESIAN_POINT ( 'NONE',  ( 0.7500000000000006661, 11.58333333333333393, 1.299038105676657340 ) ) ;
#84175=ORIENTED_EDGE ( 'NONE', *, *, #66221, .T. ) ;
#84185=CARTESIAN_POINT ( 'NONE',  ( -1.364683531250010740, 9.942708333674728394, 0.7879004041258445001 ) ) ;
#84246=CARTESIAN_POINT ( 'NONE',  ( 1.500000000000001332, 12.37499999999999645, 0.000000000000000000 ) ) ;
#84259=CARTESIAN_POINT ( 'NONE',  ( 1.499999999999997113, 12.67708333401612819, -0.8660254037844378194 ) ) ;
#84297=VERTEX_POINT ( 'NONE', #70654 ) ;
#84332=CARTESIAN_POINT ( 'NONE',  ( 1.407792700327077151, 3.466403870727115422, 0.5229849042009182547 ) ) ;
#84348=CARTESIAN_POINT ( 'NONE',  ( 0.6823417656249969321, 12.77604166700806232, -1.181850606188757036 ) ) ;
#84375=ADVANCED_FACE ( 'NONE', ( #72806 ), #74956, .F. ) ;
#84402=CARTESIAN_POINT ( 'NONE',  ( 1.364683531249997417, 12.48437500034139980, 2.602085213965210642E-15 ) ) ;
#84491=ORIENTED_EDGE ( 'NONE', *, *, #46115, .F. ) ;
#84546=CARTESIAN_POINT ( 'NONE',  ( -8.012344526598182026E-15, 11.04687500034139980, -1.575800808251669460 ) ) ;
#84580=CARTESIAN_POINT ( 'NONE',  ( 1.406843869218815657, 13.32828740661201472, -0.1535876347566223210 ) ) ;
#84664=CARTESIAN_POINT ( 'NONE',  ( 0.000000000000000000, 13.49999999999999822, -1.500000000000000222 ) ) ;
#84700=CARTESIAN_POINT ( 'NONE',  ( -8.012344526598182026E-15, 12.10937500034140157, -1.575800808251669460 ) ) ;
#84766=CARTESIAN_POINT ( 'NONE',  ( -1.364683531250000748, 9.421875000341396245, 0.000000000000000000 ) ) ;
#84806=CARTESIAN_POINT ( 'NONE',  ( -0.6823417656250003738, 15.15104166700806410, 1.181850606188754593 ) ) ;
#84877=EDGE_CURVE ( 'NONE', #96508, #84297, #34893, .T. ) ;
#84943=CARTESIAN_POINT ( 'NONE',  ( 1.364683531250000748, 8.505208333674730170, -0.7879004041258355073 ) ) ;
#85013=CARTESIAN_POINT ( 'NONE',  ( -1.402160292154681736E-14, 13.98437500034139624, 1.575800808251682339 ) ) ;
#85053=ADVANCED_FACE ( 'NONE', ( #114973 ), #164727, .F. ) ;
#85198=CARTESIAN_POINT ( 'NONE',  ( -1.402160292154681736E-14, 11.67187500034139980, 1.575800808251682339 ) ) ;
#85204=CARTESIAN_POINT ( 'NONE',  ( 1.499999999999997113, 9.145833333333330373, -0.8660254037844378194 ) ) ;
#85248=CARTESIAN_POINT ( 'NONE',  ( -0.6823417656250003738, 8.963541667008065872, 1.181850606188754593 ) ) ;
#85303=CARTESIAN_POINT ( 'NONE',  ( -1.500000000000015099, 11.51041666734946567, -0.8660254037844309360 ) ) ;
#85309=CARTESIAN_POINT ( 'NONE',  ( 0.4019237886466816012, 8.676335450315372455, -1.499999999999998668 ) ) ;
#85326=CARTESIAN_POINT ( 'NONE',  ( -0.7500000000000179856, 12.57291666734946389, 1.299038105676658228 ) ) ;
#85398=CARTESIAN_POINT ( 'NONE',  ( 1.355395447572484313, 3.764859155812621871, -0.6425755019599879159 ) ) ;
#85415=CARTESIAN_POINT ( 'NONE',  ( -0.6823417656250039265, 12.81770833367473017, -1.181850606188755259 ) ) ;
#85458=CARTESIAN_POINT ( 'NONE',  ( 1.499999999999997113, 13.64583333333332860, -0.8660254037844378194 ) ) ;
#85464=CARTESIAN_POINT ( 'NONE',  ( 0.6823417656249934904, 11.94270833367473017, 1.181850606188764807 ) ) ;
#85501=LINE ( 'NONE', #102828, #128801 ) ;
#85512=CARTESIAN_POINT ( 'NONE',  ( -1.402160292154681736E-14, 12.98437500034139980, 1.575800808251682339 ) ) ;
#85601=CARTESIAN_POINT ( 'NONE',  ( 0.5998553420608258024, 4.283167794419532548, 0.2583637543479620491 ) ) ;
#85612=CARTESIAN_POINT ( 'NONE',  ( -1.402160292154681736E-14, 12.17187500034140335, 1.575800808251682339 ) ) ;
#85634=ORIENTED_EDGE ( 'NONE', *, *, #201285, .F. ) ;
#85715=CARTESIAN_POINT ( 'NONE',  ( -2.788906526875773208E-15, 11.71875000068279604, -1.499999999999998446 ) ) ;
#85766=CARTESIAN_POINT ( 'NONE',  ( 0.6823417656249934904, 10.50520833367472839, 1.181850606188764807 ) ) ;
#85770=ORIENTED_EDGE ( 'NONE', *, *, #166482, .T. ) ;
#85793=CARTESIAN_POINT ( 'NONE',  ( -8.012344526598182026E-15, 15.29687500034140157, -1.575800808251669460 ) ) ;
#85834=CARTESIAN_POINT ( 'NONE',  ( 0.6823417656249969321, 9.588541667008065872, -1.181850606188757036 ) ) ;
#85841=DIRECTION ( 'NONE',  ( 0.000000000000000000, 0.000000000000000000, -1.000000000000000000 ) ) ;
#85877=CARTESIAN_POINT ( 'NONE',  ( -0.7500000000000179856, 9.072916667349467446, 1.299038105676658228 ) ) ;
#85892=CONICAL_SURFACE ( 'NONE', #206950, 1.540450515248283025, 0.7853981633974428389 ) ;
#85929=EDGE_LOOP ( 'NONE', ( #7781, #724, #134375, #67258 ) ) ;
#85952=CARTESIAN_POINT ( 'NONE',  ( 3.834746474454188013E-15, 10.56250000000000178, 1.500000000000001554 ) ) ;
#86015=CARTESIAN_POINT ( 'NONE',  ( 1.500000000000001332, 12.62499999999999645, 0.000000000000000000 ) ) ;
#86017=CARTESIAN_POINT ( 'NONE',  ( 3.834746474454188013E-15, 12.56250000000000000, 1.500000000000001554 ) ) ;
#86024=CARTESIAN_POINT ( 'NONE',  ( 3.834746474454188013E-15, 10.59375000068279604, 1.500000000000001554 ) ) ;
#86082=CARTESIAN_POINT ( 'NONE',  ( 0.6823417656249934904, 13.25520833367473195, 1.181850606188764807 ) ) ;
#86113=AXIS2_PLACEMENT_3D ( 'NONE', #196503, #114258, #180254 ) ;
#86125=AXIS2_PLACEMENT_3D ( 'NONE', #25030, #91130, #9850 ) ;
#86232=CYLINDRICAL_SURFACE ( 'NONE', #70115, 1.500000000000000222 ) ;
#86269=CARTESIAN_POINT ( 'NONE',  ( 1.364683531249997417, 11.48437500034139802, 2.602085213965210642E-15 ) ) ;
#86275=CARTESIAN_POINT ( 'NONE',  ( 0.7500000000000006661, 10.16666666666667140, -1.299038105676657340 ) ) ;
#86282=CIRCLE ( 'NONE', #155394, 1.249999999999999778 ) ;
#86318=VERTEX_POINT ( 'NONE', #214278 ) ;
#86323=CARTESIAN_POINT ( 'NONE',  ( 0.6823417656249934904, 9.005208333674726617, 1.181850606188764807 ) ) ;
#86330=CARTESIAN_POINT ( 'NONE',  ( -0.4019237886466933696, 10.33258545099817027, 1.500000000000005995 ) ) ;
#86400=CARTESIAN_POINT ( 'NONE',  ( -1.500000000000008216, 11.53125000068279427, 3.469446951953614189E-15 ) ) ;
#86485=CARTESIAN_POINT ( 'NONE',  ( -0.6823417656250003738, 13.40104166700806232, 1.181850606188754593 ) ) ;
#86528=CARTESIAN_POINT ( 'NONE',  ( -6.009258394948636914E-15, 13.43749999999999822, -1.732050807568875195 ) ) ;
#86535=CARTESIAN_POINT ( 'NONE',  ( -1.364683531250014514, 11.33854166700806410, -0.7879004041258335089 ) ) ;
#86548=EDGE_LOOP ( 'NONE', ( #4966, #109113, #116495, #130229, #129193 ) ) ;
#86583=CARTESIAN_POINT ( 'NONE',  ( -1.364683531250014514, 12.90104166700806410, -0.7879004041258335089 ) ) ;
#86666=VERTEX_POINT ( 'NONE', #51390 ) ;
#86672=CARTESIAN_POINT ( 'NONE',  ( 0.6500572981163011965, 4.350074487569242976, 0.06817653764027256647 ) ) ;
#86681=CARTESIAN_POINT ( 'NONE',  ( 0.6823417656249934904, 12.19270833367473017, 1.181850606188764807 ) ) ;
#86713=CARTESIAN_POINT ( 'NONE',  ( 0.3667533499403192732, 13.35836302003387743, -1.335730745167230893 ) ) ;
#86834=CARTESIAN_POINT ( 'NONE',  ( 0.6823417656249969321, 11.33854166700806765, -1.181850606188757036 ) ) ;
#86860=CARTESIAN_POINT ( 'NONE',  ( -1.364683531250010295, 15.13020833367473017, 0.7879004041258445001 ) ) ;
#86864=B_SPLINE_CURVE_WITH_KNOTS ( 'NONE', 3,
 ( #143252, #127045, #208187, #9994, #4896, #92358 ),
 .UNSPECIFIED., .F., .F.,
 ( 4, 2, 4 ),
 ( 0.001616326159039276067, 0.001719602896561277672, 0.001822879634083279061 ),
 .UNSPECIFIED. ) ;
#86903=CARTESIAN_POINT ( 'NONE',  ( -1.364683531250000748, 8.671875000341403350, 0.000000000000000000 ) ) ;
#86909=CARTESIAN_POINT ( 'NONE',  ( -1.378728738066235859, 3.613591550242559070, -0.5908528300941767730 ) ) ;
#86945=CARTESIAN_POINT ( 'NONE',  ( -0.6823417656250039265, 15.31770833367473372, -1.181850606188755259 ) ) ;
#86980=ORIENTED_EDGE ( 'NONE', *, *, #186000, .T. ) ;
#87012=CARTESIAN_POINT ( 'NONE',  ( 0.4019237886466816012, 10.67633545031537246, -1.499999999999998668 ) ) ;
#87038=LINE ( 'NONE', #34018, #166007 ) ;
#87078=CARTESIAN_POINT ( 'NONE',  ( 3.834746474454188013E-15, 12.56250000000000178, 1.500000000000001554 ) ) ;
#87084=CARTESIAN_POINT ( 'NONE',  ( 1.364683531249996529, 14.77604166700806410, 0.7879004041258405033 ) ) ;
#87119=LINE ( 'NONE', #4762, #173911 ) ;
#87135=CARTESIAN_POINT ( 'NONE',  ( -0.7500000000000006661, 8.708333333333332149, -1.299038105676657340 ) ) ;
#87145=CARTESIAN_POINT ( 'NONE',  ( -0.6823417656250039265, 13.38020833367473195, -1.181850606188755259 ) ) ;
#87174=VECTOR ( 'NONE', #72395, 1000.000000000000000 ) ;
#87339=CARTESIAN_POINT ( 'NONE',  ( 1.286813488861813459, 4.086408449757453099, -0.5514626414212294714 ) ) ;
#87341=CARTESIAN_POINT ( 'NONE',  ( -1.402160292154681736E-14, 12.67187500034139802, 1.575800808251682339 ) ) ;
#87348=CARTESIAN_POINT ( 'NONE',  ( -1.500000000000008216, 9.750000000000001776, 3.469446951953614189E-15 ) ) ;
#87378=( BOUNDED_SURFACE ( )  B_SPLINE_SURFACE ( 3, 2, ( 
 ( #112159, #160838, #43905 ),
 ( #95861, #96930, #210641 ),
 ( #46038, #11365, #143561 ),
 ( #177087, #209555, #176033 ),
 ( #178162, #145698, #62268 ),
 ( #93726, #61199, #27626 ),
 ( #48179, #159765, #126285 ),
 ( #211697, #44974, #158703 ),
 ( #29777, #28704, #161917 ),
 ( #60127, #12429, #127358 ),
 ( #13507, #79580, #129493 ),
 ( #94790, #10302, #78509 ),
 ( #144627, #128428, #113222 ),
 ( #179227, #76376, #30852 ),
 ( #142483, #162981, #80657 ),
 ( #146748, #64402, #212766 ),
 ( #130545, #114292, #180290 ),
 ( #208491, #34022, #35075 ) ),
 .UNSPECIFIED., .F., .F., .T. ) 
 B_SPLINE_SURFACE_WITH_KNOTS ( ( 4, 2, 2, 2, 2, 2, 2, 2, 4 ),
 ( 3, 3 ),
 ( 0.001893572594152294905, 0.002130269168421384217, 0.002366965742690473745, 0.002603662316959563273, 0.002840358891228652802, 0.003077055465497742330, 0.003313752039766831858, 0.003550448614035921387, 0.003787145188305010481 ),
 ( 0.000000000000000000, 1.000000000000000000 ),
 .UNSPECIFIED. ) 
 GEOMETRIC_REPRESENTATION_ITEM ( )  RATIONAL_B_SPLINE_SURFACE ( (
 ( 1.000000000000000000, 0.5649783097559792910, 1.000000000000000000),
 ( 1.000000000000000000, 0.5467450299869786035, 1.000000000000000000),
 ( 1.000000000000000000, 0.5350701846666650052, 1.000000000000000000),
 ( 1.000000000000000000, 0.5340147030925761484, 1.000000000000000000),
 ( 1.000000000000000000, 0.5447811154896929908, 1.000000000000000000),
 ( 1.000000000000000000, 0.5795975317819822559, 1.000000000000000000),
 ( 1.000000000000000000, 0.6028840214605843961, 1.000000000000000000),
 ( 1.000000000000000000, 0.6474634991924845817, 1.000000000000000000),
 ( 1.000000000000000000, 0.6683065367293009595, 1.000000000000000000),
 ( 1.000000000000000000, 0.6980320384850667859, 1.000000000000000000),
 ( 1.000000000000000000, 0.7066998895408396208, 1.000000000000000000),
 ( 1.000000000000000000, 0.7074845257686435129, 1.000000000000000000),
 ( 1.000000000000000000, 0.6995439292593913505, 1.000000000000000000),
 ( 1.000000000000000000, 0.6710262760327935228, 1.000000000000000000),
 ( 1.000000000000000000, 0.6504357685074171336, 1.000000000000000000),
 ( 1.000000000000000000, 0.6062099919889232247, 1.000000000000000000),
 ( 1.000000000000000000, 0.5828135443829657314, 1.000000000000000000),
 ( 1.000000000000000000, 0.5647844906712728985, 1.000000000000000000) ) ) 
 REPRESENTATION_ITEM ( '' )  SURFACE ( )  );
#87382=ORIENTED_EDGE ( 'NONE', *, *, #78658, .F. ) ;
#87399=CARTESIAN_POINT ( 'NONE',  ( 1.364683531249996529, 9.526041667008062319, 0.7879004041258403923 ) ) ;
#87469=CARTESIAN_POINT ( 'NONE',  ( 0.000000000000000000, 13.49999999999999822, 0.000000000000000000 ) ) ;
#87470=AXIS2_PLACEMENT_3D ( 'NONE', #106068, #73506, #123431 ) ;
#87559=CARTESIAN_POINT ( 'NONE',  ( -0.6823417656250003738, 12.90104166700806232, 1.181850606188754593 ) ) ;
#87580=CARTESIAN_POINT ( 'NONE',  ( 1.350829346764933936, 3.446353025980462892, -0.3155766437963711257 ) ) ;
#87604=CARTESIAN_POINT ( 'NONE',  ( -6.009258394948636914E-15, 13.93750000000000178, -1.732050807568875195 ) ) ;
#87609=CARTESIAN_POINT ( 'NONE',  ( 1.364683531250000303, 12.00520833367473195, -0.7879004041258355073 ) ) ;
#87652=CARTESIAN_POINT ( 'NONE',  ( -0.5368768833858145184, 13.37576698399828246, -1.254641125003840507 ) ) ;
#87692=ORIENTED_EDGE ( 'NONE', *, *, #122759, .F. ) ;
#87716=CARTESIAN_POINT ( 'NONE',  ( 1.499999999999993117, 14.88541666734946567, 0.8660254037844409281 ) ) ;
#87718=ORIENTED_EDGE ( 'NONE', *, *, #167500, .T. ) ;
#87723=DIRECTION ( 'NONE',  ( 0.000000000000000000, 0.000000000000000000, -1.000000000000000000 ) ) ;
#87748=CARTESIAN_POINT ( 'NONE',  ( 1.364683531249997417, 10.73437500034139802, 2.602085213965210642E-15 ) ) ;
#87783=EDGE_CURVE ( 'NONE', #79633, #120384, #65828, .T. ) ;
#87902=CARTESIAN_POINT ( 'NONE',  ( 0.6823417656249969321, 11.08854166700806765, -1.181850606188757036 ) ) ;
#87917=ORIENTED_EDGE ( 'NONE', *, *, #135584, .F. ) ;
#87925=CARTESIAN_POINT ( 'NONE',  ( -1.364683531250010295, 14.88020833367472839, 0.7879004041258445001 ) ) ;
#87968=CARTESIAN_POINT ( 'NONE',  ( 1.364683531249996529, 9.026041667008060543, 0.7879004041258405033 ) ) ;
#88014=CARTESIAN_POINT ( 'NONE',  ( -0.7500000000000006661, 8.739583334016129967, -1.299038105676657340 ) ) ;
#88049=CARTESIAN_POINT ( 'NONE',  ( 0.000000000000000000, -4.500000000000003553, 0.000000000000000000 ) ) ;
#88158=CARTESIAN_POINT ( 'NONE',  ( -8.012344526598182026E-15, 14.85937500034139980, -1.575800808251669460 ) ) ;
#88196=ORIENTED_EDGE ( 'NONE', *, *, #141409, .F. ) ;
#88220=CARTESIAN_POINT ( 'NONE',  ( 1.364683531249996529, 13.02604166700806410, 0.7879004041258405033 ) ) ;
#88358=DIRECTION ( 'NONE',  ( 0.000000000000000000, -1.000000000000000000, 0.000000000000000000 ) ) ;
#88395=CARTESIAN_POINT ( 'NONE',  ( 1.350866880800080105, 4.253815248464132281, 0.3155278943301796923 ) ) ;
#88414=CARTESIAN_POINT ( 'NONE',  ( -8.012344526598182026E-15, 12.04687500034140335, -1.575800808251669460 ) ) ;
#88422=CARTESIAN_POINT ( 'NONE',  ( -1.402160292154681736E-14, 9.812499999999998224, 1.732050807568881190 ) ) ;
#88446=CARTESIAN_POINT ( 'NONE',  ( -0.7500000000000006661, 8.489583334016129967, -1.299038105676657340 ) ) ;
#88476=CARTESIAN_POINT ( 'NONE',  ( -1.364683531250000748, 8.671875000341403350, 0.000000000000000000 ) ) ;
#88481=CARTESIAN_POINT ( 'NONE',  ( -1.500000000000008216, 10.28125000068279249, 3.469446951953614189E-15 ) ) ;
#88490=CARTESIAN_POINT ( 'NONE',  ( -3.602337597214539753E-15, 12.59375000068279782, 1.500000000000001554 ) ) ;
#88536=CARTESIAN_POINT ( 'NONE',  ( -0.4019237886466802689, 9.729914550367427140, -1.500000000000002887 ) ) ;
#88548=ORIENTED_EDGE ( 'NONE', *, *, #196068, .T. ) ;
#88557=LINE ( 'NONE', #154617, #119874 ) ;
#88681=CARTESIAN_POINT ( 'NONE',  ( -1.500000000000008216, 13.99999999999999822, 3.469446951953614189E-15 ) ) ;
#88686=CARTESIAN_POINT ( 'NONE',  ( -8.012344526598182026E-15, 10.54687500034139624, -1.575800808251669460 ) ) ;
#88734=CARTESIAN_POINT ( 'NONE',  ( -1.364683531250000748, 12.67187500034139980, 0.000000000000000000 ) ) ;
#88739=CARTESIAN_POINT ( 'NONE',  ( -0.7500000000000179856, 12.32291666734946389, 1.299038105676658228 ) ) ;
#88799=CARTESIAN_POINT ( 'NONE',  ( -1.500000000000008216, 15.28125000068279782, 3.469446951953614189E-15 ) ) ;
#88836=CARTESIAN_POINT ( 'NONE',  ( -1.364683531250010295, 10.13020833367472839, 0.7879004041258445001 ) ) ;
#88838=CARTESIAN_POINT ( 'NONE',  ( -0.7500000000000006661, 13.23958333401613352, -1.299038105676657340 ) ) ;
#88843=CARTESIAN_POINT ( 'NONE',  ( -2.788906526875773208E-15, 8.968750000682797818, -1.499999999999998446 ) ) ;
#88961=FACE_OUTER_BOUND ( 'NONE', #90755, .T. ) ;
#88962=CARTESIAN_POINT ( 'NONE',  ( 3.834746474454188013E-15, 10.34375000068279782, 1.500000000000001554 ) ) ;
#88986=CARTESIAN_POINT ( 'NONE',  ( -1.364683531250000748, 11.67187500034139802, 0.000000000000000000 ) ) ;
#88998=CARTESIAN_POINT ( 'NONE',  ( -0.7500000000000179856, 10.79166666666666430, 1.299038105676658228 ) ) ;
#89008=CARTESIAN_POINT ( 'NONE',  ( 0.4153311931459124917, 3.780327751615584653, 0.5000000000000073275 ) ) ;
#89012=CARTESIAN_POINT ( 'NONE',  ( 1.364683531249997417, 14.98437500034140157, 2.602085213965210642E-15 ) ) ;
#89055=CARTESIAN_POINT ( 'NONE',  ( -8.012344526598182026E-15, 9.609375000341399797, -1.575800808251669460 ) ) ;
#89061=CARTESIAN_POINT ( 'NONE',  ( -1.456019627564700158, 4.349501266769085994, -0.3924612876561416885 ) ) ;
#89102=CARTESIAN_POINT ( 'NONE',  ( 0.6823417656249934904, 14.19270833367473195, 1.181850606188764807 ) ) ;
#89242=CARTESIAN_POINT ( 'NONE',  ( -1.402160292154681736E-14, 15.23437500034140157, 1.575800808251682339 ) ) ;
#89250=CARTESIAN_POINT ( 'NONE',  ( 1.499999999999996891, 12.42708333401612819, -0.8660254037844378194 ) ) ;
#89302=CARTESIAN_POINT ( 'NONE',  ( 1.364683531249996529, 12.77604166700806587, 0.7879004041258405033 ) ) ;
#89328=ADVANCED_FACE ( 'NONE', ( #143921 ), #173201, .T. ) ;
#89337=AXIS2_PLACEMENT_3D ( 'NONE', #106093, #205656, #90876 ) ;
#89474=CARTESIAN_POINT ( 'NONE',  ( 1.396252044512854118, 4.345153108015988863, -0.1338139928737633322 ) ) ;
#89495=CARTESIAN_POINT ( 'NONE',  ( 1.364683531249997417, 10.98437500034139802, 2.602085213965210642E-15 ) ) ;
#89500=CARTESIAN_POINT ( 'NONE',  ( 1.500000000000001332, 9.625000000000001776, 0.000000000000000000 ) ) ;
#89513=ORIENTED_EDGE ( 'NONE', *, *, #62276, .T. ) ;
#89515=ORIENTED_EDGE ( 'NONE', *, *, #116111, .F. ) ;
#89760=CARTESIAN_POINT ( 'NONE',  ( 1.499999999999997113, 13.14583333333333393, -0.8660254037844378194 ) ) ;
#89768=CARTESIAN_POINT ( 'NONE',  ( 1.364683531250000303, 10.75520833367473195, -0.7879004041258355073 ) ) ;
#89836=CARTESIAN_POINT ( 'NONE',  ( -0.6823417656250003738, 12.90104166700806232, 1.181850606188754593 ) ) ;
#89859=CYLINDRICAL_SURFACE ( 'NONE', #178227, 1.500000000000000222 ) ;
#89860=ADVANCED_FACE ( 'NONE', ( #129842 ), #31202, .T. ) ;
#89862=CARTESIAN_POINT ( 'NONE',  ( -5.000000000000009770, 3.850000000000006306, -0.4999999999999942824 ) ) ;
#89907=CARTESIAN_POINT ( 'NONE',  ( 1.364683531250000303, 10.50520833367473195, -0.7879004041258355073 ) ) ;
#89987=CARTESIAN_POINT ( 'NONE',  ( 0.000000000000000000, -0.5000000000000004441, 0.000000000000000000 ) ) ;
#90010=CARTESIAN_POINT ( 'NONE',  ( -1.346456596051761601, 3.462271664236989288, -0.3357819570988693214 ) ) ;
#90053=CARTESIAN_POINT ( 'NONE',  ( -0.6823417656250003738, 9.713541667008065872, 1.181850606188754593 ) ) ;
#90076=CARTESIAN_POINT ( 'NONE',  ( 0.6823417656249934904, 14.69270833367473195, 1.181850606188764807 ) ) ;
#90098=DIRECTION ( 'NONE',  ( -0.1664974550714433121, -0.9062754367152189294, 0.3885143887443193722 ) ) ;
#90111=CARTESIAN_POINT ( 'NONE',  ( 3.834746474454188013E-15, 13.09375000068279959, 1.500000000000001554 ) ) ;
#90119=CARTESIAN_POINT ( 'NONE',  ( -6.009258394948636914E-15, 14.43750000000000355, -1.732050807568875195 ) ) ;
#90135=LINE ( 'NONE', #157267, #46825 ) ;
#90166=CARTESIAN_POINT ( 'NONE',  ( 1.364683531250000303, 13.75520833367473195, -0.7879004041258355073 ) ) ;
#90295=EDGE_CURVE ( 'NONE', #65269, #180121, #139062, .T. ) ;
#90299=CARTESIAN_POINT ( 'NONE',  ( -0.6823417656250003738, 14.96354166700806410, 1.181850606188754593 ) ) ;
#90344=ORIENTED_EDGE ( 'NONE', *, *, #41132, .T. ) ;
#90364=DIRECTION ( 'NONE',  ( 0.000000000000000000, -1.000000000000000000, 0.000000000000000000 ) ) ;
#90365=CARTESIAN_POINT ( 'NONE',  ( -1.364683531250014514, 13.15104166700806410, -0.7879004041258335089 ) ) ;
#90405=CARTESIAN_POINT ( 'NONE',  ( 0.7500000000000006661, 11.44791666734946212, -1.299038105676657340 ) ) ;
#90559=CARTESIAN_POINT ( 'NONE',  ( -1.364683531250010740, 10.63020833367473195, 0.7879004041258445001 ) ) ;
#90567=CARTESIAN_POINT ( 'NONE',  ( -1.402160292154681736E-14, 8.562500000000001776, 1.732050807568881190 ) ) ;
#90614=ORIENTED_EDGE ( 'NONE', *, *, #153040, .F. ) ;
#90620=CARTESIAN_POINT ( 'NONE',  ( 1.364683531250000748, 8.567708333674730170, -0.7879004041258355073 ) ) ;
#90677=CARTESIAN_POINT ( 'NONE',  ( -0.7500000000000006661, 9.739583334016129967, -1.299038105676657340 ) ) ;
#90678=EDGE_CURVE ( 'NONE', #180121, #133382, #94789, .T. ) ;
#90755=EDGE_LOOP ( 'NONE', ( #114514, #13203 ) ) ;
#90820=CARTESIAN_POINT ( 'NONE',  ( -6.009258394948636914E-15, 12.93749999999999822, -1.732050807568875195 ) ) ;
#90826=CARTESIAN_POINT ( 'NONE',  ( 0.6823417656249934904, 11.19270833367473550, 1.181850606188764807 ) ) ;
#90866=CARTESIAN_POINT ( 'NONE',  ( -0.4019237886466871523, 11.97991455036742714, -1.499999999999998668 ) ) ;
#90871=CARTESIAN_POINT ( 'NONE',  ( -1.364683531250010740, 11.44270833367472839, 0.7879004041258445001 ) ) ;
#90876=DIRECTION ( 'NONE',  ( 0.000000000000000000, 0.000000000000000000, -1.000000000000000000 ) ) ;
#90880=ADVANCED_FACE ( 'NONE', ( #125020 ), #32493, .T. ) ;
#90898=CARTESIAN_POINT ( 'NONE',  ( 1.364683531250000748, 12.75520833367473372, -0.7879004041258355073 ) ) ;
#90944=DIRECTION ( 'NONE',  ( 0.000000000000000000, -1.000000000000000000, 0.000000000000000000 ) ) ;
#90972=CARTESIAN_POINT ( 'NONE',  ( -1.364683531250014514, 10.83854166700806942, -0.7879004041258335089 ) ) ;
#91018=CARTESIAN_POINT ( 'NONE',  ( -0.7500000000000179856, 11.82291666734946389, 1.299038105676658228 ) ) ;
#91043=VERTEX_POINT ( 'NONE', #76177 ) ;
#91121=CARTESIAN_POINT ( 'NONE',  ( 0.6823417656249969321, 10.08854166700806587, -1.181850606188757036 ) ) ;
#91130=DIRECTION ( 'NONE',  ( 0.000000000000000000, -1.000000000000000000, 0.000000000000000000 ) ) ;
#91148=CARTESIAN_POINT ( 'NONE',  ( 1.364683531249997417, 14.73437500034140157, 2.602085213965210642E-15 ) ) ;
#91167=CARTESIAN_POINT ( 'NONE',  ( 0.4019237886466816012, 9.957585450998168497, -1.499999999999998668 ) ) ;
#91180=CARTESIAN_POINT ( 'NONE',  ( -1.115562610750309283E-14, 11.59375000068279604, 1.500000000000001554 ) ) ;
#91189=CARTESIAN_POINT ( 'NONE',  ( 1.499999999999993117, 15.35416666666666430, 0.8660254037844409281 ) ) ;
#91209=ORIENTED_EDGE ( 'NONE', *, *, #129599, .F. ) ;
#91236=CARTESIAN_POINT ( 'NONE',  ( -0.6823417656250039265, 14.56770833367473195, -1.181850606188755259 ) ) ;
#91247=DIRECTION ( 'NONE',  ( 0.000000000000000000, -1.000000000000000000, 0.000000000000000000 ) ) ;
#91269=FILL_AREA_STYLE_COLOUR ( '', #183331 ) ;
#91360=CIRCLE ( 'NONE', #115648, 0.09999999999999990841 ) ;
#91382=CARTESIAN_POINT ( 'NONE',  ( -1.402160292154681736E-14, 13.73437500034139624, 1.575800808251682339 ) ) ;
#91420=ORIENTED_EDGE ( 'NONE', *, *, #178139, .F. ) ;
#91443=CARTESIAN_POINT ( 'NONE',  ( -1.402160292154681736E-14, 12.23437500034140335, 1.575800808251682339 ) ) ;
#91462=EDGE_CURVE ( 'NONE', #8253, #112831, #99182, .T. ) ;
#91485=CARTESIAN_POINT ( 'NONE',  ( 1.499999999999993117, 10.63541666734946212, 0.8660254037844409281 ) ) ;
#91487=EDGE_LOOP ( 'NONE', ( #102868, #1073, #63778, #108205, #100446 ) ) ;
#91616=CARTESIAN_POINT ( 'NONE',  ( 0.7500000000000006661, 8.947916667349467446, -1.299038105676657340 ) ) ;
#91636=CARTESIAN_POINT ( 'NONE',  ( 0.6823417656249969321, 10.27604166700806587, -1.181850606188757036 ) ) ;
#91647=( BOUNDED_CURVE ( )  B_SPLINE_CURVE ( 2, ( #97989, #198635, #164048, #50283, #182390, #133700, #34020, #106546, #201827 ),
 .UNSPECIFIED., .F., .T. ) 
 B_SPLINE_CURVE_WITH_KNOTS ( ( 3, 2, 2, 2, 3 ),
 ( 0.8839285714285713969, 0.8869047619047618625, 0.8928571428571429047, 0.8988095238095238360, 0.9017857142857143016 ),
 .UNSPECIFIED. ) 
 CURVE ( )  GEOMETRIC_REPRESENTATION_ITEM ( )  RATIONAL_B_SPLINE_CURVE ( ( 0.9330127018922194093, 0.9330127018922194093, 1.000000000000000000, 0.8660254037844387076, 1.000000000000000000, 0.8660254037844387076, 1.000000000000000000, 0.9330127018922194093, 0.9330127018922194093 ) ) 
 REPRESENTATION_ITEM ( '' )  );
#91704=ORIENTED_EDGE ( 'NONE', *, *, #56238, .F. ) ;
#91708=CARTESIAN_POINT ( 'NONE',  ( -8.012344526598182026E-15, 15.35937500034140513, -1.575800808251669460 ) ) ;
#91752=LINE ( 'NONE', #188146, #201722 ) ;
#91867=CARTESIAN_POINT ( 'NONE',  ( 0.000000000000000000, -1.500000000000001332, 1.249999999999999778 ) ) ;
#91898=CARTESIAN_POINT ( 'NONE',  ( 1.500000000000001332, 12.87499999999999822, 0.000000000000000000 ) ) ;
#91903=CARTESIAN_POINT ( 'NONE',  ( -1.364683531250014514, 10.58854166700806765, -0.7879004041258335089 ) ) ;
#91910=EDGE_CURVE ( 'NONE', #5587, #67094, #148352, .T. ) ;
#91915=CARTESIAN_POINT ( 'NONE',  ( -1.500000000000001110, 10.80208333401613707, 0.8660254037844418162 ) ) ;
#91941=CARTESIAN_POINT ( 'NONE',  ( 1.364683531250000748, 11.81770833367472839, -0.7879004041258355073 ) ) ;
#91968=EDGE_CURVE ( 'NONE', #171094, #70036, #202899, .T. ) ;
#92011=CARTESIAN_POINT ( 'NONE',  ( 0.7500000000000006661, 14.69791666734946567, -1.299038105676657340 ) ) ;
#92045=CARTESIAN_POINT ( 'NONE',  ( 1.364683531250000303, 10.00520833367473017, -0.7879004041258355073 ) ) ;
#92203=CARTESIAN_POINT ( 'NONE',  ( -0.6823417656250003738, 10.21354166700806587, 1.181850606188754593 ) ) ;
#92244=CARTESIAN_POINT ( 'NONE',  ( 1.499999999999993117, 10.35416666666666430, 0.8660254037844408170 ) ) ;
#92272=CARTESIAN_POINT ( 'NONE',  ( -1.500000000000001110, 15.27083333333333570, 0.8660254037844419273 ) ) ;
#92316=( BOUNDED_SURFACE ( )  B_SPLINE_SURFACE ( 1, 2, ( 
 ( #142595, #143676, #77553, #91708, #92771, #211807, #46150, #178277, #157759, #13616, #124270, #208604, #190228, #107998, #9356, #75430, #207549, #60235, #182498, #115454, #101258, #50388, #196644, #35181, #64508, #181444, #17855, #150030, #116509, #195584, #179342, #83940, #48283, #1600, #131688, #130652, #81821, #99151, #165202, #65542, #16794, #197690, #51460, #98098, #114396, #34129, #67660, #180392, #133805, #32015, #146855, #97039, #164149, #80766, #212875, #33073, #167341, #15735, #132738, #117582, #147903, #213920, #49336, #63445, #47219, #82877, #148955, #525, #113335, #85013, #66594, #198741, #100199, #166265, #183575, #199816, #18927, #30964, #151103, #129597, #163091, #14672, #119714, #4787, #105560, #69801, #168402, #155351, #201927, #169463, #200869, #52513, #37328, #122952, #73017, #2667, #204061, #185696, #87145, #152158, #19998, #102328, #3728, #106655, #86082, #55713, #6936, #138047, #22108, #90365, #68740, #120796, #135909, #38399, #21048, #88220, #186773, #184632, #53581, #24259, #71937, #154290, #118647, #5865, #188912, #103402, #39464, #89302, #36248, #104479, #134862, #153217, #121866, #54647, #40551, #187837, #70865, #172682, #136980, #170525, #171593, #139114, #23187, #203007, #205142, #56784, #141286, #176942, #9100, #193181, #92521, #28557, #174831, #91443, #209407, #158560, #208352, #93580, #156432, #107743, #10158, #44830, #26410, #173767, #175889, #157504, #144484, #94646, #76234, #74108, #127213, #58919, #124010, #59983, #125078, #142343, #110936, #75176, #25344, #160690, #207295, #108808, #140201, #206223, #191034, #62126, #12283, #8017, #143413, #42701, #126136, #192098, #43764, #41629, #109877, #45892, #27480, #61054, #78364, #77301, #159625, #29631, #57849, #11219, #210491, #128287, #194249, #112013, #178014, #189977, #14415, #117330, #164949, #115201, #145553, #32821, #67414, #64260, #132494, #182252, #79436, #65291, #161770, #162837, #278, #147651, #133555, #82623, #80504, #199564, #96787, #213667, #50139, #33876, #148708, #13362, #211552, #116261, #146601, #99954, #212619, #198494, #31769, #166019, #114150, #30704, #66350, #97839, #131438, #98896, #95717, #46960, #163904, #17605, #15480, #130405, #180143, #197442, #49083, #81565, #181194, #16542, #83689, #196393, #48036, #149777, #1353, #51208, #183328, #63185, #179082, #129350, #195329, #113078, #184385, #152970, #72772, #19753, #104229, #89055, #85834, #53332, #36004, #34934, #18684, #103154, #102085, #168154, #84766, #56540, #151912, #201687, #150852, #2416, #69554, #155112, #105307, #101006, #21860, #3485, #119465, #135664, #52272, #134620, #185453, #138871, #200623, #87968, #39216, #170275, #54408, #122702, #167095, #4544, #118399, #70617, #37075, #120548, #136731, #68493, #169215, #20806, #154042, #186526, #86903, #38156, #6696, #202755, #71690, #121622, #5607, #137803, #203822, #55466, #187591, #171345, #204889 ),
 ( #22939, #205973, #123765, #60800, #41379, #126958, #107489, #91189, #190784, #142089, #9910, #92272, #73852, #175638, #57605, #25089, #158319, #58670, #192918, #143166, #124819, #208104, #75985, #59732, #125890, #209161, #189726, #191849, #43511, #173515, #42447, #157250, #109632, #108551, #8843, #174582, #27224, #93329, #159365, #10965, #26158, #44574, #188665, #77039, #40295, #74921, #106406, #141033, #207040, #172429, #24017, #90119, #156186, #7763, #139947, #153674, #41003, #22575, #3111, #205600, #123398, #39927, #36700, #104935, #189362, #170976, #5242, #57238, #69182, #139573, #135303, #201316, #88681, #138497, #188287, #87604, #167782, #19378, #71318, #55103, #119094, #121252, #4180, #20446, #106036, #21493, #172058, #137431, #6323, #85458, #203449, #151544, #154740, #52956, #185074, #102785, #23652, #168843, #72397, #86528, #204519, #187223, #152594, #70251, #136364, #202384, #54034, #120171, #56166, #38851, #186148, #122330, #37782, #89760, #155809, #7393, #103856, #169906, #73472, #94028, #110321, #44200, #43149, #90820, #76676, #74556, #91898, #108188, #142790, #29004, #176327, #42075, #24718, #25787, #190417, #27934, #140657, #207739, #78800, #173136, #161139, #160066, #144924, #194691, #11670, #12727, #77744, #143865, #107113, #156883, #109262, #8470, #60426, #209858, #208796, #141731, #177390, #62556, #206671, #126586, #59364, #191481, #174214, #61496, #157954, #9546, #210930, #75622, #128720, #125520, #175270, #10599, #127663, #193625, #192547, #124458, #45267, #26855, #92960, #111388, #159006, #58303, #95091, #32196, #99338, #49510, #181625, #197880, #84138, #113519, #16982, #83061, #14855, #98272, #179528, #149137, #164330, #213059, #15920, #719, #196826, #30070, #82003, #13797, #31147, #47407, #148091, #182695, #115630, #195768, #178461, #97221, #129787, #33254, #79871, #147037, #18052, #112448, #100390, #165387, #150226, #134001, #66783, #166460, #132923, #198928, #46333, #96160, #48468, #162212, #214096, #50574, #65723, #80945, #116696, #1796, #145981, #131871, #64689, #130834, #163274, #34314, #114583, #180574, #67853, #211992, #63633, #36450, #152345, #103598, #186965, #203201, #71061, #2859, #72137, #135049, #86275, #137177, #185889, #155555, #105769, #37523, #38597, #54848, #120998, #104675, #23389, #52704, #170723, #22309, #168587, #169656, #118834, #88422, #21241, #3923, #87348, #154488, #6067, #138245, #204259, #119913, #89500, #7135, #153414, #4985, #151288, #55910, #102525, #184820, #122068, #53780, #188031, #39661, #171795, #73207, #200007, #51657, #117779, #35381, #183771, #101455, #167527, #68929, #19125, #85204, #201062, #20187, #69993, #136105, #202120, #189111, #106850, #190169, #192287, #59104, #12478, #126328, #41823, #10343, #92702, #207485, #24453, #107936, #75365, #43947, #142527, #76417, #110063, #173961, #9292, #74302, #156628, #90567, #140398, #28748, #8217 ) ),
 .UNSPECIFIED., .F., .F., .T. ) 
 B_SPLINE_SURFACE_WITH_KNOTS ( ( 2, 2 ),
 ( 3, 2, 2, 2, 2, 2, 2, 2, 2, 2, 2, 2, 2, 2, 2, 2, 2, 2, 2, 2, 2, 2, 2, 2, 2, 2, 2, 2, 2, 2, 2, 2, 2, 2, 2, 2, 2, 2, 2, 2, 2, 2, 2, 2, 2, 2, 2, 2, 2, 2, 2, 2, 2, 2, 2, 2, 2, 2, 2, 2, 2, 2, 2, 2, 2, 2, 2, 2, 2, 2, 2, 2, 2, 2, 2, 2, 2, 2, 2, 2, 2, 2, 2, 2, 2, 2, 2, 2, 2, 2, 2, 2, 2, 2, 2, 2, 2, 2, 2, 2, 2, 2, 2, 2, 2, 2, 2, 2, 2, 2, 2, 2, 2, 2, 2, 2, 2, 2, 2, 2, 2, 2, 2, 2, 2, 2, 2, 2, 2, 2, 2, 2, 2, 2, 2, 2, 2, 2, 2, 2, 2, 2, 2, 2, 2, 2, 2, 2, 2, 2, 2, 2, 2, 2, 2, 2, 2, 2, 2, 2, 2, 2, 2, 2, 2, 2, 2, 2, 3 ),
 ( 0.000000000000000000, 1.000000000000000000 ),
 ( 0.000000000000000000, 0.005952380952380952051, 0.01190476190476190410, 0.01785714285714285615, 0.02380952380952380820, 0.02976190476190476025, 0.03571428571428571230, 0.04166666666666666435, 0.04761904761904761640, 0.05357142857142856845, 0.05952380952380952051, 0.06547619047619047949, 0.07142857142857142461, 0.07738095238095238360, 0.08333333333333332871, 0.08928571428571428770, 0.09523809523809523281, 0.1011904761904761918, 0.1071428571428571369, 0.1130952380952380959, 0.1190476190476190410, 0.1250000000000000000, 0.1309523809523809590, 0.1369047619047619180, 0.1428571428571428492, 0.1488095238095238082, 0.1547619047619047672, 0.1607142857142857262, 0.1666666666666666574, 0.1726190476190476164, 0.1785714285714285754, 0.1845238095238095344, 0.1904761904761904656, 0.1964285714285714246, 0.2023809523809523836, 0.2083333333333333426, 0.2142857142857142738, 0.2202380952380952328, 0.2261904761904761918, 0.2321428571428571508, 0.2380952380952380820, 0.2440476190476190410, 0.2500000000000000000, 0.2559523809523809312, 0.2619047619047619180, 0.2678571428571428492, 0.2738095238095238360, 0.2797619047619047672, 0.2857142857142856984, 0.2916666666666666852, 0.2976190476190476164, 0.3035714285714285476, 0.3095238095238095344, 0.3154761904761904656, 0.3214285714285714524, 0.3273809523809523836, 0.3333333333333333148, 0.3392857142857143016, 0.3452380952380952328, 0.3511904761904761640, 0.3571428571428571508, 0.3630952380952380820, 0.3690476190476190688, 0.3750000000000000000, 0.3809523809523809312, 0.3869047619047619180, 0.3928571428571428492, 0.3988095238095238360, 0.4047619047619047672, 0.4107142857142856984, 0.4166666666666666852, 0.4226190476190476164, 0.4285714285714285476, 0.4345238095238095344, 0.4404761904761904656, 0.4464285714285714524, 0.4523809523809523836, 0.4583333333333333148, 0.4642857142857143016, 0.4702380952380952328, 0.4761904761904761640, 0.4821428571428571508, 0.4880952380952380820, 0.4940476190476190688, 0.5000000000000000000, 0.5059523809523809312, 0.5119047619047618625, 0.5178571428571429047, 0.5238095238095238360, 0.5297619047619047672, 0.5357142857142856984, 0.5416666666666666297, 0.5476190476190476719, 0.5535714285714286031, 0.5595238095238095344, 0.5654761904761904656, 0.5714285714285713969, 0.5773809523809523281, 0.5833333333333333703, 0.5892857142857143016, 0.5952380952380952328, 0.6011904761904761640, 0.6071428571428570953, 0.6130952380952381375, 0.6190476190476190688, 0.6250000000000000000, 0.6309523809523809312, 0.6369047619047618625, 0.6428571428571429047, 0.6488095238095238360, 0.6547619047619047672, 0.6607142857142856984, 0.6666666666666666297, 0.6726190476190476719, 0.6785714285714286031, 0.6845238095238095344, 0.6904761904761904656, 0.6964285714285713969, 0.7023809523809523281, 0.7083333333333333703, 0.7142857142857143016, 0.7202380952380952328, 0.7261904761904761640, 0.7321428571428570953, 0.7380952380952381375, 0.7440476190476190688, 0.7500000000000000000, 0.7559523809523809312, 0.7619047619047618625, 0.7678571428571429047, 0.7738095238095238360, 0.7797619047619047672, 0.7857142857142856984, 0.7916666666666666297, 0.7976190476190476719, 0.8035714285714286031, 0.8095238095238095344, 0.8154761904761904656, 0.8214285714285713969, 0.8273809523809523281, 0.8333333333333333703, 0.8392857142857143016, 0.8452380952380952328, 0.8511904761904761640, 0.8571428571428570953, 0.8630952380952381375, 0.8690476190476190688, 0.8750000000000000000, 0.8809523809523809312, 0.8869047619047618625, 0.8928571428571429047, 0.8988095238095238360, 0.9047619047619047672, 0.9107142857142856984, 0.9166666666666666297, 0.9226190476190476719, 0.9285714285714286031, 0.9345238095238095344, 0.9404761904761904656, 0.9464285714285713969, 0.9523809523809523281, 0.9583333333333333703, 0.9642857142857143016, 0.9702380952380952328, 0.9761904761904761640, 0.9821428571428570953, 0.9880952380952381375, 0.9940476190476190688, 1.000000000000000000 ),
 .UNSPECIFIED. ) 
 GEOMETRIC_REPRESENTATION_ITEM ( )  RATIONAL_B_SPLINE_SURFACE ( (
 ( 1.000000000000000000, 0.8660254037844387076, 1.000000000000000000, 0.8660254037844387076, 1.000000000000000000, 0.8660254037844387076, 1.000000000000000000, 0.8660254037844387076, 1.000000000000000000, 0.8660254037844387076, 1.000000000000000000, 0.8660254037844387076, 1.000000000000000000, 0.8660254037844387076, 1.000000000000000000, 0.8660254037844387076, 1.000000000000000000, 0.8660254037844387076, 1.000000000000000000, 0.8660254037844387076, 1.000000000000000000, 0.8660254037844387076, 1.000000000000000000, 0.8660254037844387076, 1.000000000000000000, 0.8660254037844387076, 1.000000000000000000, 0.8660254037844387076, 1.000000000000000000, 0.8660254037844387076, 1.000000000000000000, 0.8660254037844387076, 1.000000000000000000, 0.8660254037844387076, 1.000000000000000000, 0.8660254037844387076, 1.000000000000000000, 0.8660254037844387076, 1.000000000000000000, 0.8660254037844387076, 1.000000000000000000, 0.8660254037844387076, 1.000000000000000000, 0.8660254037844387076, 1.000000000000000000, 0.8660254037844387076, 1.000000000000000000, 0.8660254037844387076, 1.000000000000000000, 0.8660254037844387076, 1.000000000000000000, 0.8660254037844387076, 1.000000000000000000, 0.8660254037844387076, 1.000000000000000000, 0.8660254037844387076, 1.000000000000000000, 0.8660254037844387076, 1.000000000000000000, 0.8660254037844387076, 1.000000000000000000, 0.8660254037844387076, 1.000000000000000000, 0.8660254037844387076, 1.000000000000000000, 0.8660254037844387076, 1.000000000000000000, 0.8660254037844387076, 1.000000000000000000, 0.8660254037844387076, 1.000000000000000000, 0.8660254037844387076, 1.000000000000000000, 0.8660254037844387076, 1.000000000000000000, 0.8660254037844387076, 1.000000000000000000, 0.8660254037844387076, 1.000000000000000000, 0.8660254037844387076, 1.000000000000000000, 0.8660254037844387076, 1.000000000000000000, 0.8660254037844387076, 1.000000000000000000, 0.8660254037844387076, 1.000000000000000000, 0.8660254037844387076, 1.000000000000000000, 0.8660254037844387076, 1.000000000000000000, 0.8660254037844387076, 1.000000000000000000, 0.8660254037844387076, 1.000000000000000000, 0.8660254037844387076, 1.000000000000000000, 0.8660254037844387076, 1.000000000000000000, 0.8660254037844387076, 1.000000000000000000, 0.8660254037844387076, 1.000000000000000000, 0.8660254037844387076, 1.000000000000000000, 0.8660254037844387076, 1.000000000000000000, 0.8660254037844387076, 1.000000000000000000, 0.8660254037844387076, 1.000000000000000000, 0.8660254037844387076, 1.000000000000000000, 0.8660254037844387076, 1.000000000000000000, 0.8660254037844387076, 1.000000000000000000, 0.8660254037844387076, 1.000000000000000000, 0.8660254037844387076, 1.000000000000000000, 0.8660254037844387076, 1.000000000000000000, 0.8660254037844387076, 1.000000000000000000, 0.8660254037844387076, 1.000000000000000000, 0.8660254037844387076, 1.000000000000000000, 0.8660254037844387076, 1.000000000000000000, 0.8660254037844387076, 1.000000000000000000, 0.8660254037844387076, 1.000000000000000000, 0.8660254037844387076, 1.000000000000000000, 0.8660254037844387076, 1.000000000000000000, 0.8660254037844387076, 1.000000000000000000, 0.8660254037844387076, 1.000000000000000000, 0.8660254037844387076, 1.000000000000000000, 0.8660254037844387076, 1.000000000000000000, 0.8660254037844387076, 1.000000000000000000, 0.8660254037844387076, 1.000000000000000000, 0.8660254037844387076, 1.000000000000000000, 0.8660254037844387076, 1.000000000000000000, 0.8660254037844387076, 1.000000000000000000, 0.8660254037844387076, 1.000000000000000000, 0.8660254037844387076, 1.000000000000000000, 0.8660254037844387076, 1.000000000000000000, 0.8660254037844387076, 1.000000000000000000, 0.8660254037844387076, 1.000000000000000000, 0.8660254037844387076, 1.000000000000000000, 0.8660254037844387076, 1.000000000000000000, 0.8660254037844387076, 1.000000000000000000, 0.8660254037844387076, 1.000000000000000000, 0.8660254037844387076, 1.000000000000000000, 0.8660254037844387076, 1.000000000000000000, 0.8660254037844387076, 1.000000000000000000, 0.8660254037844387076, 1.000000000000000000, 0.8660254037844387076, 1.000000000000000000, 0.8660254037844387076, 1.000000000000000000, 0.8660254037844387076, 1.000000000000000000, 0.8660254037844387076, 1.000000000000000000, 0.8660254037844387076, 1.000000000000000000, 0.8660254037844387076, 1.000000000000000000, 0.8660254037844387076, 1.000000000000000000, 0.8660254037844387076, 1.000000000000000000, 0.8660254037844387076, 1.000000000000000000, 0.8660254037844387076, 1.000000000000000000, 0.8660254037844387076, 1.000000000000000000, 0.8660254037844387076, 1.000000000000000000, 0.8660254037844387076, 1.000000000000000000, 0.8660254037844387076, 1.000000000000000000, 0.8660254037844387076, 1.000000000000000000, 0.8660254037844387076, 1.000000000000000000, 0.8660254037844387076, 1.000000000000000000, 0.8660254037844387076, 1.000000000000000000, 0.8660254037844387076, 1.000000000000000000, 0.8660254037844387076, 1.000000000000000000, 0.8660254037844387076, 1.000000000000000000, 0.8660254037844387076, 1.000000000000000000, 0.8660254037844387076, 1.000000000000000000, 0.8660254037844387076, 1.000000000000000000, 0.8660254037844387076, 1.000000000000000000, 0.8660254037844387076, 1.000000000000000000, 0.8660254037844387076, 1.000000000000000000, 0.8660254037844387076, 1.000000000000000000, 0.8660254037844387076, 1.000000000000000000, 0.8660254037844387076, 1.000000000000000000, 0.8660254037844387076, 1.000000000000000000, 0.8660254037844387076, 1.000000000000000000, 0.8660254037844387076, 1.000000000000000000, 0.8660254037844387076, 1.000000000000000000, 0.8660254037844387076, 1.000000000000000000, 0.8660254037844387076, 1.000000000000000000, 0.8660254037844387076, 1.000000000000000000, 0.8660254037844387076, 1.000000000000000000, 0.8660254037844387076, 1.000000000000000000, 0.8660254037844387076, 1.000000000000000000, 0.8660254037844387076, 1.000000000000000000, 0.8660254037844387076, 1.000000000000000000, 0.8660254037844387076, 1.000000000000000000, 0.8660254037844387076, 1.000000000000000000, 0.8660254037844387076, 1.000000000000000000, 0.8660254037844387076, 1.000000000000000000, 0.8660254037844387076, 1.000000000000000000, 0.8660254037844387076, 1.000000000000000000, 0.8660254037844387076, 1.000000000000000000, 0.8660254037844387076, 1.000000000000000000, 0.8660254037844387076, 1.000000000000000000, 0.8660254037844387076, 1.000000000000000000, 0.8660254037844387076, 1.000000000000000000, 0.8660254037844387076, 1.000000000000000000, 0.8660254037844387076, 1.000000000000000000, 0.8660254037844387076, 1.000000000000000000, 0.8660254037844387076, 1.000000000000000000, 0.8660254037844387076, 1.000000000000000000, 0.8660254037844387076, 1.000000000000000000, 0.8660254037844387076, 1.000000000000000000, 0.8660254037844387076, 1.000000000000000000, 0.8660254037844387076, 1.000000000000000000, 0.8660254037844387076, 1.000000000000000000, 0.8660254037844387076, 1.000000000000000000, 0.8660254037844387076, 1.000000000000000000, 0.8660254037844387076, 1.000000000000000000, 0.8660254037844387076, 1.000000000000000000, 0.8660254037844387076, 1.000000000000000000, 0.8660254037844387076, 1.000000000000000000, 0.8660254037844387076, 1.000000000000000000, 0.8660254037844387076, 1.000000000000000000, 0.8660254037844387076, 1.000000000000000000, 0.8660254037844387076, 1.000000000000000000, 0.8660254037844387076, 1.000000000000000000, 0.8660254037844387076, 1.000000000000000000, 0.8660254037844387076, 1.000000000000000000, 0.8660254037844387076, 1.000000000000000000),
 ( 1.000000000000000000, 0.8660254037844387076, 1.000000000000000000, 0.8660254037844387076, 1.000000000000000000, 0.8660254037844387076, 1.000000000000000000, 0.8660254037844387076, 1.000000000000000000, 0.8660254037844387076, 1.000000000000000000, 0.8660254037844387076, 1.000000000000000000, 0.8660254037844387076, 1.000000000000000000, 0.8660254037844387076, 1.000000000000000000, 0.8660254037844387076, 1.000000000000000000, 0.8660254037844387076, 1.000000000000000000, 0.8660254037844387076, 1.000000000000000000, 0.8660254037844387076, 1.000000000000000000, 0.8660254037844387076, 1.000000000000000000, 0.8660254037844387076, 1.000000000000000000, 0.8660254037844387076, 1.000000000000000000, 0.8660254037844387076, 1.000000000000000000, 0.8660254037844387076, 1.000000000000000000, 0.8660254037844387076, 1.000000000000000000, 0.8660254037844387076, 1.000000000000000000, 0.8660254037844387076, 1.000000000000000000, 0.8660254037844387076, 1.000000000000000000, 0.8660254037844387076, 1.000000000000000000, 0.8660254037844387076, 1.000000000000000000, 0.8660254037844387076, 1.000000000000000000, 0.8660254037844387076, 1.000000000000000000, 0.8660254037844387076, 1.000000000000000000, 0.8660254037844387076, 1.000000000000000000, 0.8660254037844387076, 1.000000000000000000, 0.8660254037844387076, 1.000000000000000000, 0.8660254037844387076, 1.000000000000000000, 0.8660254037844387076, 1.000000000000000000, 0.8660254037844387076, 1.000000000000000000, 0.8660254037844387076, 1.000000000000000000, 0.8660254037844387076, 1.000000000000000000, 0.8660254037844387076, 1.000000000000000000, 0.8660254037844387076, 1.000000000000000000, 0.8660254037844387076, 1.000000000000000000, 0.8660254037844387076, 1.000000000000000000, 0.8660254037844387076, 1.000000000000000000, 0.8660254037844387076, 1.000000000000000000, 0.8660254037844387076, 1.000000000000000000, 0.8660254037844387076, 1.000000000000000000, 0.8660254037844387076, 1.000000000000000000, 0.8660254037844387076, 1.000000000000000000, 0.8660254037844387076, 1.000000000000000000, 0.8660254037844387076, 1.000000000000000000, 0.8660254037844387076, 1.000000000000000000, 0.8660254037844387076, 1.000000000000000000, 0.8660254037844387076, 1.000000000000000000, 0.8660254037844387076, 1.000000000000000000, 0.8660254037844387076, 1.000000000000000000, 0.8660254037844387076, 1.000000000000000000, 0.8660254037844387076, 1.000000000000000000, 0.8660254037844387076, 1.000000000000000000, 0.8660254037844387076, 1.000000000000000000, 0.8660254037844387076, 1.000000000000000000, 0.8660254037844387076, 1.000000000000000000, 0.8660254037844387076, 1.000000000000000000, 0.8660254037844387076, 1.000000000000000000, 0.8660254037844387076, 1.000000000000000000, 0.8660254037844387076, 1.000000000000000000, 0.8660254037844387076, 1.000000000000000000, 0.8660254037844387076, 1.000000000000000000, 0.8660254037844387076, 1.000000000000000000, 0.8660254037844387076, 1.000000000000000000, 0.8660254037844387076, 1.000000000000000000, 0.8660254037844387076, 1.000000000000000000, 0.8660254037844387076, 1.000000000000000000, 0.8660254037844387076, 1.000000000000000000, 0.8660254037844387076, 1.000000000000000000, 0.8660254037844387076, 1.000000000000000000, 0.8660254037844387076, 1.000000000000000000, 0.8660254037844387076, 1.000000000000000000, 0.8660254037844387076, 1.000000000000000000, 0.8660254037844387076, 1.000000000000000000, 0.8660254037844387076, 1.000000000000000000, 0.8660254037844387076, 1.000000000000000000, 0.8660254037844387076, 1.000000000000000000, 0.8660254037844387076, 1.000000000000000000, 0.8660254037844387076, 1.000000000000000000, 0.8660254037844387076, 1.000000000000000000, 0.8660254037844387076, 1.000000000000000000, 0.8660254037844387076, 1.000000000000000000, 0.8660254037844387076, 1.000000000000000000, 0.8660254037844387076, 1.000000000000000000, 0.8660254037844387076, 1.000000000000000000, 0.8660254037844387076, 1.000000000000000000, 0.8660254037844387076, 1.000000000000000000, 0.8660254037844387076, 1.000000000000000000, 0.8660254037844387076, 1.000000000000000000, 0.8660254037844387076, 1.000000000000000000, 0.8660254037844387076, 1.000000000000000000, 0.8660254037844387076, 1.000000000000000000, 0.8660254037844387076, 1.000000000000000000, 0.8660254037844387076, 1.000000000000000000, 0.8660254037844387076, 1.000000000000000000, 0.8660254037844387076, 1.000000000000000000, 0.8660254037844387076, 1.000000000000000000, 0.8660254037844387076, 1.000000000000000000, 0.8660254037844387076, 1.000000000000000000, 0.8660254037844387076, 1.000000000000000000, 0.8660254037844387076, 1.000000000000000000, 0.8660254037844387076, 1.000000000000000000, 0.8660254037844387076, 1.000000000000000000, 0.8660254037844387076, 1.000000000000000000, 0.8660254037844387076, 1.000000000000000000, 0.8660254037844387076, 1.000000000000000000, 0.8660254037844387076, 1.000000000000000000, 0.8660254037844387076, 1.000000000000000000, 0.8660254037844387076, 1.000000000000000000, 0.8660254037844387076, 1.000000000000000000, 0.8660254037844387076, 1.000000000000000000, 0.8660254037844387076, 1.000000000000000000, 0.8660254037844387076, 1.000000000000000000, 0.8660254037844387076, 1.000000000000000000, 0.8660254037844387076, 1.000000000000000000, 0.8660254037844387076, 1.000000000000000000, 0.8660254037844387076, 1.000000000000000000, 0.8660254037844387076, 1.000000000000000000, 0.8660254037844387076, 1.000000000000000000, 0.8660254037844387076, 1.000000000000000000, 0.8660254037844387076, 1.000000000000000000, 0.8660254037844387076, 1.000000000000000000, 0.8660254037844387076, 1.000000000000000000, 0.8660254037844387076, 1.000000000000000000, 0.8660254037844387076, 1.000000000000000000, 0.8660254037844387076, 1.000000000000000000, 0.8660254037844387076, 1.000000000000000000, 0.8660254037844387076, 1.000000000000000000, 0.8660254037844387076, 1.000000000000000000, 0.8660254037844387076, 1.000000000000000000, 0.8660254037844387076, 1.000000000000000000, 0.8660254037844387076, 1.000000000000000000, 0.8660254037844387076, 1.000000000000000000, 0.8660254037844387076, 1.000000000000000000, 0.8660254037844387076, 1.000000000000000000, 0.8660254037844387076, 1.000000000000000000, 0.8660254037844387076, 1.000000000000000000, 0.8660254037844387076, 1.000000000000000000, 0.8660254037844387076, 1.000000000000000000, 0.8660254037844387076, 1.000000000000000000, 0.8660254037844387076, 1.000000000000000000, 0.8660254037844387076, 1.000000000000000000, 0.8660254037844387076, 1.000000000000000000, 0.8660254037844387076, 1.000000000000000000, 0.8660254037844387076, 1.000000000000000000, 0.8660254037844387076, 1.000000000000000000, 0.8660254037844387076, 1.000000000000000000, 0.8660254037844387076, 1.000000000000000000, 0.8660254037844387076, 1.000000000000000000, 0.8660254037844387076, 1.000000000000000000, 0.8660254037844387076, 1.000000000000000000, 0.8660254037844387076, 1.000000000000000000, 0.8660254037844387076, 1.000000000000000000, 0.8660254037844387076, 1.000000000000000000, 0.8660254037844387076, 1.000000000000000000, 0.8660254037844387076, 1.000000000000000000, 0.8660254037844387076, 1.000000000000000000, 0.8660254037844387076, 1.000000000000000000, 0.8660254037844387076, 1.000000000000000000, 0.8660254037844387076, 1.000000000000000000, 0.8660254037844387076, 1.000000000000000000, 0.8660254037844387076, 1.000000000000000000, 0.8660254037844387076, 1.000000000000000000, 0.8660254037844387076, 1.000000000000000000, 0.8660254037844387076, 1.000000000000000000, 0.8660254037844387076, 1.000000000000000000, 0.8660254037844387076, 1.000000000000000000) ) ) 
 REPRESENTATION_ITEM ( '' )  SURFACE ( )  );
#92319=CARTESIAN_POINT ( 'NONE',  ( -1.364683531250014514, 14.58854166700806232, -0.7879004041258335089 ) ) ;
#92334=ORIENTED_EDGE ( 'NONE', *, *, #105381, .F. ) ;
#92358=CARTESIAN_POINT ( 'NONE',  ( -1.286956418854606543, 4.047654341997520611, 0.4592741676706140197 ) ) ;
#92360=ORIENTED_EDGE ( 'NONE', *, *, #38367, .T. ) ;
#92381=CARTESIAN_POINT ( 'NONE',  ( 0.7500000000000006661, 11.44791666734946212, -1.299038105676657340 ) ) ;
#92430=CARTESIAN_POINT ( 'NONE',  ( 1.446621748570332322, 3.374878948858031080, -0.4012476001784985313 ) ) ;
#92433=VECTOR ( 'NONE', #97315, 1000.000000000000000 ) ;
#92457=CARTESIAN_POINT ( 'NONE',  ( -0.6823417656250039265, 13.38020833367473195, -1.181850606188755259 ) ) ;
#92468=ORIENTED_EDGE ( 'NONE', *, *, #29848, .F. ) ;
#92484=AXIS2_PLACEMENT_3D ( 'NONE', #191603, #90944, #157011 ) ;
#92494=LINE ( 'NONE', #158533, #63174 ) ;
#92521=CARTESIAN_POINT ( 'NONE',  ( 1.364683531249997417, 12.29687500034139980, 2.602085213965210642E-15 ) ) ;
#92562=CARTESIAN_POINT ( 'NONE',  ( 0.7500000000000006661, 11.36458333401613174, 1.299038105676657340 ) ) ;
#92564=ORIENTED_EDGE ( 'NONE', *, *, #83416, .T. ) ;
#92646=ORIENTED_EDGE ( 'NONE', *, *, #203174, .F. ) ;
#92696=CARTESIAN_POINT ( 'NONE',  ( 1.364683531249997417, 11.23437500034139802, 2.602085213965210642E-15 ) ) ;
#92702=CARTESIAN_POINT ( 'NONE',  ( 0.7500000000000006661, 8.833333333333332149, 1.299038105676657340 ) ) ;
#92771=CARTESIAN_POINT ( 'NONE',  ( 0.6823417656249969321, 15.33854166700806410, -1.181850606188757036 ) ) ;
#92815=CARTESIAN_POINT ( 'NONE',  ( 1.220146605508150803E-14, 9.718750000682797818, -1.499999999999998446 ) ) ;
#92938=CYLINDRICAL_SURFACE ( 'NONE', #72023, 1.500000000000000222 ) ;
#92960=CARTESIAN_POINT ( 'NONE',  ( -0.7500000000000179856, 11.79166666666666607, 1.299038105676658228 ) ) ;
#92965=CARTESIAN_POINT ( 'NONE',  ( -1.364683531250014514, 10.83854166700806942, -0.7879004041258335089 ) ) ;
#93004=CARTESIAN_POINT ( 'NONE',  ( 1.364683531250000748, 12.31770833367473195, -0.7879004041258355073 ) ) ;
#93019=AXIS2_PLACEMENT_3D ( 'NONE', #159611, #176929, #11208 ) ;
#93073=CARTESIAN_POINT ( 'NONE',  ( 0.7500000000000006661, 13.36458333401613352, 1.299038105676657340 ) ) ;
#93083=CARTESIAN_POINT ( 'NONE',  ( -3.602337597214539753E-15, 12.59375000068279782, 1.500000000000001554 ) ) ;
#93087=( BOUNDED_CURVE ( )  B_SPLINE_CURVE ( 2, ( #52835, #199057, #36576, #101587, #102662, #134126, #33380, #150354, #67983 ),
 .UNSPECIFIED., .F., .T. ) 
 B_SPLINE_CURVE_WITH_KNOTS ( ( 3, 2, 2, 2, 3 ),
 ( 0.3839285714285713969, 0.3869047619047619180, 0.3928571428571428492, 0.3988095238095238360, 0.4017857142857143016 ),
 .UNSPECIFIED. ) 
 CURVE ( )  GEOMETRIC_REPRESENTATION_ITEM ( )  RATIONAL_B_SPLINE_CURVE ( ( 0.9330127018922194093, 0.9330127018922187432, 1.000000000000000000, 0.8660254037844387076, 1.000000000000000000, 0.8660254037844387076, 1.000000000000000000, 0.9330127018922194093, 0.9330127018922194093 ) ) 
 REPRESENTATION_ITEM ( '' )  );
#93106=CARTESIAN_POINT ( 'NONE',  ( 1.364683531249996529, 9.463541667008062319, 0.7879004041258405033 ) ) ;
#93138=EDGE_CURVE ( 'NONE', #100761, #86666, #69500, .T. ) ;
#93238=FACE_OUTER_BOUND ( 'NONE', #58078, .T. ) ;
#93261=CARTESIAN_POINT ( 'NONE',  ( 0.6823417656249934904, 10.25520833367472839, 1.181850606188764807 ) ) ;
#93329=CARTESIAN_POINT ( 'NONE',  ( -1.500000000000015099, 14.72916666666666252, -0.8660254037844309360 ) ) ;
#93373=CARTESIAN_POINT ( 'NONE',  ( -1.364683531250010295, 14.63020833367473550, 0.7879004041258445001 ) ) ;
#93384=VECTOR ( 'NONE', #156913, 1000.000000000000000 ) ;
#93385=CARTESIAN_POINT ( 'NONE',  ( -1.393602545685228788, 4.337953148244114487, 0.1272763605452716384 ) ) ;
#93438=FACE_OUTER_BOUND ( 'NONE', #104424, .T. ) ;
#93491=CARTESIAN_POINT ( 'NONE',  ( 1.435158330144293393, 3.628467426565245901, -0.4529249069356899304 ) ) ;
#93514=CARTESIAN_POINT ( 'NONE',  ( -0.6823417656250003738, 13.46354166700806942, 1.181850606188754593 ) ) ;
#93523=CARTESIAN_POINT ( 'NONE',  ( 0.000000000000000000, 13.49999999999999822, 0.000000000000000000 ) ) ;
#93531=VERTEX_POINT ( 'NONE', #171289 ) ;
#93566=FACE_OUTER_BOUND ( 'NONE', #1193, .T. ) ;
#93580=CARTESIAN_POINT ( 'NONE',  ( -1.364683531250014514, 12.15104166700806765, -0.7879004041258335089 ) ) ;
#93622=CARTESIAN_POINT ( 'NONE',  ( -6.009258394948636914E-15, 11.46875000068279604, -1.732050807568875195 ) ) ;
#93645=ADVANCED_FACE ( 'NONE', ( #155049 ), #41317, .T. ) ;
#93693=AXIS2_PLACEMENT_3D ( 'NONE', #108588, #121657, #71725 ) ;
#93726=CARTESIAN_POINT ( 'NONE',  ( 1.297698954646254954, 4.098833406624212472, 0.4386024987755403060 ) ) ;
#93745=CARTESIAN_POINT ( 'NONE',  ( -1.286956418854627637, 4.047654341997620975, 0.4592741676705713871 ) ) ;
#93761=CARTESIAN_POINT ( 'NONE',  ( 1.364683531250000748, 11.25520833367473372, -0.7879004041258355073 ) ) ;
#93776=DIRECTION ( 'NONE',  ( 0.000000000000000000, -1.000000000000000000, 0.000000000000000000 ) ) ;
#93875=FACE_OUTER_BOUND ( 'NONE', #149605, .T. ) ;
#93987=CARTESIAN_POINT ( 'NONE',  ( -2.788906526875773208E-15, 10.43750000000000000, -1.499999999999998446 ) ) ;
#94028=CARTESIAN_POINT ( 'NONE',  ( -1.500000000000001110, 13.02083333333333393, 0.8660254037844419273 ) ) ;
#94034=CARTESIAN_POINT ( 'NONE',  ( 1.364683531249996529, 8.963541667008067648, 0.7879004041258405033 ) ) ;
#94038=ORIENTED_EDGE ( 'NONE', *, *, #122759, .T. ) ;
#94071=CARTESIAN_POINT ( 'NONE',  ( -8.012344526598182026E-15, 11.85937500034140157, -1.575800808251669460 ) ) ;
#94076=AXIS2_PLACEMENT_3D ( 'NONE', #5599, #117321, #38148 ) ;
#94081=ORIENTED_EDGE ( 'NONE', *, *, #167459, .F. ) ;
#94143=CARTESIAN_POINT ( 'NONE',  ( -1.500000000000001110, 14.55208333401612819, 0.8660254037844419273 ) ) ;
#94145=EDGE_LOOP ( 'NONE', ( #67247, #146507, #83493, #41859 ) ) ;
#94177=CARTESIAN_POINT ( 'NONE',  ( -1.364683531250010295, 8.380208333674730170, 0.7879004041258445001 ) ) ;
#94185=CARTESIAN_POINT ( 'NONE',  ( 1.499999999999993117, 11.13541666734946389, 0.8660254037844408170 ) ) ;
#94326=CARTESIAN_POINT ( 'NONE',  ( -1.364683531250010295, 9.192708333674733723, 0.7879004041258445001 ) ) ;
#94347=CARTESIAN_POINT ( 'NONE',  ( 0.6500564563262788420, 3.349926606758537151, -0.06808518787146825013 ) ) ;
#94440=CARTESIAN_POINT ( 'NONE',  ( 1.364683531249997417, 13.48437500034139980, 2.602085213965210642E-15 ) ) ;
#94451=CARTESIAN_POINT ( 'NONE',  ( -1.436299488671407332, 4.080021472972510388, 0.4486666144298727121 ) ) ;
#94456=VERTEX_POINT ( 'NONE', #142326 ) ;
#94507=PLANE ( 'NONE',  #151847 ) ;
#94510=EDGE_LOOP ( 'NONE', ( #94081, #205953, #59263, #193229 ) ) ;
#94527=CARTESIAN_POINT ( 'NONE',  ( -2.788906526875773208E-15, 10.18750000000000000, -1.499999999999998446 ) ) ;
#94558=CARTESIAN_POINT ( 'NONE',  ( 1.272148008267887986, 3.722367574780562460, -0.4878157535072898954 ) ) ;
#94581=CARTESIAN_POINT ( 'NONE',  ( 0.6823417656249969321, 14.33854166700806232, -1.181850606188757036 ) ) ;
#94636=LINE ( 'NONE', #122940, #165668 ) ;
#94646=CARTESIAN_POINT ( 'NONE',  ( -1.364683531250010295, 11.94270833367473017, 0.7879004041258445001 ) ) ;
#94692=CARTESIAN_POINT ( 'NONE',  ( 1.499999999999997113, 10.42708333401613352, -0.8660254037844378194 ) ) ;
#94741=CARTESIAN_POINT ( 'NONE',  ( -0.4153311931458959494, 3.850000000000006306, 0.5000000000000064393 ) ) ;
#94789=( BOUNDED_CURVE ( )  B_SPLINE_CURVE ( 2, ( #105508, #38346, #140144, #89250, #57798, #6884, #185646, #39413, #171540 ),
 .UNSPECIFIED., .F., .T. ) 
 B_SPLINE_CURVE_WITH_KNOTS ( ( 3, 2, 2, 2, 3 ),
 ( 0.4017857142857143016, 0.4047619047619047672, 0.4107142857142856984, 0.4166666666666666852, 0.4196428571428570953 ),
 .UNSPECIFIED. ) 
 CURVE ( )  GEOMETRIC_REPRESENTATION_ITEM ( )  RATIONAL_B_SPLINE_CURVE ( ( 0.9330127018922194093, 0.9330127018922194093, 1.000000000000000000, 0.8660254037844387076, 1.000000000000000000, 0.8660254037844387076, 1.000000000000000000, 0.9330127018922206306, 0.9330127018922194093 ) ) 
 REPRESENTATION_ITEM ( '' )  );
#94790=CARTESIAN_POINT ( 'NONE',  ( 1.400320522945621482, 4.350623259974997659, -0.06109695461879249834 ) ) ;
#94809=CARTESIAN_POINT ( 'NONE',  ( -1.352862181796079533, 3.447832334330404258, -0.3040832447043430586 ) ) ;
#94826=CARTESIAN_POINT ( 'NONE',  ( 0.6823417656249934904, 9.192708333674733723, 1.181850606188764807 ) ) ;
#94875=ORIENTED_EDGE ( 'NONE', *, *, #17750, .F. ) ;
#94901=VECTOR ( 'NONE', #7551, 1000.000000000000000 ) ;
#94971=( BOUNDED_CURVE ( )  B_SPLINE_CURVE ( 2, ( #97895, #193236, #13412, #181244, #11274, #79487, #163955, #115253, #145606 ),
 .UNSPECIFIED., .F., .T. ) 
 B_SPLINE_CURVE_WITH_KNOTS ( ( 3, 2, 2, 2, 3 ),
 ( 0.7232142857142856984, 0.7261904761904761640, 0.7321428571428570953, 0.7380952380952381375, 0.7410714285714286031 ),
 .UNSPECIFIED. ) 
 CURVE ( )  GEOMETRIC_REPRESENTATION_ITEM ( )  RATIONAL_B_SPLINE_CURVE ( ( 0.9330127018922194093, 0.9330127018922194093, 1.000000000000000000, 0.8660254037844387076, 1.000000000000000000, 0.8660254037844387076, 1.000000000000000000, 0.9330127018922194093, 0.9330127018922194093 ) ) 
 REPRESENTATION_ITEM ( '' )  );
#94982=UNCERTAINTY_MEASURE_WITH_UNIT (LENGTH_MEASURE( 1.000000000000000082E-05 ), #159440, 'distance_accuracy_value', 'NONE');
#94998=ORIENTED_EDGE ( 'NONE', *, *, #90295, .F. ) ;
#95091=CARTESIAN_POINT ( 'NONE',  ( -0.7500000000000006661, 11.70833333333333393, -1.299038105676657340 ) ) ;
#95097=CARTESIAN_POINT ( 'NONE',  ( 0.6823417656249969321, 9.276041667008065872, -1.181850606188757036 ) ) ;
#95133=CARTESIAN_POINT ( 'NONE',  ( 0.6823417656249934904, 12.50520833367473017, 1.181850606188764807 ) ) ;
#95199=EDGE_CURVE ( 'NONE', #80954, #40283, #124565, .T. ) ;
#95203=CARTESIAN_POINT ( 'NONE',  ( 1.499999999999993117, 14.38541666734946389, 0.8660254037844409281 ) ) ;
#95216=CARTESIAN_POINT ( 'NONE',  ( 0.000000000000000000, 0.000000000000000000, 0.000000000000000000 ) ) ;
#95240=CARTESIAN_POINT ( 'NONE',  ( 1.364683531250000303, 8.755208333674731946, -0.7879004041258355073 ) ) ;
#95241=AXIS2_PLACEMENT_3D ( 'NONE', #140971, #142029, #205914 ) ;
#95421=ORIENTED_EDGE ( 'NONE', *, *, #199200, .T. ) ;
#95513=CARTESIAN_POINT ( 'NONE',  ( -0.6823417656250039265, 12.81770833367473017, -1.181850606188755259 ) ) ;
#95524=CARTESIAN_POINT ( 'NONE',  ( -1.499577476386907859, 4.449079813965669317, -0.09296422598484958832 ) ) ;
#95555=EDGE_LOOP ( 'NONE', ( #147856, #130378, #210413, #176896 ) ) ;
#95634=CARTESIAN_POINT ( 'NONE',  ( 1.491588839496432728, 3.267857031437547466, -0.1769418395740485206 ) ) ;
#95658=CARTESIAN_POINT ( 'NONE',  ( 1.364683531250000303, 14.31770833367473372, -0.7879004041258355073 ) ) ;
#95692=VERTEX_POINT ( 'NONE', #91867 ) ;
#95717=CARTESIAN_POINT ( 'NONE',  ( -0.6823417656250003738, 10.21354166700806587, 1.181850606188754593 ) ) ;
#95759=CARTESIAN_POINT ( 'NONE',  ( -1.500000000000001110, 10.05208333401613174, 0.8660254037844419273 ) ) ;
#95810=CARTESIAN_POINT ( 'NONE',  ( -5.000000000000009770, 3.850000000000006306, 0.5000000000000064393 ) ) ;
#95861=CARTESIAN_POINT ( 'NONE',  ( 1.273728293839817116, 3.712158128753963560, 0.4850152072975459361 ) ) ;
#95881=CARTESIAN_POINT ( 'NONE',  ( -1.378728738066232307, 3.613591550242559070, -0.5908528300941753297 ) ) ;
#95901=CARTESIAN_POINT ( 'NONE',  ( 1.364683531249996529, 8.713541667008067648, 0.7879004041258403923 ) ) ;
#95914=FACE_OUTER_BOUND ( 'NONE', #2434, .T. ) ;
#96004=CYLINDRICAL_SURFACE ( 'NONE', #131089, 1.500000000000000222 ) ;
#96138=CARTESIAN_POINT ( 'NONE',  ( 4.764381983412778688E-15, 12.93749999999999645, -1.499999999999998446 ) ) ;
#96160=CARTESIAN_POINT ( 'NONE',  ( -1.500000000000001110, 10.77083333333333037, 0.8660254037844419273 ) ) ;
#96167=CARTESIAN_POINT ( 'NONE',  ( -8.012344526598182026E-15, 9.296875000341398021, -1.575800808251669460 ) ) ;
#96201=CARTESIAN_POINT ( 'NONE',  ( -1.364683531250014514, 11.15104166700806232, -0.7879004041258335089 ) ) ;
#96233=ORIENTED_EDGE ( 'NONE', *, *, #59329, .F. ) ;
#96252=CARTESIAN_POINT ( 'NONE',  ( 1.836970198721030181E-16, 13.49999999999999822, 1.500000000000000222 ) ) ;
#96268=VECTOR ( 'NONE', #114947, 1000.000000000000000 ) ;
#96272=CARTESIAN_POINT ( 'NONE',  ( 1.500000000000001332, 13.65625000068279604, 0.000000000000000000 ) ) ;
#96304=CARTESIAN_POINT ( 'NONE',  ( -8.012344526598182026E-15, 8.546875000341403350, -1.575800808251669460 ) ) ;
#96318=AXIS2_PLACEMENT_3D ( 'NONE', #3711, #200851, #168387 ) ;
#96366=EDGE_CURVE ( 'NONE', #109852, #39789, #67506, .T. ) ;
#96430=VERTEX_POINT ( 'NONE', #203171 ) ;
#96463=CARTESIAN_POINT ( 'NONE',  ( -1.364683531250010295, 8.442708333674730170, 0.7879004041258445001 ) ) ;
#96469=CARTESIAN_POINT ( 'NONE',  ( -1.301544632936721735, 13.25916247302991380, 0.7160067306521127328 ) ) ;
#96476=CARTESIAN_POINT ( 'NONE',  ( -1.500000000000001110, 9.520833333333333925, 0.8660254037844418162 ) ) ;
#96501=CARTESIAN_POINT ( 'NONE',  ( -0.7500000000000179856, 10.07291666734946922, 1.299038105676658228 ) ) ;
#96508=VERTEX_POINT ( 'NONE', #67821 ) ;
#96512=ORIENTED_EDGE ( 'NONE', *, *, #19860, .T. ) ;
#96574=CARTESIAN_POINT ( 'NONE',  ( -1.402160292154681736E-14, 12.67187500034139802, 1.575800808251682339 ) ) ;
#96640=CIRCLE ( 'NONE', #114007, 0.6500000000000000222 ) ;
#96703=CARTESIAN_POINT ( 'NONE',  ( 1.378881877344207085, 3.612814789603054688, 0.5904953584336758432 ) ) ;
#96725=CARTESIAN_POINT ( 'NONE',  ( 0.6823417656249969321, 12.58854166700806942, -1.181850606188757036 ) ) ;
#96787=CARTESIAN_POINT ( 'NONE',  ( -0.6823417656250039265, 10.63020833367472839, -1.181850606188755259 ) ) ;
#96827=CARTESIAN_POINT ( 'NONE',  ( -0.7500000000000179856, 9.822916667349467446, 1.299038105676658228 ) ) ;
#96879=CARTESIAN_POINT ( 'NONE',  ( -0.4841688312534676575, 4.104470248636722829, -0.4351271339794008930 ) ) ;
#96930=CARTESIAN_POINT ( 'NONE',  ( 1.425171720896451832, 3.733877413282800095, 0.4907744223921421955 ) ) ;
#96950=EDGE_CURVE ( 'NONE', #170253, #140850, #116448, .T. ) ;
#96968=CARTESIAN_POINT ( 'NONE',  ( -1.364683531250014514, 9.088541667008060543, -0.7879004041258335089 ) ) ;
#97021=ORIENTED_EDGE ( 'NONE', *, *, #154979, .F. ) ;
#97039=CARTESIAN_POINT ( 'NONE',  ( -8.012344526598182026E-15, 14.35937500034139802, -1.575800808251669460 ) ) ;
#97221=CARTESIAN_POINT ( 'NONE',  ( 1.499999999999993117, 11.10416666666666785, 0.8660254037844409281 ) ) ;
#97225=CARTESIAN_POINT ( 'NONE',  ( -1.364683531250010295, 9.630208333674735499, 0.7879004041258445001 ) ) ;
#97242=CARTESIAN_POINT ( 'NONE',  ( -1.264911064067355984, 3.850000000000006306, -0.5000000000000004441 ) ) ;
#97259=CARTESIAN_POINT ( 'NONE',  ( 0.6823417656249969321, 10.58854166700806587, -1.181850606188757036 ) ) ;
#97315=DIRECTION ( 'NONE',  ( 0.000000000000000000, -1.000000000000000000, 0.000000000000000000 ) ) ;
#97333=CARTESIAN_POINT ( 'NONE',  ( 1.499999999999997113, 13.42708333401613174, -0.8660254037844378194 ) ) ;
#97367=CARTESIAN_POINT ( 'NONE',  ( -1.364683531250014514, 8.588541667008067648, -0.7879004041258335089 ) ) ;
#97390=EDGE_LOOP ( 'NONE', ( #92360, #71911 ) ) ;
#97472=CARTESIAN_POINT ( 'NONE',  ( -8.012344526598182026E-15, 12.29687500034140513, -1.575800808251669460 ) ) ;
#97519=CARTESIAN_POINT ( 'NONE',  ( -0.6823417656250003738, 8.463541667008064096, 1.181850606188754593 ) ) ;
#97525=CARTESIAN_POINT ( 'NONE',  ( -1.022621712794113735, 13.26710252192129502, 1.066516380167074507 ) ) ;
#97544=CARTESIAN_POINT ( 'NONE',  ( 1.355148357678327420, 3.769637942705310163, 0.6430964159811484171 ) ) ;
#97592=CARTESIAN_POINT ( 'NONE',  ( -0.4019237886467001974, 9.832585450998172050, 1.500000000000001998 ) ) ;
#97601=CARTESIAN_POINT ( 'NONE',  ( -1.500000000000008216, 8.281250000682797818, 3.469446951953614189E-15 ) ) ;
#97613=CARTESIAN_POINT ( 'NONE',  ( 0.7500000000000006661, 11.16666666666666430, -1.299038105676657340 ) ) ;
#97630=CARTESIAN_POINT ( 'NONE',  ( -0.6823417656250039265, 13.06770833367473017, -1.181850606188755259 ) ) ;
#97634=AXIS2_PLACEMENT_3D ( 'NONE', #160583, #108702, #127108 ) ;
#97769=DIRECTION ( 'NONE',  ( 0.000000000000000000, -1.000000000000000000, 0.000000000000000000 ) ) ;
#97778=CARTESIAN_POINT ( 'NONE',  ( -1.364683531250010295, 11.94270833367473017, 0.7879004041258445001 ) ) ;
#97839=CARTESIAN_POINT ( 'NONE',  ( 1.364683531249996529, 10.27604166700806765, 0.7879004041258405033 ) ) ;
#97850=CARTESIAN_POINT ( 'NONE',  ( 1.378728738066221871, 4.086408449757453099, -0.5908528300941785494 ) ) ;
#97886=CARTESIAN_POINT ( 'NONE',  ( 1.500000000000001332, 9.656250000682799595, 0.000000000000000000 ) ) ;
#97895=CARTESIAN_POINT ( 'NONE',  ( -2.788906526875773208E-15, 10.21875000068279782, -1.499999999999998446 ) ) ;
#97989=CARTESIAN_POINT ( 'NONE',  ( -1.115562610750309283E-14, 9.312500000000001776, 1.500000000000001554 ) ) ;
#98029=CARTESIAN_POINT ( 'NONE',  ( -1.364683531250000748, 8.859375000341396245, 0.000000000000000000 ) ) ;
#98045=ORIENTED_EDGE ( 'NONE', *, *, #207616, .F. ) ;
#98055=CARTESIAN_POINT ( 'NONE',  ( 0.000000000000000000, 13.49999999999999822, -1.500000000000000222 ) ) ;
#98073=VERTEX_POINT ( 'NONE', #69498 ) ;
#98098=CARTESIAN_POINT ( 'NONE',  ( 1.364683531249996529, 14.52604166700806232, 0.7879004041258405033 ) ) ;
#98272=CARTESIAN_POINT ( 'NONE',  ( -1.500000000000015099, 11.47916666666666252, -0.8660254037844309360 ) ) ;
#98277=CARTESIAN_POINT ( 'NONE',  ( 0.6823417656249969321, 8.776041667008065872, -1.181850606188757036 ) ) ;
#98311=CARTESIAN_POINT ( 'NONE',  ( 0.6823417656249969321, 10.33854166700806587, -1.181850606188757036 ) ) ;
#98379=EDGE_CURVE ( 'NONE', #99270, #72363, #132479, .T. ) ;
#98382=CARTESIAN_POINT ( 'NONE',  ( 0.7500000000000006661, 13.11458333401613352, 1.299038105676657340 ) ) ;
#98429=CARTESIAN_POINT ( 'NONE',  ( 1.499999999999993117, 10.88541666734946389, 0.8660254037844408170 ) ) ;
#98439=ORIENTED_EDGE ( 'NONE', *, *, #201285, .T. ) ;
#98560=CARTESIAN_POINT ( 'NONE',  ( -1.264911064067355984, 3.850000000000006306, -0.5000000000000004441 ) ) ;
#98573=CARTESIAN_POINT ( 'NONE',  ( -0.4019237886466933696, 12.08258545099816850, 1.500000000000005995 ) ) ;
#98664=CARTESIAN_POINT ( 'NONE',  ( -1.500000000000015099, 9.729166666666671404, -0.8660254037844309360 ) ) ;
#98679=CARTESIAN_POINT ( 'NONE',  ( -0.6823417656250003738, 12.40104166700806232, 1.181850606188754593 ) ) ;
#98728=VERTEX_POINT ( 'NONE', #160375 ) ;
#98818=EDGE_CURVE ( 'NONE', #170262, #170765, #70652, .T. ) ;
#98835=CARTESIAN_POINT ( 'NONE',  ( -1.364683531250010295, 12.69270833367473550, 0.7879004041258445001 ) ) ;
#98859=CARTESIAN_POINT ( 'NONE',  ( -1.500000000000001110, 12.02083333333333570, 0.8660254037844418162 ) ) ;
#98896=CARTESIAN_POINT ( 'NONE',  ( -1.402160292154681736E-14, 10.23437500034139447, 1.575800808251682339 ) ) ;
#98900=VECTOR ( 'NONE', #113173, 1000.000000000000000 ) ;
#98939=CARTESIAN_POINT ( 'NONE',  ( -0.7500000000000006661, 10.48958333401613174, -1.299038105676657340 ) ) ;
#98978=ORIENTED_EDGE ( 'NONE', *, *, #36800, .T. ) ;
#99044=CARTESIAN_POINT ( 'NONE',  ( 1.499999999999996891, 9.427083334016128191, -0.8660254037844378194 ) ) ;
#99081=CARTESIAN_POINT ( 'NONE',  ( 1.364683531249997417, 8.984375000341396245, 2.602085213965210642E-15 ) ) ;
#99082=LINE ( 'NONE', #148886, #148461 ) ;
#99125=EDGE_CURVE ( 'NONE', #178226, #75675, #142231, .T. ) ;
#99151=CARTESIAN_POINT ( 'NONE',  ( -1.364683531250014514, 14.65104166700806410, -0.7879004041258335089 ) ) ;
#99182=( BOUNDED_CURVE ( )  B_SPLINE_CURVE ( 2, ( #142807, #25806, #191499, #91915, #109278, #175287, #26873, #10616, #60441 ),
 .UNSPECIFIED., .F., .T. ) 
 B_SPLINE_CURVE_WITH_KNOTS ( ( 3, 2, 2, 2, 3 ),
 ( 0.6339285714285713969, 0.6369047619047618625, 0.6428571428571429047, 0.6488095238095238360, 0.6517857142857143016 ),
 .UNSPECIFIED. ) 
 CURVE ( )  GEOMETRIC_REPRESENTATION_ITEM ( )  RATIONAL_B_SPLINE_CURVE ( ( 0.9330127018922194093, 0.9330127018922194093, 1.000000000000000000, 0.8660254037844387076, 1.000000000000000000, 0.8660254037844387076, 1.000000000000000000, 0.9330127018922194093, 0.9330127018922194093 ) ) 
 REPRESENTATION_ITEM ( '' )  );
#99270=VERTEX_POINT ( 'NONE', #87652 ) ;
#99338=CARTESIAN_POINT ( 'NONE',  ( 0.7500000000000006661, 11.66666666666666607, -1.299038105676657340 ) ) ;
#99342=CARTESIAN_POINT ( 'NONE',  ( -0.6823417656250039265, 14.38020833367473195, -1.181850606188755259 ) ) ;
#99380=CARTESIAN_POINT ( 'NONE',  ( -1.364683531250014514, 10.90104166700806942, -0.7879004041258335089 ) ) ;
#99394=CARTESIAN_POINT ( 'NONE',  ( 0.7500000000000006661, 10.83333333333333393, 1.299038105676657340 ) ) ;
#99451=CARTESIAN_POINT ( 'NONE',  ( 0.7500000000000006661, 13.19791666734946389, -1.299038105676657340 ) ) ;
#99507=CARTESIAN_POINT ( 'NONE',  ( 0.000000000000000000, 13.49999999999999822, 0.000000000000000000 ) ) ;
#99626=CARTESIAN_POINT ( 'NONE',  ( -1.402722028335470661, 13.31903653030363266, -0.2864402455888475085 ) ) ;
#99670=CARTESIAN_POINT ( 'NONE',  ( 0.7500000000000006661, 10.69791666734946212, -1.299038105676657340 ) ) ;
#99678=CARTESIAN_POINT ( 'NONE',  ( 2.449293598294706414E-16, 0.000000000000000000, -2.000000000000000000 ) ) ;
#99685=CARTESIAN_POINT ( 'NONE',  ( 4.344593448898664693E-13, 13.36537488277823371, -1.375075632470054154 ) ) ;
#99735=CARTESIAN_POINT ( 'NONE',  ( -0.6823417656250039265, 12.31770833367473017, -1.181850606188755259 ) ) ;
#99770=CARTESIAN_POINT ( 'NONE',  ( 1.367928747935657885, 13.31884955369513968, 0.3977952243826033407 ) ) ;
#99891=CARTESIAN_POINT ( 'NONE',  ( 0.6823417656249934904, 12.00520833367473017, 1.181850606188764807 ) ) ;
#99916=CARTESIAN_POINT ( 'NONE',  ( 0.6823417656249969321, 15.27604166700806410, -1.181850606188757036 ) ) ;
#99954=CARTESIAN_POINT ( 'NONE',  ( -1.364683531250010295, 10.44270833367473017, 0.7879004041258445001 ) ) ;
#99995=CARTESIAN_POINT ( 'NONE',  ( 1.499999999999993117, 8.885416667349462116, 0.8660254037844409281 ) ) ;
#100145=EDGE_LOOP ( 'NONE', ( #179899, #145285, #126338, #18515 ) ) ;
#100199=CARTESIAN_POINT ( 'NONE',  ( -1.364683531250000748, 13.92187500034140157, 0.000000000000000000 ) ) ;
#100239=ORIENTED_EDGE ( 'NONE', *, *, #173052, .T. ) ;
#100309=AXIS2_PLACEMENT_3D ( 'NONE', #39959, #186180, #24748 ) ;
#100334=ORIENTED_EDGE ( 'NONE', *, *, #191341, .F. ) ;
#100376=CARTESIAN_POINT ( 'NONE',  ( 0.7500000000000006661, 13.11458333401613352, 1.299038105676657340 ) ) ;
#100390=CARTESIAN_POINT ( 'NONE',  ( -0.7500000000000006661, 10.95833333333333393, -1.299038105676657340 ) ) ;
#100394=CARTESIAN_POINT ( 'NONE',  ( 0.6823417656249969321, 15.33854166700806410, -1.181850606188757036 ) ) ;
#100435=CARTESIAN_POINT ( 'NONE',  ( 1.364683531249996529, 11.02604166700807120, 0.7879004041258403923 ) ) ;
#100446=ORIENTED_EDGE ( 'NONE', *, *, #28580, .F. ) ;
#100469=CARTESIAN_POINT ( 'NONE',  ( 1.220146605508150803E-14, 9.937500000000000000, -1.499999999999998446 ) ) ;
#100508=CARTESIAN_POINT ( 'NONE',  ( 1.500000000000001332, 12.90625000068279604, 0.000000000000000000 ) ) ;
#100598=CARTESIAN_POINT ( 'NONE',  ( 0.6823417656249969321, 13.77604166700806232, -1.181850606188757036 ) ) ;
#100650=CARTESIAN_POINT ( 'NONE',  ( -0.6823417656250039265, 12.56770833367473017, -1.181850606188755259 ) ) ;
#100690=ORIENTED_EDGE ( 'NONE', *, *, #174144, .T. ) ;
#100708=ORIENTED_EDGE ( 'NONE', *, *, #91462, .T. ) ;
#100761=VERTEX_POINT ( 'NONE', #77538 ) ;
#100769=CARTESIAN_POINT ( 'NONE',  ( 0.000000000000000000, 13.49999999999999822, 0.000000000000000000 ) ) ;
#100784=CARTESIAN_POINT ( 'NONE',  ( -1.154700538379266339, -2.500000000000002220, 2.602085213965210642E-15 ) ) ;
#100792=CARTESIAN_POINT ( 'NONE',  ( 1.364683531249997417, 11.73437500034139802, 2.602085213965210642E-15 ) ) ;
#100939=CARTESIAN_POINT ( 'NONE',  ( 1.364683531249996529, 11.77604166700806410, 0.7879004041258405033 ) ) ;
#100966=EDGE_CURVE ( 'NONE', #178226, #178739, #59155, .T. ) ;
#100990=CARTESIAN_POINT ( 'NONE',  ( -1.364683531250010740, 13.13020833367472839, 0.7879004041258445001 ) ) ;
#101006=CARTESIAN_POINT ( 'NONE',  ( -1.402160292154681736E-14, 9.234375000341398021, 1.575800808251682339 ) ) ;
#101047=CARTESIAN_POINT ( 'NONE',  ( 0.7500000000000006661, 9.114583334016129967, 1.299038105676657340 ) ) ;
#101092=VECTOR ( 'NONE', #202544, 1000.000000000000000 ) ;
#101111=DIRECTION ( 'NONE',  ( 0.000000000000000000, 0.000000000000000000, -1.000000000000000000 ) ) ;
#101258=CARTESIAN_POINT ( 'NONE',  ( 0.6823417656249934904, 15.00520833367473195, 1.181850606188764807 ) ) ;
#101300=ORIENTED_EDGE ( 'NONE', *, *, #36782, .T. ) ;
#101373=CARTESIAN_POINT ( 'NONE',  ( 0.4019237886466847653, 12.85491455036742892, 1.499999999999997113 ) ) ;
#101442=PLANE ( 'NONE',  #172979 ) ;
#101449=CARTESIAN_POINT ( 'NONE',  ( -0.6823417656250003738, 12.15104166700806054, 1.181850606188754593 ) ) ;
#101455=CARTESIAN_POINT ( 'NONE',  ( -1.500000000000015099, 9.229166666666667851, -0.8660254037844309360 ) ) ;
#101505=CARTESIAN_POINT ( 'NONE',  ( 1.364683531249997417, 9.796875000341396245, 2.602085213965210642E-15 ) ) ;
#101577=CARTESIAN_POINT ( 'NONE',  ( -1.500000000000001110, 13.05208333401612997, 0.8660254037844419273 ) ) ;
#101587=CARTESIAN_POINT ( 'NONE',  ( -1.500000000000001110, 12.77083333333333215, 0.8660254037844418162 ) ) ;
#101667=CARTESIAN_POINT ( 'NONE',  ( 1.364683531250000303, 13.00520833367473550, -0.7879004041258355073 ) ) ;
#101719=CARTESIAN_POINT ( 'NONE',  ( -1.364683531250000748, 12.60937500034139980, 0.000000000000000000 ) ) ;
#101806=CARTESIAN_POINT ( 'NONE',  ( 0.000000000000000000, 13.49999999999999822, 0.000000000000000000 ) ) ;
#101807=CARTESIAN_POINT ( 'NONE',  ( 0.000000000000000000, 6.161115872820241535, 0.000000000000000000 ) ) ;
#101849=CIRCLE ( 'NONE', #8460, 1.249999999999999778 ) ;
#101867=CARTESIAN_POINT ( 'NONE',  ( 0.6823417656249969321, 11.77604166700806054, -1.181850606188757036 ) ) ;
#101900=CARTESIAN_POINT ( 'NONE',  ( 1.239108386966929265, 13.33839687343696490, -0.6814443383427297718 ) ) ;
#102020=CARTESIAN_POINT ( 'NONE',  ( -1.364683531250010295, 11.69270833367473017, 0.7879004041258445001 ) ) ;
#102072=CARTESIAN_POINT ( 'NONE',  ( 0.4019237886466816012, 11.70758545099816494, -1.499999999999998668 ) ) ;
#102085=CARTESIAN_POINT ( 'NONE',  ( -0.6823417656250003738, 9.463541667008065872, 1.181850606188754593 ) ) ;
#102112=CARTESIAN_POINT ( 'NONE',  ( 0.7500000000000006661, 12.16666666666666607, -1.299038105676657340 ) ) ;
#102126=CARTESIAN_POINT ( 'NONE',  ( 1.499999999999993117, 9.135416667349463893, 0.8660254037844409281 ) ) ;
#102291=ORIENTED_EDGE ( 'NONE', *, *, #66894, .T. ) ;
#102315=CARTESIAN_POINT ( 'NONE',  ( 3.834746474454188013E-15, 8.812500000000000000, 1.500000000000001554 ) ) ;
#102327=CARTESIAN_POINT ( 'NONE',  ( 1.499999999999996891, 12.89583333333333215, -0.8660254037844378194 ) ) ;
#102328=CARTESIAN_POINT ( 'NONE',  ( 1.364683531250000303, 13.31770833367472839, -0.7879004041258355073 ) ) ;
#102438=AXIS2_PLACEMENT_3D ( 'NONE', #188570, #42350, #208012 ) ;
#102483=DIRECTION ( 'NONE',  ( 0.000000000000000000, 0.000000000000000000, -1.000000000000000000 ) ) ;
#102502=CARTESIAN_POINT ( 'NONE',  ( 0.000000000000000000, 13.49999999999999822, 0.000000000000000000 ) ) ;
#102519=CARTESIAN_POINT ( 'NONE',  ( 0.6823417656249934904, 11.94270833367473017, 1.181850606188764807 ) ) ;
#102525=CARTESIAN_POINT ( 'NONE',  ( -1.500000000000008216, 9.500000000000001776, 3.469446951953614189E-15 ) ) ;
#102575=CARTESIAN_POINT ( 'NONE',  ( -8.012344526598182026E-15, 9.609375000341398021, -1.575800808251669460 ) ) ;
#102636=CARTESIAN_POINT ( 'NONE',  ( 0.7500000000000006661, 8.583333333333332149, 1.299038105676657340 ) ) ;
#102643=ORIENTED_EDGE ( 'NONE', *, *, #129790, .T. ) ;
#102650=CARTESIAN_POINT ( 'NONE',  ( 0.000000000000000000, 0.000000000000000000, 0.000000000000000000 ) ) ;
#102653=CARTESIAN_POINT ( 'NONE',  ( -0.7500000000000006661, 12.48958333401613352, -1.299038105676657340 ) ) ;
#102662=CARTESIAN_POINT ( 'NONE',  ( -1.500000000000008216, 12.74999999999999822, 3.469446951953614189E-15 ) ) ;
#102725=CARTESIAN_POINT ( 'NONE',  ( 1.499912825862921295, 3.250189846351735135, 0.08469158891783865051 ) ) ;
#102732=ORIENTED_EDGE ( 'NONE', *, *, #38945, .T. ) ;
#102742=CARTESIAN_POINT ( 'NONE',  ( 1.364683531250000303, 13.75520833367473195, -0.7879004041258355073 ) ) ;
#102754=VERTEX_POINT ( 'NONE', #148288 ) ;
#102785=CARTESIAN_POINT ( 'NONE',  ( -1.500000000000001110, 13.52083333333332682, 0.8660254037844419273 ) ) ;
#102793=CARTESIAN_POINT ( 'NONE',  ( -0.6823417656250003738, 11.40104166700806765, 1.181850606188754593 ) ) ;
#102828=CARTESIAN_POINT ( 'NONE',  ( -0.5773502691896261751, -2.500000000000002220, -0.9999999999999991118 ) ) ;
#102860=CARTESIAN_POINT ( 'NONE',  ( -1.500000000000008216, 10.25000000000000178, 3.469446951953614189E-15 ) ) ;
#102868=ORIENTED_EDGE ( 'NONE', *, *, #87783, .T. ) ;
#102884=ORIENTED_EDGE ( 'NONE', *, *, #100966, .T. ) ;
#102928=FACE_OUTER_BOUND ( 'NONE', #9733, .T. ) ;
#102936=CARTESIAN_POINT ( 'NONE',  ( 0.6823417656249934904, 11.94270833367473017, 1.181850606188764807 ) ) ;
#102993=ORIENTED_EDGE ( 'NONE', *, *, #129717, .F. ) ;
#102994=( BOUNDED_CURVE ( )  B_SPLINE_CURVE ( 2, ( #141455, #107912, #186941, #155528, #104649, #207462, #7108, #123128, #189087 ),
 .UNSPECIFIED., .F., .T. ) 
 B_SPLINE_CURVE_WITH_KNOTS ( ( 3, 2, 2, 2, 3 ),
 ( 0.9375000000000000000, 0.9404761904761904656, 0.9464285714285713969, 0.9523809523809523281, 0.9553571428571427937 ),
 .UNSPECIFIED. ) 
 CURVE ( )  GEOMETRIC_REPRESENTATION_ITEM ( )  RATIONAL_B_SPLINE_CURVE ( ( 0.9330127018922194093, 0.9330127018922194093, 1.000000000000000000, 0.8660254037844387076, 1.000000000000000000, 0.8660254037844387076, 1.000000000000000000, 0.9330127018922206306, 0.9330127018922194093 ) ) 
 REPRESENTATION_ITEM ( '' )  );
#102999=ORIENTED_EDGE ( 'NONE', *, *, #41033, .T. ) ;
#103088=CARTESIAN_POINT ( 'NONE',  ( -0.6823417656250039265, 11.63020833367473017, -1.181850606188755259 ) ) ;
#103115=CARTESIAN_POINT ( 'NONE',  ( 0.6823417656249934904, 15.19270833367473372, 1.181850606188764807 ) ) ;
#103154=CARTESIAN_POINT ( 'NONE',  ( -1.402160292154681736E-14, 9.484375000341398021, 1.575800808251682339 ) ) ;
#103172=ORIENTED_EDGE ( 'NONE', *, *, #142087, .F. ) ;
#103198=CARTESIAN_POINT ( 'NONE',  ( -6.009258394948636914E-15, 8.718750000682796042, -1.732050807568875195 ) ) ;
#103292=ORIENTED_EDGE ( 'NONE', *, *, #63733, .T. ) ;
#103333=CARTESIAN_POINT ( 'NONE',  ( 0.4019237886466847653, 12.57366454968463110, 1.499999999999997113 ) ) ;
#103348=VERTEX_POINT ( 'NONE', #160011 ) ;
#103402=CARTESIAN_POINT ( 'NONE',  ( 1.364683531250000303, 12.81770833367473372, -0.7879004041258355073 ) ) ;
#103483=EDGE_CURVE ( 'NONE', #124391, #65269, #187731, .T. ) ;
#103489=CARTESIAN_POINT ( 'NONE',  ( -1.115562610750309283E-14, 11.09375000068279427, 1.500000000000001554 ) ) ;
#103530=CARTESIAN_POINT ( 'NONE',  ( -1.382971907303421233, 4.316406942282006831, -0.2136448034514826788 ) ) ;
#103555=CARTESIAN_POINT ( 'NONE',  ( 0.000000000000000000, 13.49999999999999822, 0.000000000000000000 ) ) ;
#103594=CARTESIAN_POINT ( 'NONE',  ( -1.364683531250000748, 11.60937500034139802, 0.000000000000000000 ) ) ;
#103598=CARTESIAN_POINT ( 'NONE',  ( -1.402160292154681736E-14, 10.31250000000000178, 1.732050807568881190 ) ) ;
#103643=ORIENTED_EDGE ( 'NONE', *, *, #99125, .T. ) ;
#103653=CARTESIAN_POINT ( 'NONE',  ( 1.364683531249996529, 9.276041667008062319, 0.7879004041258403923 ) ) ;
#103658=MECHANICAL_DESIGN_GEOMETRIC_PRESENTATION_REPRESENTATION('',(#69140),#110683);
#103722=DIRECTION ( 'NONE',  ( 0.000000000000000000, 0.000000000000000000, -1.000000000000000000 ) ) ;
#103725=CARTESIAN_POINT ( 'NONE',  ( -6.009258394948636914E-15, 10.71875000068279959, -1.732050807568875195 ) ) ;
#103775=CARTESIAN_POINT ( 'NONE',  ( 1.264911064067349322, 3.816124033181332642, 0.5000000000000056621 ) ) ;
#103813=CARTESIAN_POINT ( 'NONE',  ( -0.6823417656250003738, 12.65104166700806232, 1.181850606188754593 ) ) ;
#103856=CARTESIAN_POINT ( 'NONE',  ( 0.7500000000000006661, 13.08333333333333570, 1.299038105676657340 ) ) ;
#103863=CARTESIAN_POINT ( 'NONE',  ( -8.012344526598182026E-15, 12.04687500034140335, -1.575800808251669460 ) ) ;
#103870=ORIENTED_EDGE ( 'NONE', *, *, #32262, .T. ) ;
#103952=DIRECTION ( 'NONE',  ( 0.000000000000000000, -1.000000000000000000, 0.000000000000000000 ) ) ;
#103958=PLANE ( 'NONE',  #39693 ) ;
#103979=CARTESIAN_POINT ( 'NONE',  ( -0.7500000000000006661, 14.98958333401613530, -1.299038105676657340 ) ) ;
#104011=CARTESIAN_POINT ( 'NONE',  ( 1.364683531250000303, 11.25520833367473550, -0.7879004041258355073 ) ) ;
#104082=EDGE_CURVE ( 'NONE', #169050, #28009, #209860, .T. ) ;
#104161=CARTESIAN_POINT ( 'NONE',  ( 1.364683531250000303, 10.56770833367473195, -0.7879004041258355073 ) ) ;
#104175=ORIENTED_EDGE ( 'NONE', *, *, #173881, .F. ) ;
#104229=CARTESIAN_POINT ( 'NONE',  ( -0.6823417656250039265, 9.630208333674728394, -1.181850606188755259 ) ) ;
#104235=CARTESIAN_POINT ( 'NONE',  ( -1.407792700327074931, 4.233596129272890529, 0.5229849042009224735 ) ) ;
#104263=( BOUNDED_CURVE ( )  B_SPLINE_CURVE ( 2, ( #55327, #49204, #165073, #32943, #198614, #36929, #213787, #186375, #65410 ),
 .UNSPECIFIED., .F., .T. ) 
 B_SPLINE_CURVE_WITH_KNOTS ( ( 3, 2, 2, 2, 3 ),
 ( 0.3482142857142856429, 0.3511904761904761640, 0.3571428571428571508, 0.3630952380952380820, 0.3660714285714286031 ),
 .UNSPECIFIED. ) 
 CURVE ( )  GEOMETRIC_REPRESENTATION_ITEM ( )  RATIONAL_B_SPLINE_CURVE ( ( 0.9330127018922194093, 0.9330127018922180770, 1.000000000000000000, 0.8660254037844387076, 1.000000000000000000, 0.8660254037844387076, 1.000000000000000000, 0.9330127018922187432, 0.9330127018922194093 ) ) 
 REPRESENTATION_ITEM ( '' )  );
#104271=CARTESIAN_POINT ( 'NONE',  ( -0.7500000000000179856, 8.322916667349467446, 1.299038105676658228 ) ) ;
#104283=CARTESIAN_POINT ( 'NONE',  ( -1.364564222265963300, 3.685551582065023091, -0.6239050962422643121 ) ) ;
#104314=EDGE_CURVE ( 'NONE', #45033, #98073, #60671, .T. ) ;
#104336=CARTESIAN_POINT ( 'NONE',  ( 1.500000000000001332, 11.40625000068279427, 0.000000000000000000 ) ) ;
#104413=CARTESIAN_POINT ( 'NONE',  ( 1.364683531249997417, 15.29687500034139447, 2.602085213965210642E-15 ) ) ;
#104424=EDGE_LOOP ( 'NONE', ( #102732, #157732, #126100, #18798, #146364, #56376 ) ) ;
#104477=ADVANCED_FACE ( 'NONE', ( #23769 ), #172574, .T. ) ;
#104479=CARTESIAN_POINT ( 'NONE',  ( -1.402160292154681736E-14, 12.73437500034139980, 1.575800808251682339 ) ) ;
#104649=CARTESIAN_POINT ( 'NONE',  ( 1.500000000000001332, 8.875000000000001776, 0.000000000000000000 ) ) ;
#104650=CARTESIAN_POINT ( 'NONE',  ( 1.290813828370756866, 4.079998697030315924, 0.4579576469030108843 ) ) ;
#104669=CARTESIAN_POINT ( 'NONE',  ( -1.364683531250014514, 12.08854166700806765, -0.7879004041258335089 ) ) ;
#104673=CARTESIAN_POINT ( 'NONE',  ( -2.788906526875773208E-15, 9.437499999999998224, -1.499999999999998446 ) ) ;
#104675=CARTESIAN_POINT ( 'NONE',  ( -1.500000000000015099, 9.979166666666671404, -0.8660254037844309360 ) ) ;
#104727=CARTESIAN_POINT ( 'NONE',  ( -1.364683531250000748, 9.171875000341403350, 0.000000000000000000 ) ) ;
#104789=DIRECTION ( 'NONE',  ( 0.000000000000000000, -1.000000000000000000, 0.000000000000000000 ) ) ;
#104840=VERTEX_POINT ( 'NONE', #116897 ) ;
#104850=ADVANCED_FACE ( 'NONE', ( #53976 ), #183963, .T. ) ;
#104887=CARTESIAN_POINT ( 'NONE',  ( 0.6823417656249969321, 13.27604166700806232, -1.181850606188757036 ) ) ;
#104935=CARTESIAN_POINT ( 'NONE',  ( -6.009258394948636914E-15, 14.18750000000000355, -1.732050807568875195 ) ) ;
#104941=CARTESIAN_POINT ( 'NONE',  ( 1.364683531250000303, 11.50520833367472839, -0.7879004041258355073 ) ) ;
#104977=EDGE_CURVE ( 'NONE', #210054, #195556, #37722, .T. ) ;
#104987=CARTESIAN_POINT ( 'NONE',  ( -0.6823417656250003738, 12.71354166700806942, 1.181850606188754593 ) ) ;
#105013=CARTESIAN_POINT ( 'NONE',  ( -1.247849810309911822, 13.37576698399836594, 0.5524780460566154350 ) ) ;
#105015=ORIENTED_EDGE ( 'NONE', *, *, #23723, .F. ) ;
#105027=FACE_OUTER_BOUND ( 'NONE', #121198, .T. ) ;
#105090=CARTESIAN_POINT ( 'NONE',  ( 0.6823417656249969321, 10.77604166700806765, -1.181850606188757036 ) ) ;
#105136=CARTESIAN_POINT ( 'NONE',  ( -1.500000000000001110, 11.80208333401612997, 0.8660254037844418162 ) ) ;
#105224=ORIENTED_EDGE ( 'NONE', *, *, #68596, .T. ) ;
#105237=CARTESIAN_POINT ( 'NONE',  ( -8.012344526598182026E-15, 11.10937500034139802, -1.575800808251669460 ) ) ;
#105246=CARTESIAN_POINT ( 'NONE',  ( -1.335881052060646557, 13.37576698399828423, -0.3319583403691591106 ) ) ;
#105263=CARTESIAN_POINT ( 'NONE',  ( -1.364683531250000748, 14.10937500034140157, 0.000000000000000000 ) ) ;
#105307=CARTESIAN_POINT ( 'NONE',  ( 0.6823417656249934904, 9.255208333674728394, 1.181850606188764807 ) ) ;
#105310=ADVANCED_FACE ( 'NONE', ( #153729, #122388 ), #6382, .F. ) ;
#105355=CARTESIAN_POINT ( 'NONE',  ( -1.364683531250014514, 13.83854166700806765, -0.7879004041258335089 ) ) ;
#105366=CARTESIAN_POINT ( 'NONE',  ( -1.354873262373948339, 3.923680654322774686, -0.6436764175676684685 ) ) ;
#105381=EDGE_CURVE ( 'NONE', #133382, #180856, #74508, .T. ) ;
#105461=VECTOR ( 'NONE', #35951, 1000.000000000000000 ) ;
#105500=CARTESIAN_POINT ( 'NONE',  ( -1.364683531250010295, 14.94270833367472839, 0.7879004041258445001 ) ) ;
#105508=CARTESIAN_POINT ( 'NONE',  ( -2.788906526875773208E-15, 12.46875000068279782, -1.499999999999998446 ) ) ;
#105545=CARTESIAN_POINT ( 'NONE',  ( 1.220146605508150803E-14, 9.718750000682797818, -1.499999999999998446 ) ) ;
#105560=CARTESIAN_POINT ( 'NONE',  ( -1.364683531250000748, 13.67187500034139980, 0.000000000000000000 ) ) ;
#105563=EDGE_CURVE ( 'NONE', #57617, #29485, #118837, .T. ) ;
#105761=DIRECTION ( 'NONE',  ( 0.000000000000000000, -0.3940140829290787461, 0.9191044023687172659 ) ) ;
#105763=CARTESIAN_POINT ( 'NONE',  ( -1.364683531250000748, 10.60937500034139802, 0.000000000000000000 ) ) ;
#105769=CARTESIAN_POINT ( 'NONE',  ( 0.7500000000000006661, 10.08333333333333215, 1.299038105676657340 ) ) ;
#105792=CARTESIAN_POINT ( 'NONE',  ( -1.500000000000008216, 8.781250000682797818, 3.469446951953614189E-15 ) ) ;
#105841=CARTESIAN_POINT ( 'NONE',  ( -0.5773502691896470473, -2.500000000000002220, 0.9999999999999991118 ) ) ;
#106015=CARTESIAN_POINT ( 'NONE',  ( 1.382971907303421233, 3.383593057718003561, -0.2136448034514799310 ) ) ;
#106036=CARTESIAN_POINT ( 'NONE',  ( -1.500000000000008216, 13.74999999999999822, 3.469446951953614189E-15 ) ) ;
#106041=CARTESIAN_POINT ( 'NONE',  ( -0.6823417656250039265, 10.81770833367473550, -1.181850606188755259 ) ) ;
#106068=CARTESIAN_POINT ( 'NONE',  ( 0.000000000000000000, 13.49999999999999822, 0.000000000000000000 ) ) ;
#106087=CARTESIAN_POINT ( 'NONE',  ( 1.364683531249996529, 12.77604166700806587, 0.7879004041258403923 ) ) ;
#106093=CARTESIAN_POINT ( 'NONE',  ( 0.000000000000000000, 14.00000000000000533, 0.000000000000000000 ) ) ;
#106115=CARTESIAN_POINT ( 'NONE',  ( 1.364683531249996529, 12.96354166700806410, 0.7879004041258403923 ) ) ;
#106153=CARTESIAN_POINT ( 'NONE',  ( -1.500000000000008216, 15.03125000068279782, 3.469446951953614189E-15 ) ) ;
#106188=CARTESIAN_POINT ( 'NONE',  ( -1.364683531250000748, 10.10937500034139802, 0.000000000000000000 ) ) ;
#106246=( BOUNDED_CURVE ( )  B_SPLINE_CURVE ( 2, ( #125335, #142603, #139385, #60246, #77565, #27753, #172954, #143687, #141550 ),
 .UNSPECIFIED., .F., .T. ) 
 B_SPLINE_CURVE_WITH_KNOTS ( ( 3, 2, 2, 2, 3 ),
 ( 0.3303571428571428492, 0.3333333333333333148, 0.3392857142857143016, 0.3452380952380952328, 0.3482142857142856429 ),
 .UNSPECIFIED. ) 
 CURVE ( )  GEOMETRIC_REPRESENTATION_ITEM ( )  RATIONAL_B_SPLINE_CURVE ( ( 0.9330127018922194093, 0.9330127018922194093, 1.000000000000000000, 0.8660254037844387076, 1.000000000000000000, 0.8660254037844387076, 1.000000000000000000, 0.9330127018922206306, 0.9330127018922194093 ) ) 
 REPRESENTATION_ITEM ( '' )  );
#106284=LINE ( 'NONE', #172305, #21719 ) ;
#106286=CARTESIAN_POINT ( 'NONE',  ( 0.4019237886466778820, 9.354914550367425363, 1.500000000000001554 ) ) ;
#106288=CARTESIAN_POINT ( 'NONE',  ( -2.788906526875773208E-15, 10.93750000000000178, -1.499999999999998446 ) ) ;
#106295=CARTESIAN_POINT ( 'NONE',  ( -1.406531590435020185, 3.336988665940368470, -0.01155683023987377767 ) ) ;
#106337=CARTESIAN_POINT ( 'NONE',  ( -1.364683531250000748, 10.42187500034139802, 0.000000000000000000 ) ) ;
#106362=CARTESIAN_POINT ( 'NONE',  ( -1.364683531250000748, 14.35937500034140157, 0.000000000000000000 ) ) ;
#106384=CARTESIAN_POINT ( 'NONE',  ( -1.286813488861816790, 3.613591550242559070, -0.5514626414212303596 ) ) ;
#106392=CARTESIAN_POINT ( 'NONE',  ( 1.499999999999996891, 11.67708333401613174, -0.8660254037844378194 ) ) ;
#106394=CARTESIAN_POINT ( 'NONE',  ( -2.788906526875773208E-15, 12.18750000000000000, -1.499999999999998446 ) ) ;
#106406=CARTESIAN_POINT ( 'NONE',  ( -0.7500000000000179856, 14.54166666666666785, 1.299038105676658228 ) ) ;
#106420=LINE ( 'NONE', #156200, #35806 ) ;
#106452=CARTESIAN_POINT ( 'NONE',  ( -1.364683531250010295, 13.88020833367473195, 0.7879004041258445001 ) ) ;
#106546=CARTESIAN_POINT ( 'NONE',  ( -0.4019237886466871523, 9.198664549684631098, -1.499999999999998668 ) ) ;
#106592=CARTESIAN_POINT ( 'NONE',  ( -1.402160292154681736E-14, 14.73437500034139980, 1.575800808251682339 ) ) ;
#106655=CARTESIAN_POINT ( 'NONE',  ( 1.364683531249996529, 13.27604166700806410, 0.7879004041258405033 ) ) ;
#106844=CARTESIAN_POINT ( 'NONE',  ( 1.364683531249996529, 10.71354166700806942, 0.7879004041258403923 ) ) ;
#106850=CARTESIAN_POINT ( 'NONE',  ( -1.500000000000008216, 9.000000000000001776, 3.469446951953614189E-15 ) ) ;
#106957=DIRECTION ( 'NONE',  ( 0.000000000000000000, 0.000000000000000000, -1.000000000000000000 ) ) ;
#107051=CARTESIAN_POINT ( 'NONE',  ( 0.7500000000000006661, 12.61458333401613352, 1.299038105676657340 ) ) ;
#107076=EDGE_CURVE ( 'NONE', #205543, #161998, #41097, .T. ) ;
#107113=CARTESIAN_POINT ( 'NONE',  ( 0.7500000000000006661, 12.41666666666666607, -1.299038105676657340 ) ) ;
#107119=CARTESIAN_POINT ( 'NONE',  ( -8.012344526598182026E-15, 10.29687500034139447, -1.575800808251669460 ) ) ;
#107163=CARTESIAN_POINT ( 'NONE',  ( 0.6823417656249969321, 12.08854166700806765, -1.181850606188757036 ) ) ;
#107175=DIRECTION ( 'NONE',  ( 0.000000000000000000, -1.000000000000000000, 0.000000000000000000 ) ) ;
#107191=CARTESIAN_POINT ( 'NONE',  ( -1.364683531250000748, 13.10937500034139980, 0.000000000000000000 ) ) ;
#107266=CARTESIAN_POINT ( 'NONE',  ( -1.364683531250010295, 10.63020833367473195, 0.7879004041258445001 ) ) ;
#107383=CARTESIAN_POINT ( 'NONE',  ( -0.4019237886467001974, 11.05133545031537068, 1.500000000000001998 ) ) ;
#107417=CARTESIAN_POINT ( 'NONE',  ( 1.364683531249997417, 10.29687500034139802, 2.602085213965210642E-15 ) ) ;
#107424=CARTESIAN_POINT ( 'NONE',  ( -1.368157835711294013, 13.37576698399829134, -0.1511644340184340740 ) ) ;
#107425=FACE_BOUND ( 'NONE', #128766, .T. ) ;
#107443=CARTESIAN_POINT ( 'NONE',  ( -0.6823417656250039265, 14.56770833367473195, -1.181850606188755259 ) ) ;
#107489=CARTESIAN_POINT ( 'NONE',  ( 1.500000000000001332, 15.37500000000000000, 0.000000000000000000 ) ) ;
#107531=CARTESIAN_POINT ( 'NONE',  ( -1.364683531250010295, 14.38020833367473372, 0.7879004041258445001 ) ) ;
#107542=DIRECTION ( 'NONE',  ( 0.000000000000000000, -1.000000000000000000, 0.000000000000000000 ) ) ;
#107570=DIRECTION ( 'NONE',  ( 0.000000000000000000, -1.000000000000000000, 0.000000000000000000 ) ) ;
#107599=ORIENTED_EDGE ( 'NONE', *, *, #158884, .F. ) ;
#107676=CARTESIAN_POINT ( 'NONE',  ( -0.6823417656250039265, 13.13020833367473017, -1.181850606188755259 ) ) ;
#107686=EDGE_LOOP ( 'NONE', ( #177600, #37019, #191347, #42007, #81610, #147876, #89515 ) ) ;
#107713=LINE ( 'NONE', #26382, #125564 ) ;
#107743=CARTESIAN_POINT ( 'NONE',  ( -8.012344526598182026E-15, 12.10937500034140157, -1.575800808251669460 ) ) ;
#107765=LINE ( 'NONE', #60009, #137094 ) ;
#107782=CARTESIAN_POINT ( 'NONE',  ( 1.499999999999997113, 10.67708333401613530, -0.8660254037844378194 ) ) ;
#107863=CARTESIAN_POINT ( 'NONE',  ( -1.309956906536927201, 4.151654029309398197, 0.4145166106152409768 ) ) ;
#107912=CARTESIAN_POINT ( 'NONE',  ( 0.4019237886466816012, 8.926335450315372455, -1.499999999999998668 ) ) ;
#107930=CARTESIAN_POINT ( 'NONE',  ( -0.6823417656250039265, 11.31770833367473728, -1.181850606188755259 ) ) ;
#107936=CARTESIAN_POINT ( 'NONE',  ( -1.500000000000001110, 8.770833333333337478, 0.8660254037844419273 ) ) ;
#107998=CARTESIAN_POINT ( 'NONE',  ( -1.364683531250014514, 15.15104166700806587, -0.7879004041258335089 ) ) ;
#108023=DIRECTION ( 'NONE',  ( 0.000000000000000000, 0.000000000000000000, -1.000000000000000000 ) ) ;
#108076=EDGE_CURVE ( 'NONE', #86666, #152917, #128882, .T. ) ;
#108147=CARTESIAN_POINT ( 'NONE',  ( -0.7500000000000179856, 10.54166666666667140, 1.299038105676658228 ) ) ;
#108168=ADVANCED_FACE ( 'NONE', ( #146146 ), #65897, .T. ) ;
#108188=CARTESIAN_POINT ( 'NONE',  ( 1.499999999999993117, 12.85416666666666785, 0.8660254037844409281 ) ) ;
#108195=CARTESIAN_POINT ( 'NONE',  ( -1.364683531250010295, 10.88020833367473372, 0.7879004041258445001 ) ) ;
#108205=ORIENTED_EDGE ( 'NONE', *, *, #91910, .F. ) ;
#108236=CARTESIAN_POINT ( 'NONE',  ( -1.402160292154681736E-14, 12.23437500034140513, 1.575800808251682339 ) ) ;
#108244=ORIENTED_EDGE ( 'NONE', *, *, #67112, .F. ) ;
#108296=DIRECTION ( 'NONE',  ( 0.000000000000000000, -1.000000000000000000, 0.000000000000000000 ) ) ;
#108339=CARTESIAN_POINT ( 'NONE',  ( -1.364683531250010295, 9.880208333674728394, 0.7879004041258445001 ) ) ;
#108350=CARTESIAN_POINT ( 'NONE',  ( 3.834746474454188013E-15, 8.843750000682797818, 1.500000000000001554 ) ) ;
#108356=ORIENTED_EDGE ( 'NONE', *, *, #66919, .T. ) ;
#108442=CARTESIAN_POINT ( 'NONE',  ( -0.5773502691896470473, -2.500000000000002220, 0.9999999999999991118 ) ) ;
#108473=CARTESIAN_POINT ( 'NONE',  ( 0.7500000000000006661, 10.36458333401613174, 1.299038105676657340 ) ) ;
#108488=CARTESIAN_POINT ( 'NONE',  ( 0.6823417656249934904, 9.255208333674728394, 1.181850606188764807 ) ) ;
#108526=CARTESIAN_POINT ( 'NONE',  ( 0.4019237886466816012, 10.42633545031537423, -1.499999999999998668 ) ) ;
#108551=CARTESIAN_POINT ( 'NONE',  ( -1.402160292154681736E-14, 14.81249999999999645, 1.732050807568881190 ) ) ;
#108558=CARTESIAN_POINT ( 'NONE',  ( -1.364853456228725115, 4.017025827590854803, -0.6233480900563461713 ) ) ;
#108588=CARTESIAN_POINT ( 'NONE',  ( 1.154700538379228147, -2.500000000000002220, -1.734723475976807094E-15 ) ) ;
#108597=CARTESIAN_POINT ( 'NONE',  ( 1.364683531249996529, 14.21354166700806942, 0.7879004041258405033 ) ) ;
#108680=ORIENTED_EDGE ( 'NONE', *, *, #75612, .F. ) ;
#108702=DIRECTION ( 'NONE',  ( 0.000000000000000000, 1.000000000000000000, 0.000000000000000000 ) ) ;
#108743=CARTESIAN_POINT ( 'NONE',  ( 1.364683531249996529, 14.27604166700806942, 0.7879004041258405033 ) ) ;
#108795=CYLINDRICAL_SURFACE ( 'NONE', #93019, 1.500000000000000222 ) ;
#108808=CARTESIAN_POINT ( 'NONE',  ( -1.364683531250014514, 11.65104166700806587, -0.7879004041258335089 ) ) ;
#108847=CARTESIAN_POINT ( 'NONE',  ( -0.7500000000000006661, 11.23958333401613174, -1.299038105676657340 ) ) ;
#108943=EDGE_CURVE ( 'NONE', #210699, #81951, #140953, .T. ) ;
#108951=DIRECTION ( 'NONE',  ( 0.000000000000000000, 0.000000000000000000, -1.000000000000000000 ) ) ;
#108990=CARTESIAN_POINT ( 'NONE',  ( -1.364683531250010740, 10.88020833367473372, 0.7879004041258445001 ) ) ;
#109021=CARTESIAN_POINT ( 'NONE',  ( -1.453605123272271094, 13.24045051524828942, -0.3701785320580647798 ) ) ;
#109113=ORIENTED_EDGE ( 'NONE', *, *, #67371, .F. ) ;
#109262=CARTESIAN_POINT ( 'NONE',  ( 1.500000000000001332, 12.37499999999999645, 0.000000000000000000 ) ) ;
#109267=CARTESIAN_POINT ( 'NONE',  ( -1.402160292154681736E-14, 10.17187500034139447, 1.575800808251682339 ) ) ;
#109278=CARTESIAN_POINT ( 'NONE',  ( -1.500000000000008216, 10.78125000068279249, 3.469446951953614189E-15 ) ) ;
#109304=CARTESIAN_POINT ( 'NONE',  ( -1.364683531250000748, 11.67187500034139802, 0.000000000000000000 ) ) ;
#109319=DIRECTION ( 'NONE',  ( 0.000000000000000000, 0.000000000000000000, -1.000000000000000000 ) ) ;
#109375=CARTESIAN_POINT ( 'NONE',  ( 0.7500000000000006661, 13.44791666734946389, -1.299038105676657340 ) ) ;
#109395=ORIENTED_EDGE ( 'NONE', *, *, #49580, .F. ) ;
#109411=CARTESIAN_POINT ( 'NONE',  ( 1.364683531249997417, 10.48437500034139802, 2.602085213965210642E-15 ) ) ;
#109510=DIRECTION ( 'NONE',  ( 0.5000000000000003331, 0.000000000000000000, 0.8660254037844383745 ) ) ;
#109527=EDGE_LOOP ( 'NONE', ( #166998, #195526 ) ) ;
#109555=CARTESIAN_POINT ( 'NONE',  ( -1.500000000000001110, 10.55208333401613530, 0.8660254037844418162 ) ) ;
#109562=CARTESIAN_POINT ( 'NONE',  ( 1.364683531250000303, 10.06770833367473017, -0.7879004041258355073 ) ) ;
#109569=CARTESIAN_POINT ( 'NONE',  ( -0.2233545620225162176, 13.28207115425022877, 1.458379360998039997 ) ) ;
#109582=CARTESIAN_POINT ( 'NONE',  ( -1.115562610750309283E-14, 9.093750000682799595, 1.500000000000001554 ) ) ;
#109587=CARTESIAN_POINT ( 'NONE',  ( 1.408835580989207914, 4.237373208279807457, 0.5203893312692566830 ) ) ;
#109632=CARTESIAN_POINT ( 'NONE',  ( 0.7500000000000006661, 14.83333333333333748, 1.299038105676657340 ) ) ;
#109675=CARTESIAN_POINT ( 'NONE',  ( -1.364683531250014514, 14.08854166700806942, -0.7879004041258335089 ) ) ;
#109685=CARTESIAN_POINT ( 'NONE',  ( -1.350180276725266415, 4.245934212466626612, -0.3120814641734330208 ) ) ;
#109767=EDGE_CURVE ( 'NONE', #95692, #45033, #153174, .T. ) ;
#109771=CARTESIAN_POINT ( 'NONE',  ( -1.364417678870916806, 4.013935251703865781, 0.6242711042719457648 ) ) ;
#109791=CARTESIAN_POINT ( 'NONE',  ( 1.350180276725264639, 3.454065787533412646, -0.3120814641734592776 ) ) ;
#109814=CARTESIAN_POINT ( 'NONE',  ( 0.6823417656249934904, 13.25520833367473195, 1.181850606188764807 ) ) ;
#109845=EDGE_CURVE ( 'NONE', #179060, #81951, #56934, .T. ) ;
#109852=VERTEX_POINT ( 'NONE', #189063 ) ;
#109877=CARTESIAN_POINT ( 'NONE',  ( -0.6823417656250039265, 11.38020833367473017, -1.181850606188755259 ) ) ;
#109894=ADVANCED_FACE ( 'NONE', ( #118792 ), #86232, .T. ) ;
#109919=CARTESIAN_POINT ( 'NONE',  ( -1.500000000000015099, 11.01041666734946389, -0.8660254037844309360 ) ) ;
#109960=ORIENTED_EDGE ( 'NONE', *, *, #35190, .T. ) ;
#109972=CARTESIAN_POINT ( 'NONE',  ( -0.4340096093344613104, 3.986747911422942714, -0.4851708347456849535 ) ) ;
#110040=CARTESIAN_POINT ( 'NONE',  ( -1.500343415223059695, 3.249252082317366508, -0.07855322731632197186 ) ) ;
#110056=CARTESIAN_POINT ( 'NONE',  ( -1.364683531250010740, 11.13020833367473372, 0.7879004041258445001 ) ) ;
#110063=CARTESIAN_POINT ( 'NONE',  ( 0.7500000000000006661, 8.666666666666669627, -1.299038105676657340 ) ) ;
#110148=VERTEX_POINT ( 'NONE', #206370 ) ;
#110270=DIRECTION ( 'NONE',  ( 0.000000000000000000, -1.000000000000000000, 0.000000000000000000 ) ) ;
#110299=DIRECTION ( 'NONE',  ( 0.000000000000000000, 0.000000000000000000, -1.000000000000000000 ) ) ;
#110321=CARTESIAN_POINT ( 'NONE',  ( -1.500000000000008216, 12.99999999999999822, 3.469446951953614189E-15 ) ) ;
#110327=CARTESIAN_POINT ( 'NONE',  ( 1.364683531249997417, 10.48437500034139802, 2.602085213965210642E-15 ) ) ;
#110366=CARTESIAN_POINT ( 'NONE',  ( -1.402160292154681736E-14, 11.73437500034140335, 1.575800808251682339 ) ) ;
#110436=CARTESIAN_POINT ( 'NONE',  ( -0.7500000000000006661, 14.23958333401613352, -1.299038105676657340 ) ) ;
#110470=CARTESIAN_POINT ( 'NONE',  ( -1.364683531250010295, 9.130208333674731946, 0.7879004041258445001 ) ) ;
#110491=EDGE_LOOP ( 'NONE', ( #79343, #113394, #92564, #44316 ) ) ;
#110531=ORIENTED_EDGE ( 'NONE', *, *, #63733, .F. ) ;
#110599=VERTEX_POINT ( 'NONE', #68372 ) ;
#110621=CARTESIAN_POINT ( 'NONE',  ( 1.364683531249997417, 9.296875000341403350, 2.602085213965210642E-15 ) ) ;
#110635=ORIENTED_EDGE ( 'NONE', *, *, #162793, .F. ) ;
#110683=( GEOMETRIC_REPRESENTATION_CONTEXT ( 3 ) GLOBAL_UNCERTAINTY_ASSIGNED_CONTEXT ( ( #57143 ) ) GLOBAL_UNIT_ASSIGNED_CONTEXT ( ( #178346, #11553, #162093 ) ) REPRESENTATION_CONTEXT ( 'NONE', 'WORKASPACE' ) );
#110731=CARTESIAN_POINT ( 'NONE',  ( 1.364683531250000303, 13.00520833367473550, -0.7879004041258355073 ) ) ;
#110744=CARTESIAN_POINT ( 'NONE',  ( -1.412279214364694724, 4.224281623699000399, 0.5092244867763746630 ) ) ;
#110818=CARTESIAN_POINT ( 'NONE',  ( -0.4019237886466933696, 12.30133545031537423, 1.500000000000005995 ) ) ;
#110847=CARTESIAN_POINT ( 'NONE',  ( 1.367350270964193593, 3.416621234749356528, -0.2578043790911870858 ) ) ;
#110873=CARTESIAN_POINT ( 'NONE',  ( -1.364683531250000748, 13.67187500034139980, 0.000000000000000000 ) ) ;
#110881=DIRECTION ( 'NONE',  ( 0.000000000000000000, -1.000000000000000000, 0.000000000000000000 ) ) ;
#110936=CARTESIAN_POINT ( 'NONE',  ( 0.6823417656249934904, 11.75520833367473017, 1.181850606188764807 ) ) ;
#110951=CARTESIAN_POINT ( 'NONE',  ( 0.000000000000000000, -2.500000000000002220, 0.000000000000000000 ) ) ;
#110979=CARTESIAN_POINT ( 'NONE',  ( -1.500000000000008216, 10.53125000068279249, 3.469446951953614189E-15 ) ) ;
#111101=CARTESIAN_POINT ( 'NONE',  ( -1.478132491927081960, 3.421797542362725153, -0.2687277897297897788 ) ) ;
#111106=EDGE_CURVE ( 'NONE', #100761, #161998, #106284, .T. ) ;
#111121=CARTESIAN_POINT ( 'NONE',  ( 1.364683531249997417, 9.984375000341398021, 2.602085213965210642E-15 ) ) ;
#111193=CARTESIAN_POINT ( 'NONE',  ( 1.220146605508150803E-14, 9.468750000682799595, -1.499999999999998446 ) ) ;
#111266=( LENGTH_UNIT ( ) NAMED_UNIT ( * ) SI_UNIT ( .MILLI., .METRE. ) );
#111388=CARTESIAN_POINT ( 'NONE',  ( -1.500000000000001110, 11.77083333333333570, 0.8660254037844419273 ) ) ;
#111393=CARTESIAN_POINT ( 'NONE',  ( -1.364683531250010295, 8.630208333674731946, 0.7879004041258445001 ) ) ;
#111428=CARTESIAN_POINT ( 'NONE',  ( -0.6823417656250039265, 12.63020833367473017, -1.181850606188755259 ) ) ;
#111494=CARTESIAN_POINT ( 'NONE',  ( -1.115562610750309283E-14, 9.843750000682801371, 1.500000000000001554 ) ) ;
#111499=CARTESIAN_POINT ( 'NONE',  ( -1.500000000000015099, 13.26041666734946567, -0.8660254037844309360 ) ) ;
#111533=CARTESIAN_POINT ( 'NONE',  ( 1.364683531249996529, 9.213541667008062319, 0.7879004041258405033 ) ) ;
#111541=CARTESIAN_POINT ( 'NONE',  ( 0.000000000000000000, 13.49999999999999822, 0.000000000000000000 ) ) ;
#111552=EDGE_LOOP ( 'NONE', ( #127980, #184223, #53964, #8228 ) ) ;
#111637=ORIENTED_EDGE ( 'NONE', *, *, #198065, .F. ) ;
#111685=CARTESIAN_POINT ( 'NONE',  ( 1.364683531250000303, 9.067708333674733723, -0.7879004041258355073 ) ) ;
#111713=CARTESIAN_POINT ( 'NONE',  ( -1.115562610750309283E-14, 11.56249999999999822, 1.500000000000001554 ) ) ;
#111800=CARTESIAN_POINT ( 'NONE',  ( -1.364683531250000748, 13.60937500034139980, 0.000000000000000000 ) ) ;
#111812=CARTESIAN_POINT ( 'NONE',  ( -1.476450096886795516, 4.272190093455678905, -0.2781497094537733195 ) ) ;
#111927=CARTESIAN_POINT ( 'NONE',  ( 1.318127287744129683, 3.538098647990162604, 0.3960634941688977451 ) ) ;
#111937=VERTEX_POINT ( 'NONE', #111494 ) ;
#111950=CARTESIAN_POINT ( 'NONE',  ( -1.364683531250010295, 13.69270833367473195, 0.7879004041258445001 ) ) ;
#112013=CARTESIAN_POINT ( 'NONE',  ( -8.012344526598182026E-15, 11.10937500034139802, -1.575800808251669460 ) ) ;
#112057=CARTESIAN_POINT ( 'NONE',  ( -1.500000000000001110, 9.552083334016128191, 0.8660254037844419273 ) ) ;
#112109=CARTESIAN_POINT ( 'NONE',  ( -0.4339943706424748138, 3.986694575294704723, 0.4851827343914845714 ) ) ;
#112159=CARTESIAN_POINT ( 'NONE',  ( 1.286956418854628525, 3.652345658002387196, 0.4592741676705694998 ) ) ;
#112177=CARTESIAN_POINT ( 'NONE',  ( -1.435188857121534545, 3.628165074272017065, 0.4528096192972221878 ) ) ;
#112195=CARTESIAN_POINT ( 'NONE',  ( -1.402160292154681736E-14, 9.921875000341399797, 1.575800808251682339 ) ) ;
#112237=ORIENTED_EDGE ( 'NONE', *, *, #49372, .T. ) ;
#112300=EDGE_CURVE ( 'NONE', #135057, #93531, #212047, .T. ) ;
#112303=CARTESIAN_POINT ( 'NONE',  ( -1.286813488861823895, 3.652992958535467238, -0.4595522011843558574 ) ) ;
#112326=ADVANCED_FACE ( 'NONE', ( #186008 ), #137300, .T. ) ;
#112334=SURFACE_STYLE_USAGE ( .BOTH. , #179409 ) ;
#112380=EDGE_LOOP ( 'NONE', ( #190927, #25642, #68968, #194488, #77783, #59814, #84175 ) ) ;
#112448=CARTESIAN_POINT ( 'NONE',  ( -1.500000000000015099, 10.97916666666666785, -0.8660254037844309360 ) ) ;
#112454=CARTESIAN_POINT ( 'NONE',  ( 1.364683531249996529, 9.713541667008064096, 0.7879004041258405033 ) ) ;
#112471=EDGE_CURVE ( 'NONE', #147411, #162878, #125923, .T. ) ;
#112490=CARTESIAN_POINT ( 'NONE',  ( 1.364683531249996529, 10.77604166700806942, 0.7879004041258403923 ) ) ;
#112561=CARTESIAN_POINT ( 'NONE',  ( 1.499999999999997113, 13.67708333401613352, -0.8660254037844378194 ) ) ;
#112562=ORIENTED_EDGE ( 'NONE', *, *, #113661, .F. ) ;
#112598=CARTESIAN_POINT ( 'NONE',  ( 1.364683531249997417, 8.984375000341396245, 2.602085213965210642E-15 ) ) ;
#112607=CARTESIAN_POINT ( 'NONE',  ( 1.220146605508150803E-14, 11.21875000068279249, -1.499999999999998446 ) ) ;
#112702=VERTEX_POINT ( 'NONE', #131801 ) ;
#112752=CARTESIAN_POINT ( 'NONE',  ( -1.046564900588939029, 13.26134948416639148, -1.059077843570422672 ) ) ;
#112756=ORIENTED_EDGE ( 'NONE', *, *, #96950, .T. ) ;
#112769=ORIENTED_EDGE ( 'NONE', *, *, #114112, .T. ) ;
#112805=CARTESIAN_POINT ( 'NONE',  ( 1.499999999999993117, 11.35416666666666785, 0.8660254037844408170 ) ) ;
#112831=VERTEX_POINT ( 'NONE', #56900 ) ;
#112844=CARTESIAN_POINT ( 'NONE',  ( -1.115562610750309283E-14, 9.812500000000000000, 1.500000000000001554 ) ) ;
#112854=DIRECTION ( 'NONE',  ( 0.000000000000000000, 0.000000000000000000, 1.000000000000000000 ) ) ;
#112863=CARTESIAN_POINT ( 'NONE',  ( -1.364683531250000748, 12.85937500034139980, 0.000000000000000000 ) ) ;
#112875=CARTESIAN_POINT ( 'NONE',  ( -1.449478204280063576, 4.332514689554293419, 0.3909668688984575535 ) ) ;
#112961=CARTESIAN_POINT ( 'NONE',  ( -2.788906526875773208E-15, 12.18750000000000178, -1.499999999999998446 ) ) ;
#113014=CARTESIAN_POINT ( 'NONE',  ( -0.6823417656250003738, 11.71354166700806765, 1.181850606188754593 ) ) ;
#113078=CARTESIAN_POINT ( 'NONE',  ( -1.402160292154681736E-14, 9.734375000341399797, 1.575800808251682339 ) ) ;
#113118=CARTESIAN_POINT ( 'NONE',  ( 0.7500000000000006661, 10.11458333401612997, 1.299038105676657340 ) ) ;
#113173=DIRECTION ( 'NONE',  ( 1.000000000000000000, 0.000000000000000000, 0.000000000000000000 ) ) ;
#113222=CARTESIAN_POINT ( 'NONE',  ( 1.493068410184935191, 4.435370284924327500, -0.1642227666888356197 ) ) ;
#113262=CARTESIAN_POINT ( 'NONE',  ( 0.6823417656249969321, 9.276041667008065872, -1.181850606188757036 ) ) ;
#113276=FACE_BOUND ( 'NONE', #1571, .T. ) ;
#113291=CARTESIAN_POINT ( 'NONE',  ( -1.119339255005453736E-13, 13.28612805825129151, 1.454322456996997470 ) ) ;
#113306=ORIENTED_EDGE ( 'NONE', *, *, #157961, .T. ) ;
#113335=CARTESIAN_POINT ( 'NONE',  ( 0.6823417656249934904, 14.00520833367473195, 1.181850606188764807 ) ) ;
#113369=FACE_OUTER_BOUND ( 'NONE', #33781, .T. ) ;
#113394=ORIENTED_EDGE ( 'NONE', *, *, #62155, .T. ) ;
#113403=( NAMED_UNIT ( * ) SI_UNIT ( $, .STERADIAN. ) SOLID_ANGLE_UNIT ( ) );
#113519=CARTESIAN_POINT ( 'NONE',  ( -1.402160292154681736E-14, 11.56249999999999822, 1.732050807568881190 ) ) ;
#113526=CARTESIAN_POINT ( 'NONE',  ( 1.364683531249996529, 9.463541667008062319, 0.7879004041258405033 ) ) ;
#113529=ORIENTED_EDGE ( 'NONE', *, *, #172644, .T. ) ;
#113562=CARTESIAN_POINT ( 'NONE',  ( -1.364683531250010740, 10.44270833367473195, 0.7879004041258445001 ) ) ;
#113572=VERTEX_POINT ( 'NONE', #178030 ) ;
#113599=CARTESIAN_POINT ( 'NONE',  ( -1.115562610750309283E-14, 10.06250000000000000, 1.500000000000001554 ) ) ;
#113634=CARTESIAN_POINT ( 'NONE',  ( -0.7500000000000179856, 14.07291666734946567, 1.299038105676658228 ) ) ;
#113647=ORIENTED_EDGE ( 'NONE', *, *, #59329, .T. ) ;
#113661=EDGE_CURVE ( 'NONE', #202706, #40283, #39378, .T. ) ;
#113668=CARTESIAN_POINT ( 'NONE',  ( -0.6823417656250039265, 9.067708333674733723, -1.181850606188755259 ) ) ;
#113677=CARTESIAN_POINT ( 'NONE',  ( -1.115562610750309283E-14, 11.09375000068279427, 1.500000000000001554 ) ) ;
#113777=CARTESIAN_POINT ( 'NONE',  ( -1.402160292154681736E-14, 11.92187500034140157, 1.575800808251682339 ) ) ;
#113822=CARTESIAN_POINT ( 'NONE',  ( 0.6823417656249934904, 8.505208333674733723, 1.181850606188764807 ) ) ;
#113871=CARTESIAN_POINT ( 'NONE',  ( 1.499999999999996891, 10.67708333401613530, -0.8660254037844378194 ) ) ;
#113935=CARTESIAN_POINT ( 'NONE',  ( -1.364683531250014514, 13.58854166700806587, -0.7879004041258335089 ) ) ;
#113948=CARTESIAN_POINT ( 'NONE',  ( -1.446621748570337429, 4.325121051142003736, -0.4012476001784824331 ) ) ;
#114007=AXIS2_PLACEMENT_3D ( 'NONE', #114641, #115689, #33309 ) ;
#114029=( BOUNDED_CURVE ( )  B_SPLINE_CURVE ( 2, ( #55934, #171817, #43972, #9315, #204278, #172901, #88446, #141503, #173984 ),
 .UNSPECIFIED., .F., .T. ) 
 B_SPLINE_CURVE_WITH_KNOTS ( ( 3, 2, 2, 2, 3 ),
 ( 0.9553571428571427937, 0.9583333333333333703, 0.9642857142857143016, 0.9702380952380952328, 0.9732142857142856984 ),
 .UNSPECIFIED. ) 
 CURVE ( )  GEOMETRIC_REPRESENTATION_ITEM ( )  RATIONAL_B_SPLINE_CURVE ( ( 0.9330127018922194093, 0.9330127018922180770, 1.000000000000000000, 0.8660254037844387076, 1.000000000000000000, 0.8660254037844387076, 1.000000000000000000, 0.9330127018922194093, 0.9330127018922194093 ) ) 
 REPRESENTATION_ITEM ( '' )  );
#114075=EDGE_CURVE ( 'NONE', #155317, #18633, #201611, .T. ) ;
#114089=CARTESIAN_POINT ( 'NONE',  ( 1.364683531249997417, 12.29687500034139980, 2.602085213965210642E-15 ) ) ;
#114112=EDGE_CURVE ( 'NONE', #115710, #73128, #132788, .T. ) ;
#114113=CARTESIAN_POINT ( 'NONE',  ( -3.602337597214539753E-15, 12.06250000000000178, 1.500000000000001554 ) ) ;
#114150=CARTESIAN_POINT ( 'NONE',  ( 0.6823417656249969321, 10.33854166700806587, -1.181850606188757036 ) ) ;
#114189=CARTESIAN_POINT ( 'NONE',  ( 1.499999999999993117, 10.38541666734946212, 0.8660254037844409281 ) ) ;
#114196=CIRCLE ( 'NONE', #48436, 0.6500000000000000222 ) ;
#114249=EDGE_CURVE ( 'NONE', #131458, #39437, #106420, .T. ) ;
#114258=DIRECTION ( 'NONE',  ( 0.000000000000000000, -1.000000000000000000, 0.000000000000000000 ) ) ;
#114263=B_SPLINE_CURVE_WITH_KNOTS ( 'NONE', 3,
 ( #55420, #89008, #72726, #138820, #204841, #122652, #7717, #143117, #142037, #94347, #174530, #208053, #26108, #124775, #173462, #62875, #129042, #127989 ),
 .UNSPECIFIED., .F., .F.,
 ( 4, 2, 2, 2, 2, 2, 2, 2, 4 ),
 ( 0.001640627021451589824, 0.001845642838648680652, 0.002050658655845771696, 0.002255674473042862307, 0.002460690290239953351, 0.002665706107437043962, 0.002870721924634134573, 0.003075737741831225183, 0.003280753559028315794 ),
 .UNSPECIFIED. ) ;
#114292=CARTESIAN_POINT ( 'NONE',  ( 1.436275828743645011, 4.080015253042389212, -0.4487520553618615793 ) ) ;
#114327=CARTESIAN_POINT ( 'NONE',  ( -1.364683531250000748, 9.609375000341396245, 0.000000000000000000 ) ) ;
#114355=LINE ( 'NONE', #98055, #52316 ) ;
#114396=CARTESIAN_POINT ( 'NONE',  ( 0.6823417656249934904, 14.50520833367473195, 1.181850606188764807 ) ) ;
#114514=ORIENTED_EDGE ( 'NONE', *, *, #124881, .T. ) ;
#114519=VERTEX_POINT ( 'NONE', #74935 ) ;
#114560=CARTESIAN_POINT ( 'NONE',  ( 1.500000000000001332, 11.90625000068279427, 0.000000000000000000 ) ) ;
#114569=CARTESIAN_POINT ( 'NONE',  ( 0.7500000000000006661, 13.19791666734946389, -1.299038105676657340 ) ) ;
#114583=CARTESIAN_POINT ( 'NONE',  ( -0.7500000000000006661, 10.45833333333333393, -1.299038105676657340 ) ) ;
#114589=CARTESIAN_POINT ( 'NONE',  ( -0.6823417656250003738, 8.901041667008065872, 1.181850606188754593 ) ) ;
#114625=CARTESIAN_POINT ( 'NONE',  ( 1.364683531250000748, 10.81770833367473195, -0.7879004041258355073 ) ) ;
#114641=CARTESIAN_POINT ( 'NONE',  ( 0.000000000000000000, 13.49999999999999822, 0.000000000000000000 ) ) ;
#114662=CARTESIAN_POINT ( 'NONE',  ( -1.500000000000008216, 10.00000000000000178, 3.469446951953614189E-15 ) ) ;
#114686=VECTOR ( 'NONE', #31729, 999.9999999999998863 ) ;
#114695=CARTESIAN_POINT ( 'NONE',  ( -0.7500000000000006661, 12.98958333401613352, -1.299038105676657340 ) ) ;
#114740=CARTESIAN_POINT ( 'NONE',  ( 1.499999999999996891, 10.92708333401613707, -0.8660254037844378194 ) ) ;
#114932=CARTESIAN_POINT ( 'NONE',  ( -0.1855116875246293484, 13.36893861697142860, -1.371511898276919217 ) ) ;
#114947=DIRECTION ( 'NONE',  ( 0.000000000000000000, 1.000000000000000000, 0.000000000000000000 ) ) ;
#114965=CARTESIAN_POINT ( 'NONE',  ( 1.500000000000001332, 11.12499999999999645, 0.000000000000000000 ) ) ;
#114972=CARTESIAN_POINT ( 'NONE',  ( 0.4153311931458965045, 3.850000000000006306, -0.4999999999999987232 ) ) ;
#114973=FACE_OUTER_BOUND ( 'NONE', #195969, .T. ) ;
#114983=CARTESIAN_POINT ( 'NONE',  ( 0.6823417656249934904, 12.44270833367473017, 1.181850606188764807 ) ) ;
#115096=EDGE_CURVE ( 'NONE', #151327, #36526, #172479, .T. ) ;
#115137=CARTESIAN_POINT ( 'NONE',  ( 0.6823417656249969321, 12.33854166700806765, -1.181850606188757036 ) ) ;
#115201=CARTESIAN_POINT ( 'NONE',  ( -1.402160292154681736E-14, 10.98437500034139802, 1.575800808251682339 ) ) ;
#115245=CARTESIAN_POINT ( 'NONE',  ( -1.500000000000001110, 10.55208333401613352, 0.8660254037844419273 ) ) ;
#115253=CARTESIAN_POINT ( 'NONE',  ( 0.4019237886466778820, 10.10491455036742892, 1.500000000000001554 ) ) ;
#115385=CARTESIAN_POINT ( 'NONE',  ( -1.402160292154681736E-14, 9.171875000341398021, 1.575800808251682339 ) ) ;
#115454=CARTESIAN_POINT ( 'NONE',  ( 1.364683531249996529, 15.02604166700806587, 0.7879004041258405033 ) ) ;
#115490=ORIENTED_EDGE ( 'NONE', *, *, #212409, .F. ) ;
#115509=CARTESIAN_POINT ( 'NONE',  ( 0.7500000000000006661, 8.614583334016129967, 1.299038105676657340 ) ) ;
#115602=CARTESIAN_POINT ( 'NONE',  ( -1.500000000000008216, 12.99999999999999822, 3.469446951953614189E-15 ) ) ;
#115630=CARTESIAN_POINT ( 'NONE',  ( 0.7500000000000006661, 11.16666666666666430, -1.299038105676657340 ) ) ;
#115634=CARTESIAN_POINT ( 'NONE',  ( -1.402160292154681736E-14, 8.421875000341403350, 1.575800808251682339 ) ) ;
#115648=AXIS2_PLACEMENT_3D ( 'NONE', #87339, #154480, #105761 ) ;
#115657=CARTESIAN_POINT ( 'NONE',  ( -1.264911064067355984, 3.815615028976178102, -0.5000000000000005551 ) ) ;
#115674=CARTESIAN_POINT ( 'NONE',  ( 1.364683531249996529, 10.02604166700806587, 0.7879004041258403923 ) ) ;
#115689=DIRECTION ( 'NONE',  ( -0.000000000000000000, 1.000000000000000000, -0.000000000000000000 ) ) ;
#115710=VERTEX_POINT ( 'NONE', #33664 ) ;
#115734=CARTESIAN_POINT ( 'NONE',  ( 0.000000000000000000, 14.00000000000000533, -0.6500000000000000222 ) ) ;
#115749=CARTESIAN_POINT ( 'NONE',  ( 1.500000000000001332, 12.40625000068279427, 0.000000000000000000 ) ) ;
#115763=EDGE_LOOP ( 'NONE', ( #203388, #148552, #28417, #98045 ) ) ;
#115822=CARTESIAN_POINT ( 'NONE',  ( 0.4153311931458965045, 3.850000000000006306, -0.4999999999999987232 ) ) ;
#115941=CARTESIAN_POINT ( 'NONE',  ( -0.7500000000000006661, 11.98958333401613174, -1.299038105676657340 ) ) ;
#116044=CARTESIAN_POINT ( 'NONE',  ( -8.012344526598182026E-15, 12.29687500034140513, -1.575800808251669460 ) ) ;
#116061=EDGE_LOOP ( 'NONE', ( #189875, #103643, #137646, #58615 ) ) ;
#116111=EDGE_CURVE ( 'NONE', #133306, #104840, #157049, .T. ) ;
#116183=ORIENTED_EDGE ( 'NONE', *, *, #181109, .F. ) ;
#116198=CARTESIAN_POINT ( 'NONE',  ( -1.402160292154681736E-14, 12.48437500034139624, 1.575800808251682339 ) ) ;
#116206=EDGE_CURVE ( 'NONE', #180856, #209493, #59513, .T. ) ;
#116239=ORIENTED_EDGE ( 'NONE', *, *, #46969, .T. ) ;
#116249=CARTESIAN_POINT ( 'NONE',  ( -1.364683531250014514, 12.83854166700806410, -0.7879004041258335089 ) ) ;
#116261=CARTESIAN_POINT ( 'NONE',  ( -1.402160292154681736E-14, 10.48437500034139447, 1.575800808251682339 ) ) ;
#116303=CARTESIAN_POINT ( 'NONE',  ( -1.500000000000001110, 8.302083334016129967, 0.8660254037844419273 ) ) ;
#116438=CARTESIAN_POINT ( 'NONE',  ( -1.364683531250010740, 8.630208333674730170, 0.7879004041258445001 ) ) ;
#116440=CARTESIAN_POINT ( 'NONE',  ( -1.297568150123634245, 13.22354355972565898, -0.9828994868031125653 ) ) ;
#116448=LINE ( 'NONE', #34069, #1949 ) ;
#116495=ORIENTED_EDGE ( 'NONE', *, *, #5165, .F. ) ;
#116508=CARTESIAN_POINT ( 'NONE',  ( 1.500000000000001332, 12.87499999999999822, 0.000000000000000000 ) ) ;
#116509=CARTESIAN_POINT ( 'NONE',  ( 0.6823417656249969321, 14.83854166700806410, -1.181850606188757036 ) ) ;
#116524=( BOUNDED_CURVE ( )  B_SPLINE_CURVE ( 2, ( #113599, #213140, #214176, #146056, #114662, #195848, #180656, #66866, #100469 ),
 .UNSPECIFIED., .F., .T. ) 
 B_SPLINE_CURVE_WITH_KNOTS ( ( 3, 2, 2, 2, 3 ),
 ( 0.7767857142857143016, 0.7797619047619047672, 0.7857142857142856984, 0.7916666666666666297, 0.7946428571428572063 ),
 .UNSPECIFIED. ) 
 CURVE ( )  GEOMETRIC_REPRESENTATION_ITEM ( )  RATIONAL_B_SPLINE_CURVE ( ( 0.9330127018922194093, 0.9330127018922194093, 1.000000000000000000, 0.8660254037844387076, 1.000000000000000000, 0.8660254037844387076, 1.000000000000000000, 0.9330127018922180770, 0.9330127018922194093 ) ) 
 REPRESENTATION_ITEM ( '' )  );
#116561=VERTEX_POINT ( 'NONE', #65881 ) ;
#116683=CARTESIAN_POINT ( 'NONE',  ( 1.500000000000001332, 13.15625000068279604, 0.000000000000000000 ) ) ;
#116696=CARTESIAN_POINT ( 'NONE',  ( 1.500000000000001332, 10.62499999999999645, 0.000000000000000000 ) ) ;
#116701=CARTESIAN_POINT ( 'NONE',  ( -1.364683531250000748, 8.609375000341396245, 0.000000000000000000 ) ) ;
#116702=ORIENTED_EDGE ( 'NONE', *, *, #24366, .F. ) ;
#116744=CARTESIAN_POINT ( 'NONE',  ( -0.6823417656250003738, 10.46354166700806587, 1.181850606188754593 ) ) ;
#116817=CARTESIAN_POINT ( 'NONE',  ( -1.402160292154681736E-14, 12.59375000068279959, 1.732050807568881190 ) ) ;
#116896=CARTESIAN_POINT ( 'NONE',  ( -0.5773502691960585853, -4.295408888567775918, 1.000000000000000888 ) ) ;
#116897=CARTESIAN_POINT ( 'NONE',  ( 0.000000000000000000, -4.500000000000003553, -1.359291649810836722 ) ) ;
#116910=CARTESIAN_POINT ( 'NONE',  ( 1.364683531249997417, 13.23437500034139980, 2.602085213965210642E-15 ) ) ;
#116965=CARTESIAN_POINT ( 'NONE',  ( 0.6823417656249969321, 11.52604166700806765, -1.181850606188757036 ) ) ;
#116998=CARTESIAN_POINT ( 'NONE',  ( 0.6823417656249934904, 8.755208333674733723, 1.181850606188764807 ) ) ;
#117022=DIRECTION ( 'NONE',  ( 0.000000000000000000, -1.000000000000000000, 0.000000000000000000 ) ) ;
#117101=CARTESIAN_POINT ( 'NONE',  ( 0.4340280775911202760, 3.986815581052859603, 0.4851569899464819868 ) ) ;
#117111=CARTESIAN_POINT ( 'NONE',  ( -1.364683531250000748, 11.10937500034139802, 0.000000000000000000 ) ) ;
#117143=CARTESIAN_POINT ( 'NONE',  ( 1.129749100085160940, 13.30859003568858689, 0.8992454283418387373 ) ) ;
#117262=CARTESIAN_POINT ( 'NONE',  ( 1.364683531250000303, 12.56770833367473372, -0.7879004041258355073 ) ) ;
#117263=AXIS2_PLACEMENT_3D ( 'NONE', #70723, #199670, #200728 ) ;
#117315=CARTESIAN_POINT ( 'NONE',  ( 1.364683531249996529, 13.21354166700806410, 0.7879004041258403923 ) ) ;
#117321=DIRECTION ( 'NONE',  ( 0.000000000000000000, -1.000000000000000000, 0.000000000000000000 ) ) ;
#117330=CARTESIAN_POINT ( 'NONE',  ( 1.364683531249996529, 11.02604166700807120, 0.7879004041258405033 ) ) ;
#117345=CARTESIAN_POINT ( 'NONE',  ( 1.499999999999993117, 9.635416667349465669, 0.8660254037844408170 ) ) ;
#117374=CARTESIAN_POINT ( 'NONE',  ( 0.7500000000000006661, 8.864583334016129967, 1.299038105676657340 ) ) ;
#117582=CARTESIAN_POINT ( 'NONE',  ( -1.364683531250010295, 14.19270833367473195, 0.7879004041258445001 ) ) ;
#117626=EDGE_LOOP ( 'NONE', ( #49707, #125959, #57173, #121424 ) ) ;
#117774=CARTESIAN_POINT ( 'NONE',  ( 0.6823417656249934904, 11.69270833367473017, 1.181850606188764807 ) ) ;
#117779=CARTESIAN_POINT ( 'NONE',  ( -0.7500000000000179856, 9.291666666666669627, 1.299038105676658228 ) ) ;
#117827=CARTESIAN_POINT ( 'NONE',  ( -1.364683531250010740, 9.442708333674735499, 0.7879004041258445001 ) ) ;
#117876=CARTESIAN_POINT ( 'NONE',  ( -1.500000000000001110, 11.55208333401612997, 0.8660254037844418162 ) ) ;
#117895=CARTESIAN_POINT ( 'NONE',  ( -6.009258394948636914E-15, 12.21875000068279782, -1.732050807568875195 ) ) ;
#117958=EDGE_CURVE ( 'NONE', #47758, #135057, #185447, .T. ) ;
#117985=CARTESIAN_POINT ( 'NONE',  ( 1.364683531250000303, 13.50520833367472839, -0.7879004041258355073 ) ) ;
#118037=CARTESIAN_POINT ( 'NONE',  ( -0.6823417656250003738, 11.65104166700806765, 1.181850606188754593 ) ) ;
#118067=CARTESIAN_POINT ( 'NONE',  ( -2.926243505372967280E-18, -4.140708350189166609, -0.9999999999999991118 ) ) ;
#118084=CARTESIAN_POINT ( 'NONE',  ( -1.364683531250010740, 13.19270833367472839, 0.7879004041258445001 ) ) ;
#118125=CARTESIAN_POINT ( 'NONE',  ( -0.7500000000000006661, 11.45833333333333393, -1.299038105676657340 ) ) ;
#118175=VECTOR ( 'NONE', #88358, 1000.000000000000000 ) ;
#118183=CARTESIAN_POINT ( 'NONE',  ( 1.364683531249996529, 12.21354166700805877, 0.7879004041258405033 ) ) ;
#118317=EDGE_LOOP ( 'NONE', ( #183282, #31489, #65879, #17482 ) ) ;
#118331=CARTESIAN_POINT ( 'NONE',  ( 1.364683531249997417, 11.04687500034139802, 2.602085213965210642E-15 ) ) ;
#118381=CARTESIAN_POINT ( 'NONE',  ( -2.788906526875773208E-15, 11.71875000068279604, -1.499999999999998446 ) ) ;
#118399=CARTESIAN_POINT ( 'NONE',  ( -0.6823417656250039265, 8.880208333674733723, -1.181850606188755259 ) ) ;
#118414=CARTESIAN_POINT ( 'NONE',  ( -1.115562610750309283E-14, 9.593750000682799595, 1.500000000000001554 ) ) ;
#118442=CARTESIAN_POINT ( 'NONE',  ( 1.500000000000001332, 8.906250000682797818, 0.000000000000000000 ) ) ;
#118514=CARTESIAN_POINT ( 'NONE',  ( 0.4019237886466847653, 10.57366454968463110, 1.499999999999997113 ) ) ;
#118621=ORIENTED_EDGE ( 'NONE', *, *, #61890, .F. ) ;
#118647=CARTESIAN_POINT ( 'NONE',  ( -0.6823417656250039265, 12.88020833367473017, -1.181850606188755259 ) ) ;
#118727=CARTESIAN_POINT ( 'NONE',  ( -1.500000000000015099, 11.01041666734946389, -0.8660254037844309360 ) ) ;
#118753=CARTESIAN_POINT ( 'NONE',  ( 3.834746474454188013E-15, 12.84375000068279782, 1.500000000000001554 ) ) ;
#118792=FACE_OUTER_BOUND ( 'NONE', #47004, .T. ) ;
#118829=CARTESIAN_POINT ( 'NONE',  ( -1.402160292154681736E-14, 12.42187500034139802, 1.575800808251682339 ) ) ;
#118834=CARTESIAN_POINT ( 'NONE',  ( 0.7500000000000006661, 9.833333333333332149, 1.299038105676657340 ) ) ;
#118837=( BOUNDED_CURVE ( )  B_SPLINE_CURVE ( 2, ( #121306, #187282, #179573, #159054, #176378, #79920, #43197, #10648, #175321 ),
 .UNSPECIFIED., .F., .T. ) 
 B_SPLINE_CURVE_WITH_KNOTS ( ( 3, 2, 2, 2, 3 ),
 ( 0.7946428571428572063, 0.7976190476190476719, 0.8035714285714286031, 0.8095238095238095344, 0.8125000000000000000 ),
 .UNSPECIFIED. ) 
 CURVE ( )  GEOMETRIC_REPRESENTATION_ITEM ( )  RATIONAL_B_SPLINE_CURVE ( ( 0.9330127018922194093, 0.9330127018922206306, 1.000000000000000000, 0.8660254037844387076, 1.000000000000000000, 0.8660254037844387076, 1.000000000000000000, 0.9330127018922194093, 0.9330127018922194093 ) ) 
 REPRESENTATION_ITEM ( '' )  );
#118885=CARTESIAN_POINT ( 'NONE',  ( -1.364683531250010740, 9.192708333674731946, 0.7879004041258445001 ) ) ;
#118962=CARTESIAN_POINT ( 'NONE',  ( -1.500000000000001110, 12.05208333401613352, 0.8660254037844419273 ) ) ;
#119047=CARTESIAN_POINT ( 'NONE',  ( -1.364683531250000748, 12.85937500034139980, 0.000000000000000000 ) ) ;
#119094=CARTESIAN_POINT ( 'NONE',  ( 0.7500000000000006661, 13.83333333333333570, 1.299038105676657340 ) ) ;
#119100=CARTESIAN_POINT ( 'NONE',  ( 1.364683531249997417, 11.73437500034139802, 2.602085213965210642E-15 ) ) ;
#119146=CARTESIAN_POINT ( 'NONE',  ( 1.364683531249996529, 13.02604166700806410, 0.7879004041258403923 ) ) ;
#119236=CARTESIAN_POINT ( 'NONE',  ( 0.4153311931459133799, 3.919693508839672713, 0.5000000000000067724 ) ) ;
#119245=CARTESIAN_POINT ( 'NONE',  ( 0.6823417656249969321, 11.27604166700806765, -1.181850606188757036 ) ) ;
#119338=ADVANCED_FACE ( 'NONE', ( #208892 ), #89859, .T. ) ;
#119398=CARTESIAN_POINT ( 'NONE',  ( 1.364683531249996529, 11.52604166700806410, 0.7879004041258405033 ) ) ;
#119465=CARTESIAN_POINT ( 'NONE',  ( -1.364683531250000748, 9.171875000341403350, 0.000000000000000000 ) ) ;
#119473=CARTESIAN_POINT ( 'NONE',  ( 0.000000000000000000, 13.20000000000000284, 0.000000000000000000 ) ) ;
#119508=CARTESIAN_POINT ( 'NONE',  ( -1.500000000000001110, 8.552083334016131744, 0.8660254037844419273 ) ) ;
#119544=CARTESIAN_POINT ( 'NONE',  ( -2.788906526875773208E-15, 10.46875000068279604, -1.499999999999998446 ) ) ;
#119612=CARTESIAN_POINT ( 'NONE',  ( 1.499999999999993117, 9.385416667349463893, 0.8660254037844408170 ) ) ;
#119647=CARTESIAN_POINT ( 'NONE',  ( -1.402160292154681736E-14, 8.671875000341403350, 1.575800808251682339 ) ) ;
#119703=CARTESIAN_POINT ( 'NONE',  ( -1.500000000000008216, 8.750000000000000000, 3.469446951953614189E-15 ) ) ;
#119713=CARTESIAN_POINT ( 'NONE',  ( -3.602337597214539753E-15, 12.81249999999999822, 1.500000000000001554 ) ) ;
#119714=CARTESIAN_POINT ( 'NONE',  ( -0.6823417656250003738, 13.71354166700806942, 1.181850606188754593 ) ) ;
#119751=FACE_OUTER_BOUND ( 'NONE', #130949, .T. ) ;
#119800=CARTESIAN_POINT ( 'NONE',  ( -1.500000000000008216, 9.531250000682799595, 3.469446951953614189E-15 ) ) ;
#119874=VECTOR ( 'NONE', #6196, 1000.000000000000000 ) ;
#119908=CARTESIAN_POINT ( 'NONE',  ( -1.364683531250010740, 11.38020833367473728, 0.7879004041258445001 ) ) ;
#119912=CARTESIAN_POINT ( 'NONE',  ( -1.115562610750309283E-14, 9.312500000000001776, 1.500000000000001554 ) ) ;
#119913=CARTESIAN_POINT ( 'NONE',  ( 1.499999999999997113, 9.645833333333333925, -0.8660254037844378194 ) ) ;
#119926=ORIENTED_EDGE ( 'NONE', *, *, #199528, .T. ) ;
#119935=ORIENTED_EDGE ( 'NONE', *, *, #26279, .F. ) ;
#119963=CARTESIAN_POINT ( 'NONE',  ( 1.364683531249997417, 9.296875000341403350, 2.602085213965210642E-15 ) ) ;
#120014=CARTESIAN_POINT ( 'NONE',  ( -0.7500000000000179856, 11.57291666734946212, 1.299038105676658228 ) ) ;
#120037=CARTESIAN_POINT ( 'NONE',  ( -0.7500000000000179856, 11.82291666734946389, 1.299038105676658228 ) ) ;
#120112=CARTESIAN_POINT ( 'NONE',  ( 1.378728738066221871, 4.086408449757453099, -0.5908528300941785494 ) ) ;
#120129=CARTESIAN_POINT ( 'NONE',  ( -1.402160292154681736E-14, 13.92187500034139624, 1.575800808251682339 ) ) ;
#120145=EDGE_CURVE ( 'NONE', #151085, #39437, #53600, .T. ) ;
#120171=CARTESIAN_POINT ( 'NONE',  ( -1.500000000000001110, 13.27083333333333748, 0.8660254037844419273 ) ) ;
#120179=CARTESIAN_POINT ( 'NONE',  ( -1.364683531250014514, 12.58854166700806054, -0.7879004041258335089 ) ) ;
#120294=CARTESIAN_POINT ( 'NONE',  ( -6.009258394948636914E-15, 14.71875000068279427, -1.732050807568875195 ) ) ;
#120325=CARTESIAN_POINT ( 'NONE',  ( -1.364683531250010295, 11.88020833367473017, 0.7879004041258445001 ) ) ;
#120333=CARTESIAN_POINT ( 'NONE',  ( -1.115562610750309283E-14, 9.093750000682799595, 1.500000000000001554 ) ) ;
#120384=VERTEX_POINT ( 'NONE', #112303 ) ;
#120434=CARTESIAN_POINT ( 'NONE',  ( -1.290813828370758864, 3.620001302969693580, 0.4579576469030058883 ) ) ;
#120481=CARTESIAN_POINT ( 'NONE',  ( -1.364683531250010295, 11.19270833367473550, 0.7879004041258445001 ) ) ;
#120493=CARTESIAN_POINT ( 'NONE',  ( -1.500000000000008216, 10.74999999999999645, 3.469446951953614189E-15 ) ) ;
#120500=ORIENTED_EDGE ( 'NONE', *, *, #13528, .F. ) ;
#120507=CARTESIAN_POINT ( 'NONE',  ( -0.6823417656250039265, 15.06770833367473195, -1.181850606188755259 ) ) ;
#120514=DIRECTION ( 'NONE',  ( 0.000000000000000000, 0.000000000000000000, -1.000000000000000000 ) ) ;
#120548=CARTESIAN_POINT ( 'NONE',  ( 1.364683531250000303, 8.817708333674731946, -0.7879004041258355073 ) ) ;
#120590=CIRCLE ( 'NONE', #82466, 2.000000000000000000 ) ;
#120593=CARTESIAN_POINT ( 'NONE',  ( 0.7500000000000006661, 8.947916667349467446, -1.299038105676657340 ) ) ;
#120622=EDGE_CURVE ( 'NONE', #116561, #162002, #19777, .T. ) ;
#120628=DIRECTION ( 'NONE',  ( 0.000000000000000000, 0.000000000000000000, 1.000000000000000000 ) ) ;
#120655=CARTESIAN_POINT ( 'NONE',  ( 1.499999999999996891, 11.42708333401612997, -0.8660254037844378194 ) ) ;
#120735=CARTESIAN_POINT ( 'NONE',  ( 1.364683531249997417, 8.484375000341396245, 2.602085213965210642E-15 ) ) ;
#120778=ORIENTED_EDGE ( 'NONE', *, *, #75612, .T. ) ;
#120796=CARTESIAN_POINT ( 'NONE',  ( -8.012344526598182026E-15, 13.10937500034140157, -1.575800808251669460 ) ) ;
#120832=DIRECTION ( 'NONE',  ( 0.000000000000000000, 0.000000000000000000, -1.000000000000000000 ) ) ;
#120847=CARTESIAN_POINT ( 'NONE',  ( -1.063464886907111495, -4.211945764156256544, 0.1580247838114293979 ) ) ;
#120966=CARTESIAN_POINT ( 'NONE',  ( 1.499999999999993117, 8.885416667349462116, 0.8660254037844408170 ) ) ;
#120993=CARTESIAN_POINT ( 'NONE',  ( 1.364683531249996529, 11.71354166700806587, 0.7879004041258403923 ) ) ;
#120998=CARTESIAN_POINT ( 'NONE',  ( -1.500000000000008216, 10.00000000000000178, 3.469446951953614189E-15 ) ) ;
#121049=CARTESIAN_POINT ( 'NONE',  ( -0.6823417656250003738, 8.713541667008065872, 1.181850606188754593 ) ) ;
#121198=EDGE_LOOP ( 'NONE', ( #645, #141811, #102291, #116183 ) ) ;
#121208=CARTESIAN_POINT ( 'NONE',  ( 0.6823417656249934904, 13.69270833367473195, 1.181850606188764807 ) ) ;
#121252=CARTESIAN_POINT ( 'NONE',  ( -1.402160292154681736E-14, 13.81250000000000000, 1.732050807568881190 ) ) ;
#121256=CARTESIAN_POINT ( 'NONE',  ( 0.6823417656249969321, 12.27604166700806054, -1.181850606188757036 ) ) ;
#121294=ORIENTED_EDGE ( 'NONE', *, *, #129667, .F. ) ;
#121301=CARTESIAN_POINT ( 'NONE',  ( 1.364683531250000748, 12.81770833367473372, -0.7879004041258355073 ) ) ;
#121305=CARTESIAN_POINT ( 'NONE',  ( -1.364683531250000748, 8.359375000341396245, 0.000000000000000000 ) ) ;
#121306=CARTESIAN_POINT ( 'NONE',  ( 1.220146605508150803E-14, 9.937500000000000000, -1.499999999999998446 ) ) ;
#121341=CYLINDRICAL_SURFACE ( 'NONE', #40203, 1.249999999999999778 ) ;
#121367=CARTESIAN_POINT ( 'NONE',  ( -0.7500000000000179856, 14.57291666734946567, 1.299038105676658228 ) ) ;
#121403=CARTESIAN_POINT ( 'NONE',  ( 1.364683531250000303, 10.75520833367473195, -0.7879004041258355073 ) ) ;
#121424=ORIENTED_EDGE ( 'NONE', *, *, #28439, .F. ) ;
#121451=CARTESIAN_POINT ( 'NONE',  ( -3.602337597214539753E-15, 11.84375000068279604, 1.500000000000001554 ) ) ;
#121511=AXIS2_PLACEMENT_3D ( 'NONE', #211137, #195982, #47614 ) ;
#121553=CARTESIAN_POINT ( 'NONE',  ( -0.6823417656250039265, 10.88020833367472839, -1.181850606188755259 ) ) ;
#121578=CARTESIAN_POINT ( 'NONE',  ( -0.6823417656250003738, 14.15104166700806232, 1.181850606188754593 ) ) ;
#121592=EDGE_CURVE ( 'NONE', #39437, #210054, #172951, .T. ) ;
#121613=CARTESIAN_POINT ( 'NONE',  ( -0.4019237886466871523, 12.97991455036742892, -1.499999999999998668 ) ) ;
#121622=CARTESIAN_POINT ( 'NONE',  ( 1.364683531250000303, 8.567708333674730170, -0.7879004041258355073 ) ) ;
#121635=DIRECTION ( 'NONE',  ( 0.000000000000000000, -1.000000000000000000, 0.000000000000000000 ) ) ;
#121657=DIRECTION ( 'NONE',  ( 0.8660254037844385966, 0.000000000000000000, 0.5000000000000001110 ) ) ;
#121667=CARTESIAN_POINT ( 'NONE',  ( 1.364683531249996529, 13.96354166700806765, 0.7879004041258405033 ) ) ;
#121763=CARTESIAN_POINT ( 'NONE',  ( -1.115562610750309283E-14, 8.343750000682796042, 1.500000000000001554 ) ) ;
#121807=CARTESIAN_POINT ( 'NONE',  ( -0.6823417656250003738, 15.21354166700806410, 1.181850606188754593 ) ) ;
#121866=CARTESIAN_POINT ( 'NONE',  ( -1.364683531250000748, 12.67187500034139980, 0.000000000000000000 ) ) ;
#121889=DIRECTION ( 'NONE',  ( 0.000000000000000000, -1.000000000000000000, 0.000000000000000000 ) ) ;
#121917=CARTESIAN_POINT ( 'NONE',  ( -0.9679107548764689373, -4.157144623729469579, 0.3235293953616469320 ) ) ;
#122051=DIRECTION ( 'NONE',  ( 0.000000000000000000, 1.000000000000000000, 0.000000000000000000 ) ) ;
#122061=CARTESIAN_POINT ( 'NONE',  ( -0.6823417656250003738, 11.15104166700806765, 1.181850606188754593 ) ) ;
#122068=CARTESIAN_POINT ( 'NONE',  ( -0.7500000000000006661, 9.458333333333332149, -1.299038105676657340 ) ) ;
#122118=CARTESIAN_POINT ( 'NONE',  ( -1.402160292154681736E-14, 9.234375000341398021, 1.575800808251682339 ) ) ;
#122178=CARTESIAN_POINT ( 'NONE',  ( 0.7500000000000006661, 12.33333333333333570, 1.299038105676657340 ) ) ;
#122292=CARTESIAN_POINT ( 'NONE',  ( 0.000000000000000000, 13.49999999999999822, 0.000000000000000000 ) ) ;
#122330=CARTESIAN_POINT ( 'NONE',  ( -6.009258394948636914E-15, 13.18749999999999822, -1.732050807568875195 ) ) ;
#122336=CARTESIAN_POINT ( 'NONE',  ( 1.364683531249996529, 10.96354166700806942, 0.7879004041258405033 ) ) ;
#122348=AXIS2_PLACEMENT_3D ( 'NONE', #124831, #188679, #26168 ) ;
#122388=FACE_BOUND ( 'NONE', #171565, .T. ) ;
#122475=DIRECTION ( 'NONE',  ( 0.000000000000000000, 0.000000000000000000, -1.000000000000000000 ) ) ;
#122481=CARTESIAN_POINT ( 'NONE',  ( 0.6823417656249934904, 10.69270833367473550, 1.181850606188764807 ) ) ;
#122543=ORIENTED_EDGE ( 'NONE', *, *, #87783, .F. ) ;
#122569=EDGE_CURVE ( 'NONE', #162878, #98728, #209506, .T. ) ;
#122599=ORIENTED_EDGE ( 'NONE', *, *, #30637, .T. ) ;
#122632=CARTESIAN_POINT ( 'NONE',  ( 0.6823417656249969321, 10.83854166700806765, -1.181850606188757036 ) ) ;
#122652=CARTESIAN_POINT ( 'NONE',  ( 0.5723387408578806124, 3.454750211409410632, 0.3125093782470996229 ) ) ;
#122656=CARTESIAN_POINT ( 'NONE',  ( -0.6823417656250003738, 14.40104166700806232, 1.181850606188754593 ) ) ;
#122702=CARTESIAN_POINT ( 'NONE',  ( -1.364683531250010295, 8.942708333674731946, 0.7879004041258445001 ) ) ;
#122713=VERTEX_POINT ( 'NONE', #196487 ) ;
#122748=CARTESIAN_POINT ( 'NONE',  ( -0.6823417656250039265, 14.06770833367473195, -1.181850606188755259 ) ) ;
#122759=EDGE_CURVE ( 'NONE', #67094, #5587, #63110, .T. ) ;
#122760=CARTESIAN_POINT ( 'NONE',  ( -1.355680771150862052, 3.764352529171857142, -0.6419739358886606961 ) ) ;
#122879=ADVANCED_FACE ( 'NONE', ( #163996 ), #193279, .F. ) ;
#122893=CARTESIAN_POINT ( 'NONE',  ( -8.012344526598182026E-15, 15.10937500034140157, -1.575800808251669460 ) ) ;
#122912=CARTESIAN_POINT ( 'NONE',  ( -1.115562610750309283E-14, 11.34375000068279604, 1.500000000000001554 ) ) ;
#122940=CARTESIAN_POINT ( 'NONE',  ( 0.000000000000000000, 13.49999999999999822, -1.500000000000000222 ) ) ;
#122952=CARTESIAN_POINT ( 'NONE',  ( -1.402160292154681736E-14, 13.48437500034139269, 1.575800808251682339 ) ) ;
#122990=FACE_OUTER_BOUND ( 'NONE', #127258, .T. ) ;
#123046=CARTESIAN_POINT ( 'NONE',  ( -1.500000000000001110, 9.552083334016128191, 0.8660254037844418162 ) ) ;
#123128=CARTESIAN_POINT ( 'NONE',  ( 0.4019237886466847653, 8.823664549684627545, 1.499999999999997113 ) ) ;
#123129=CARTESIAN_POINT ( 'NONE',  ( 1.406531590435019963, 4.363011334059644142, -0.01155683023987031516 ) ) ;
#123148=CARTESIAN_POINT ( 'NONE',  ( 0.6823417656249969321, 11.02604166700806765, -1.181850606188757036 ) ) ;
#123228=ORIENTED_EDGE ( 'NONE', *, *, #207043, .T. ) ;
#123256=CARTESIAN_POINT ( 'NONE',  ( 3.834746474454188013E-15, 12.09375000068279604, 1.500000000000001554 ) ) ;
#123398=CARTESIAN_POINT ( 'NONE',  ( -1.500000000000008216, 14.24999999999999822, 3.469446951953614189E-15 ) ) ;
#123403=CARTESIAN_POINT ( 'NONE',  ( 1.364683531249996529, 10.21354166700806587, 0.7879004041258405033 ) ) ;
#123431=DIRECTION ( 'NONE',  ( 0.000000000000000000, 0.000000000000000000, -1.000000000000000000 ) ) ;
#123450=CARTESIAN_POINT ( 'NONE',  ( -8.012344526598182026E-15, 12.10937500034140157, -1.575800808251669460 ) ) ;
#123456=CARTESIAN_POINT ( 'NONE',  ( -1.500000000000001110, 12.30208333401612641, 0.8660254037844418162 ) ) ;
#123516=CARTESIAN_POINT ( 'NONE',  ( -1.500000000000001110, 15.05208333401613174, 0.8660254037844419273 ) ) ;
#123547=CARTESIAN_POINT ( 'NONE',  ( -0.6823417656250039265, 10.56770833367473550, -1.181850606188755259 ) ) ;
#123697=CARTESIAN_POINT ( 'NONE',  ( 1.364683531249996529, 10.27604166700806765, 0.7879004041258405033 ) ) ;
#123720=CARTESIAN_POINT ( 'NONE',  ( 1.364683531249996529, 14.21354166700806942, 0.7879004041258405033 ) ) ;
#123765=CARTESIAN_POINT ( 'NONE',  ( -0.7500000000000006661, 15.45833333333333037, -1.299038105676657340 ) ) ;
#123811=CARTESIAN_POINT ( 'NONE',  ( 0.6823417656249934904, 13.69270833367473195, 1.181850606188764807 ) ) ;
#123949=CARTESIAN_POINT ( 'NONE',  ( -1.364683531250014514, 13.40104166700806587, -0.7879004041258335089 ) ) ;
#123955=( BOUNDED_CURVE ( )  B_SPLINE_CURVE ( 2, ( #74470, #73383, #209778, #58217, #125433, #26774, #124375, #155722, #192465 ),
 .UNSPECIFIED., .F., .T. ) 
 B_SPLINE_CURVE_WITH_KNOTS ( ( 3, 2, 2, 2, 3 ),
 ( 0.5089285714285713969, 0.5119047619047618625, 0.5178571428571429047, 0.5238095238095238360, 0.5267857142857143016 ),
 .UNSPECIFIED. ) 
 CURVE ( )  GEOMETRIC_REPRESENTATION_ITEM ( )  RATIONAL_B_SPLINE_CURVE ( ( 0.9330127018922194093, 0.9330127018922194093, 1.000000000000000000, 0.8660254037844387076, 1.000000000000000000, 0.8660254037844387076, 1.000000000000000000, 0.9330127018922194093, 0.9330127018922194093 ) ) 
 REPRESENTATION_ITEM ( '' )  );
#124009=CARTESIAN_POINT ( 'NONE',  ( 0.000000000000000000, -4.500000000000003553, 0.000000000000000000 ) ) ;
#124010=CARTESIAN_POINT ( 'NONE',  ( 0.6823417656249969321, 11.83854166700806765, -1.181850606188757036 ) ) ;
#124048=CARTESIAN_POINT ( 'NONE',  ( -0.4019237886467001974, 11.30133545031536713, 1.500000000000001998 ) ) ;
#124053=CARTESIAN_POINT ( 'NONE',  ( -0.7500000000000006661, 10.73958333401613174, -1.299038105676657340 ) ) ;
#124059=CIRCLE ( 'NONE', #96318, 1.500000000000000222 ) ;
#124178=CARTESIAN_POINT ( 'NONE',  ( 1.499999999999996891, 8.927083334016126415, -0.8660254037844378194 ) ) ;
#124199=CARTESIAN_POINT ( 'NONE',  ( 1.364683531250000748, 10.50520833367473195, -0.7879004041258355073 ) ) ;
#124253=CIRCLE ( 'NONE', #117263, 2.000000000000000000 ) ;
#124257=CARTESIAN_POINT ( 'NONE',  ( -0.6823417656250039265, 8.630208333674733723, -1.181850606188755259 ) ) ;
#124270=CARTESIAN_POINT ( 'NONE',  ( -0.6823417656250003738, 15.21354166700806410, 1.181850606188754593 ) ) ;
#124375=CARTESIAN_POINT ( 'NONE',  ( 0.7500000000000006661, 11.83333333333333393, 1.299038105676657340 ) ) ;
#124391=VERTEX_POINT ( 'NONE', #12710 ) ;
#124458=CARTESIAN_POINT ( 'NONE',  ( 1.499999999999993117, 11.85416666666666430, 0.8660254037844409281 ) ) ;
#124461=COLOUR_RGB ( '', 0.66274510, 0.83137255, 0.94901961) ;
#124464=CARTESIAN_POINT ( 'NONE',  ( -0.6823417656250039265, 11.06770833367473550, -1.181850606188755259 ) ) ;
#124505=CARTESIAN_POINT ( 'NONE',  ( 1.364683531249996529, 12.52604166700806232, 0.7879004041258403923 ) ) ;
#124515=STYLED_ITEM ( 'NONE', ( #56615 ), #12474 ) ;
#124560=DIRECTION ( 'NONE',  ( 0.000000000000000000, 0.000000000000000000, -1.000000000000000000 ) ) ;
#124565=LINE ( 'NONE', #127773, #22829 ) ;
#124608=CARTESIAN_POINT ( 'NONE',  ( 0.6823417656249934904, 10.44270833367473550, 1.181850606188764807 ) ) ;
#124614=DIRECTION ( 'NONE',  ( 0.000000000000000000, 0.000000000000000000, -1.000000000000000000 ) ) ;
#124621=CARTESIAN_POINT ( 'NONE',  ( -0.5773502691960585853, -4.295408888567775918, 1.000000000000000888 ) ) ;
#124702=DIRECTION ( 'NONE',  ( 0.000000000000000000, 0.000000000000000000, -1.000000000000000000 ) ) ;
#124704=CARTESIAN_POINT ( 'NONE',  ( 1.195384358724066508E-16, -4.140708350189171938, 1.000000000000004441 ) ) ;
#124741=CARTESIAN_POINT ( 'NONE',  ( 3.834746474454188013E-15, 10.34375000068279782, 1.500000000000001554 ) ) ;
#124749=CARTESIAN_POINT ( 'NONE',  ( -0.7500000000000179856, 10.57291666734946212, 1.299038105676658228 ) ) ;
#124756=CARTESIAN_POINT ( 'NONE',  ( 1.364683531249997417, 9.796875000341396245, 2.602085213965210642E-15 ) ) ;
#124763=CARTESIAN_POINT ( 'NONE',  ( -1.204086455771568476, 13.37576698399828246, -0.6670459744446199934 ) ) ;
#124775=CARTESIAN_POINT ( 'NONE',  ( 0.5151611981367327786, 3.543326390565461281, -0.3998388334338426331 ) ) ;
#124779=CARTESIAN_POINT ( 'NONE',  ( -1.364683531250010295, 14.13020833367473372, 0.7879004041258445001 ) ) ;
#124797=CARTESIAN_POINT ( 'NONE',  ( 1.499999999999996891, 10.39583333333333037, -0.8660254037844378194 ) ) ;
#124819=CARTESIAN_POINT ( 'NONE',  ( 0.7500000000000006661, 15.08333333333333748, 1.299038105676657340 ) ) ;
#124831=CARTESIAN_POINT ( 'NONE',  ( 1.286956418854593442, 3.612814789603055132, 0.5511290012047642684 ) ) ;
#124863=CARTESIAN_POINT ( 'NONE',  ( 0.6823417656249969321, 14.27604166700806232, -1.181850606188757036 ) ) ;
#124866=DIRECTION ( 'NONE',  ( 0.000000000000000000, -1.000000000000000000, 0.000000000000000000 ) ) ;
#124875=CARTESIAN_POINT ( 'NONE',  ( -1.265302052550098200, 3.778627107522626094, -0.4993130731308045300 ) ) ;
#124881=EDGE_CURVE ( 'NONE', #1738, #132613, #81571, .T. ) ;
#124897=SURFACE_STYLE_FILL_AREA ( #27296 ) ;
#125011=CARTESIAN_POINT ( 'NONE',  ( 1.364683531250000303, 14.06770833367473550, -0.7879004041258355073 ) ) ;
#125020=FACE_OUTER_BOUND ( 'NONE', #202874, .T. ) ;
#125060=ORIENTED_EDGE ( 'NONE', *, *, #79549, .F. ) ;
#125078=CARTESIAN_POINT ( 'NONE',  ( 1.364683531249997417, 11.79687500034139802, 2.602085213965210642E-15 ) ) ;
#125117=CARTESIAN_POINT ( 'NONE',  ( 1.499999999999993117, 11.88541666734946034, 0.8660254037844409281 ) ) ;
#125134=CARTESIAN_POINT ( 'NONE',  ( 2.449293598294706414E-16, -4.500000000000003553, -2.000000000000000000 ) ) ;
#125219=AXIS2_PLACEMENT_3D ( 'NONE', #75678, #8534, #154800 ) ;
#125258=CARTESIAN_POINT ( 'NONE',  ( -0.6823417656250003738, 10.40104166700806587, 1.181850606188754593 ) ) ;
#125292=EDGE_CURVE ( 'NONE', #75675, #175679, #128197, .T. ) ;
#125335=CARTESIAN_POINT ( 'NONE',  ( -2.788906526875773208E-15, 13.18750000000000000, -1.499999999999998446 ) ) ;
#125356=EDGE_LOOP ( 'NONE', ( #187241, #177219, #128263, #52184 ) ) ;
#125433=CARTESIAN_POINT ( 'NONE',  ( 1.500000000000001332, 11.87499999999999645, 0.000000000000000000 ) ) ;
#125457=CARTESIAN_POINT ( 'NONE',  ( 3.834746474454188013E-15, 9.062500000000001776, 1.500000000000001554 ) ) ;
#125520=CARTESIAN_POINT ( 'NONE',  ( -1.500000000000015099, 11.97916666666666785, -0.8660254037844309360 ) ) ;
#125528=CARTESIAN_POINT ( 'NONE',  ( -1.364683531250014514, 10.33854166700806765, -0.7879004041258335089 ) ) ;
#125564=VECTOR ( 'NONE', #6911, 1000.000000000000000 ) ;
#125566=CARTESIAN_POINT ( 'NONE',  ( -8.012344526598182026E-15, 12.60937500034139802, -1.575800808251669460 ) ) ;
#125615=CARTESIAN_POINT ( 'NONE',  ( -2.788906526875773208E-15, 13.18750000000000000, -1.499999999999998446 ) ) ;
#125634=CARTESIAN_POINT ( 'NONE',  ( -6.009258394948636914E-15, 14.21875000068279782, -1.732050807568875195 ) ) ;
#125665=CARTESIAN_POINT ( 'NONE',  ( 0.6823417656249969321, 10.02604166700806587, -1.181850606188757036 ) ) ;
#125821=CARTESIAN_POINT ( 'NONE',  ( 1.364683531250000303, 10.31770833367473195, -0.7879004041258355073 ) ) ;
#125831=ORIENTED_EDGE ( 'NONE', *, *, #79219, .T. ) ;
#125848=ADVANCED_FACE ( 'NONE', ( #58577, #88961 ), #190691, .T. ) ;
#125851=CARTESIAN_POINT ( 'NONE',  ( -1.500000000000001110, 8.520833333333337478, 0.8660254037844418162 ) ) ;
#125890=CARTESIAN_POINT ( 'NONE',  ( -1.500000000000008216, 15.00000000000000000, 3.469446951953614189E-15 ) ) ;
#125923=B_SPLINE_CURVE_WITH_KNOTS ( 'NONE', 3,
 ( #114972, #19525, #70390, #48858, #20586, #164726, #200399, #49914, #184161, #86672, #151689, #85601, #18460, #197218, #3259, #117101, #119236, #199334 ),
 .UNSPECIFIED., .F., .F.,
 ( 4, 2, 2, 2, 2, 2, 2, 2, 4 ),
 ( 0.000000000000000000, 0.0002050783776814487280, 0.0004101567553628974560, 0.0006152351330443461570, 0.0008203135107257949121, 0.001025391888407243667, 0.001230470266088692314, 0.001435548643770141177, 0.001640627021451589824 ),
 .UNSPECIFIED. ) ;
#125934=CARTESIAN_POINT ( 'NONE',  ( -1.364683531250014514, 14.33854166700806232, -0.7879004041258335089 ) ) ;
#125947=CARTESIAN_POINT ( 'NONE',  ( 0.000000000000000000, 13.49999999999999822, -1.500000000000000222 ) ) ;
#125959=ORIENTED_EDGE ( 'NONE', *, *, #195251, .T. ) ;
#125969=ORIENTED_EDGE ( 'NONE', *, *, #203174, .T. ) ;
#126046=CARTESIAN_POINT ( 'NONE',  ( 1.493932498646918683, 3.368187994538051733, -0.1507059531854390566 ) ) ;
#126073=CARTESIAN_POINT ( 'NONE',  ( 1.364683531249996529, 13.27604166700806410, 0.7879004041258405033 ) ) ;
#126089=ORIENTED_EDGE ( 'NONE', *, *, #180308, .F. ) ;
#126094=DIRECTION ( 'NONE',  ( 0.000000000000000000, -1.000000000000000000, 0.000000000000000000 ) ) ;
#126100=ORIENTED_EDGE ( 'NONE', *, *, #27925, .T. ) ;
#126136=CARTESIAN_POINT ( 'NONE',  ( -0.6823417656250003738, 11.46354166700806765, 1.181850606188754593 ) ) ;
#126173=CARTESIAN_POINT ( 'NONE',  ( -0.7500000000000179856, 11.29166666666666430, 1.299038105676658228 ) ) ;
#126178=CARTESIAN_POINT ( 'NONE',  ( -1.500000000000008216, 11.28125000068279427, 3.469446951953614189E-15 ) ) ;
#126285=CARTESIAN_POINT ( 'NONE',  ( 1.409285775387288941, 4.214549824816848478, 0.5173959003036813220 ) ) ;
#126304=CARTESIAN_POINT ( 'NONE',  ( -1.264550565627408973, 3.789027290228661027, 0.5006333728358381974 ) ) ;
#126319=CARTESIAN_POINT ( 'NONE',  ( 0.6823417656249934904, 10.44270833367473550, 1.181850606188764807 ) ) ;
#126328=CARTESIAN_POINT ( 'NONE',  ( 1.499999999999997113, 8.895833333333339255, -0.8660254037844378194 ) ) ;
#126338=ORIENTED_EDGE ( 'NONE', *, *, #18978, .T. ) ;
#126354=CARTESIAN_POINT ( 'NONE',  ( -2.788906526875773208E-15, 8.718750000682796042, -1.499999999999998446 ) ) ;
#126393=CARTESIAN_POINT ( 'NONE',  ( 4.764381983412778688E-15, 12.93749999999999645, -1.499999999999998446 ) ) ;
#126520=ORIENTED_EDGE ( 'NONE', *, *, #154299, .T. ) ;
#126558=AXIS2_PLACEMENT_3D ( 'NONE', #126640, #107175, #109319 ) ;
#126586=CARTESIAN_POINT ( 'NONE',  ( -6.009258394948636914E-15, 12.18750000000000178, -1.732050807568875195 ) ) ;
#126591=CARTESIAN_POINT ( 'NONE',  ( 0.6823417656249969321, 10.02604166700806587, -1.181850606188757036 ) ) ;
#126627=CARTESIAN_POINT ( 'NONE',  ( -0.6823417656250039265, 11.63020833367473017, -1.181850606188755259 ) ) ;
#126640=CARTESIAN_POINT ( 'NONE',  ( 0.000000000000000000, 13.49999999999999822, 0.000000000000000000 ) ) ;
#126699=CARTESIAN_POINT ( 'NONE',  ( -1.500000000000008216, 14.03125000068279604, 3.469446951953614189E-15 ) ) ;
#126734=CARTESIAN_POINT ( 'NONE',  ( 1.364683531250000303, 9.005208333674731946, -0.7879004041258355073 ) ) ;
#126799=ORIENTED_EDGE ( 'NONE', *, *, #8140, .F. ) ;
#126876=CARTESIAN_POINT ( 'NONE',  ( -0.4019237886466802689, 11.69866454968463287, -1.500000000000002887 ) ) ;
#126887=CARTESIAN_POINT ( 'NONE',  ( 0.6823417656249969321, 10.33854166700806587, -1.181850606188757036 ) ) ;
#126895=CARTESIAN_POINT ( 'NONE',  ( -1.507347117465284603, 13.24758771607280572, 0.07965694612802574903 ) ) ;
#126958=CARTESIAN_POINT ( 'NONE',  ( 1.499999999999997113, 15.39583333333333748, -0.8660254037844378194 ) ) ;
#127005=CARTESIAN_POINT ( 'NONE',  ( -0.6823417656250039265, 13.56770833367473195, -1.181850606188755259 ) ) ;
#127016=CARTESIAN_POINT ( 'NONE',  ( -1.400363088670474765, 4.350706060076355186, 0.06128031220415256636 ) ) ;
#127045=CARTESIAN_POINT ( 'NONE',  ( -1.264911064067349100, 3.883875966818681302, 0.5000000000000055511 ) ) ;
#127102=CARTESIAN_POINT ( 'NONE',  ( -1.499902018610888899, 3.250213382348775770, -0.08390812002218206445 ) ) ;
#127108=DIRECTION ( 'NONE',  ( 0.000000000000000000, 0.000000000000000000, 1.000000000000000000 ) ) ;
#127121=CARTESIAN_POINT ( 'NONE',  ( 1.465018125636654123, 3.329945466055602488, -0.3314627765801584358 ) ) ;
#127123=VECTOR ( 'NONE', #97769, 1000.000000000000000 ) ;
#127144=CARTESIAN_POINT ( 'NONE',  ( -0.6823417656250039265, 13.88020833367473195, -1.181850606188755259 ) ) ;
#127199=DIRECTION ( 'NONE',  ( 0.000000000000000000, 0.000000000000000000, -1.000000000000000000 ) ) ;
#127213=CARTESIAN_POINT ( 'NONE',  ( -0.6823417656250039265, 11.88020833367473017, -1.181850606188755259 ) ) ;
#127256=CARTESIAN_POINT ( 'NONE',  ( -1.402160292154681736E-14, 11.34375000068279427, 1.732050807568881190 ) ) ;
#127258=EDGE_LOOP ( 'NONE', ( #128012, #5069, #180893, #184508 ) ) ;
#127308=CARTESIAN_POINT ( 'NONE',  ( -0.5993104169204935827, 4.282419057637656401, 0.2596433605236394548 ) ) ;
#127346=ORIENTED_EDGE ( 'NONE', *, *, #95199, .T. ) ;
#127358=CARTESIAN_POINT ( 'NONE',  ( 1.491696246971093931, 4.432377618231712724, 0.1760465247046099635 ) ) ;
#127376=CARTESIAN_POINT ( 'NONE',  ( -1.499745039105467637, 3.350786858888608943, 0.07702037080406418101 ) ) ;
#127394=CARTESIAN_POINT ( 'NONE',  ( 1.364683531250000748, 9.005208333674731946, -0.7879004041258355073 ) ) ;
#127444=LINE ( 'NONE', #129570, #80493 ) ;
#127508=DIRECTION ( 'NONE',  ( 0.000000000000000000, 0.000000000000000000, -1.000000000000000000 ) ) ;
#127541=PRESENTATION_STYLE_ASSIGNMENT (( #112334 ) ) ;
#127663=CARTESIAN_POINT ( 'NONE',  ( 0.7500000000000006661, 11.91666666666666607, -1.299038105676657340 ) ) ;
#127668=CARTESIAN_POINT ( 'NONE',  ( 1.364683531250000303, 9.755208333674735499, -0.7879004041258355073 ) ) ;
#127678=CARTESIAN_POINT ( 'NONE',  ( -0.4153311931459208184, 3.850000000000006306, -0.4999999999999961142 ) ) ;
#127706=CARTESIAN_POINT ( 'NONE',  ( -0.6823417656250039265, 11.38020833367473017, -1.181850606188755259 ) ) ;
#127738=LINE ( 'NONE', #212061, #51663 ) ;
#127773=CARTESIAN_POINT ( 'NONE',  ( 7.960204194457795477E-17, 14.00000000000000533, 0.6500000000000000222 ) ) ;
#127782=CARTESIAN_POINT ( 'NONE',  ( -1.500000000000015099, 14.26041666734946212, -0.8660254037844309360 ) ) ;
#127816=CARTESIAN_POINT ( 'NONE',  ( 0.6823417656249969321, 8.776041667008065872, -1.181850606188757036 ) ) ;
#127824=DIRECTION ( 'NONE',  ( 0.000000000000000000, -1.000000000000000000, 0.000000000000000000 ) ) ;
#127825=VECTOR ( 'NONE', #159110, 1000.000000000000000 ) ;
#127879=VERTEX_POINT ( 'NONE', #124621 ) ;
#127922=FACE_OUTER_BOUND ( 'NONE', #166133, .T. ) ;
#127955=VERTEX_POINT ( 'NONE', #108350 ) ;
#127963=( BOUNDED_CURVE ( )  B_SPLINE_CURVE ( 2, ( #24475, #140423, #6085, #76446, #105792, #175040, #72156, #189132, #126354 ),
 .UNSPECIFIED., .F., .T. ) 
 B_SPLINE_CURVE_WITH_KNOTS ( ( 3, 2, 2, 2, 3 ),
 ( 0.9196428571428570953, 0.9226190476190476719, 0.9285714285714286031, 0.9345238095238095344, 0.9375000000000000000 ),
 .UNSPECIFIED. ) 
 CURVE ( )  GEOMETRIC_REPRESENTATION_ITEM ( )  RATIONAL_B_SPLINE_CURVE ( ( 0.9330127018922194093, 0.9330127018922180770, 1.000000000000000000, 0.8660254037844387076, 1.000000000000000000, 0.8660254037844387076, 1.000000000000000000, 0.9330127018922194093, 0.9330127018922194093 ) ) 
 REPRESENTATION_ITEM ( '' )  );
#127970=CARTESIAN_POINT ( 'NONE',  ( -8.012344526598182026E-15, 9.859375000341399797, -1.575800808251669460 ) ) ;
#127980=ORIENTED_EDGE ( 'NONE', *, *, #24826, .T. ) ;
#127989=CARTESIAN_POINT ( 'NONE',  ( 0.4153311931458965045, 3.850000000000006306, -0.4999999999999987232 ) ) ;
#127995=CARTESIAN_POINT ( 'NONE',  ( 0.7500000000000006661, 11.66666666666666607, -1.299038105676657340 ) ) ;
#128012=ORIENTED_EDGE ( 'NONE', *, *, #96950, .F. ) ;
#128077=CARTESIAN_POINT ( 'NONE',  ( 0.6823417656249934904, 13.19270833367473195, 1.181850606188764807 ) ) ;
#128087=CARTESIAN_POINT ( 'NONE',  ( -1.392149563160024472, 4.335119153505146983, -0.1376214334732279998 ) ) ;
#128197=LINE ( 'NONE', #30614, #168311 ) ;
#128199=CARTESIAN_POINT ( 'NONE',  ( 1.499708767979548218, 3.350898811426534341, -0.07854769233531268269 ) ) ;
#128222=CARTESIAN_POINT ( 'NONE',  ( -1.402160292154681736E-14, 13.98437500034139624, 1.575800808251682339 ) ) ;
#128263=ORIENTED_EDGE ( 'NONE', *, *, #165616, .F. ) ;
#128287=CARTESIAN_POINT ( 'NONE',  ( -1.364683531250014514, 11.15104166700806232, -0.7879004041258335089 ) ) ;
#128330=CARTESIAN_POINT ( 'NONE',  ( 1.499999999999993117, 9.635416667349465669, 0.8660254037844409281 ) ) ;
#128428=CARTESIAN_POINT ( 'NONE',  ( 1.494964465105833584, 4.335022008103392110, -0.1399972980471321238 ) ) ;
#128429=( BOUNDED_CURVE ( )  B_SPLINE_CURVE ( 2, ( #125457, #191419, #43086, #175211, #77682, #193568, #144866, #13739, #30013 ),
 .UNSPECIFIED., .F., .T. ) 
 B_SPLINE_CURVE_WITH_KNOTS ( ( 3, 2, 2, 2, 3 ),
 ( 0.9196428571428570953, 0.9226190476190476719, 0.9285714285714286031, 0.9345238095238095344, 0.9375000000000000000 ),
 .UNSPECIFIED. ) 
 CURVE ( )  GEOMETRIC_REPRESENTATION_ITEM ( )  RATIONAL_B_SPLINE_CURVE ( ( 0.9330127018922194093, 0.9330127018922180770, 1.000000000000000000, 0.8660254037844387076, 1.000000000000000000, 0.8660254037844387076, 1.000000000000000000, 0.9330127018922194093, 0.9330127018922194093 ) ) 
 REPRESENTATION_ITEM ( '' )  );
#128447=CARTESIAN_POINT ( 'NONE',  ( -1.412038856124949504, 3.476454961006842037, -0.5099368981155086855 ) ) ;
#128465=CARTESIAN_POINT ( 'NONE',  ( 1.364683531250000748, 8.755208333674731946, -0.7879004041258355073 ) ) ;
#128586=VECTOR ( 'NONE', #9568, 1000.000000000000000 ) ;
#128668=VERTEX_POINT ( 'NONE', #35334 ) ;
#128720=CARTESIAN_POINT ( 'NONE',  ( -1.500000000000008216, 11.99999999999999645, 3.469446951953614189E-15 ) ) ;
#128725=CARTESIAN_POINT ( 'NONE',  ( 0.6823417656249969321, 9.776041667008065872, -1.181850606188757036 ) ) ;
#128759=CARTESIAN_POINT ( 'NONE',  ( -1.364683531250000748, 10.92187500034139802, 0.000000000000000000 ) ) ;
#128766=EDGE_LOOP ( 'NONE', ( #15776, #192144 ) ) ;
#128801=VECTOR ( 'NONE', #200298, 1000.000000000000000 ) ;
#128824=CARTESIAN_POINT ( 'NONE',  ( -6.009258394948636914E-15, 13.71875000068279782, -1.732050807568875195 ) ) ;
#128860=CARTESIAN_POINT ( 'NONE',  ( 0.6823417656249934904, 9.442708333674735499, 1.181850606188764807 ) ) ;
#128869=CARTESIAN_POINT ( 'NONE',  ( 0.4019237886466884846, 11.20758545099816317, -1.499999999999994449 ) ) ;
#128882=LINE ( 'NONE', #43309, #4904 ) ;
#129027=CARTESIAN_POINT ( 'NONE',  ( -1.453605123272271094, 13.24045051524828942, -0.3701785320580647798 ) ) ;
#129042=CARTESIAN_POINT ( 'NONE',  ( 0.4153311931458965600, 3.780177299622912823, -0.4999999999999988343 ) ) ;
#129051=CARTESIAN_POINT ( 'NONE',  ( 1.499999999999996891, 11.64583333333333748, -0.8660254037844378194 ) ) ;
#129059=B_SPLINE_CURVE_WITH_KNOTS ( 'NONE', 3,
 ( #23018, #203903, #54483, #41456, #40381, #187667, #7845, #55549 ),
 .UNSPECIFIED., .F., .F.,
 ( 4, 2, 2, 4 ),
 ( 2.544396950891272413E-07, 0.0002984430161323578892, 0.0005966315925696265331, 0.001193008745444163604 ),
 .UNSPECIFIED. ) ;
#129097=ADVANCED_FACE ( 'NONE', ( #63334 ), #87378, .T. ) ;
#129138=CARTESIAN_POINT ( 'NONE',  ( 1.364683531249996529, 12.96354166700806410, 0.7879004041258405033 ) ) ;
#129150=CARTESIAN_POINT ( 'NONE',  ( -1.430949710260812413, 4.025263519208086116, 0.4689103363401336266 ) ) ;
#129167=ORIENTED_EDGE ( 'NONE', *, *, #41782, .T. ) ;
#129185=AXIS2_PLACEMENT_3D ( 'NONE', #88049, #5690, #120628 ) ;
#129193=ORIENTED_EDGE ( 'NONE', *, *, #48949, .F. ) ;
#129233=CARTESIAN_POINT ( 'NONE',  ( 0.4019237886466778820, 10.07366454968462932, 1.500000000000001554 ) ) ;
#129238=CARTESIAN_POINT ( 'NONE',  ( -1.500000000000015099, 12.22916666666666607, -0.8660254037844309360 ) ) ;
#129289=CARTESIAN_POINT ( 'NONE',  ( -1.364683531250014514, 11.90104166700806587, -0.7879004041258335089 ) ) ;
#129350=CARTESIAN_POINT ( 'NONE',  ( 1.364683531249996529, 9.776041667008064096, 0.7879004041258405033 ) ) ;
#129391=CARTESIAN_POINT ( 'NONE',  ( -1.402160292154681736E-14, 9.843750000682801371, 1.732050807568881190 ) ) ;
#129444=CARTESIAN_POINT ( 'NONE',  ( -0.5150272702496208055, 4.156437351174604444, 0.3999758201171630390 ) ) ;
#129459=FACE_OUTER_BOUND ( 'NONE', #173428, .T. ) ;
#129493=CARTESIAN_POINT ( 'NONE',  ( 1.499630086250555383, 4.449194373282669979, 0.09116236908481112344 ) ) ;
#129511=CARTESIAN_POINT ( 'NONE',  ( -1.272106862006040062, 3.722537557350577675, 0.4878970607599520393 ) ) ;
#129529=CARTESIAN_POINT ( 'NONE',  ( -1.402160292154681736E-14, 9.671875000341399797, 1.575800808251682339 ) ) ;
#129570=CARTESIAN_POINT ( 'NONE',  ( 0.5773502691896192918, -2.500000000000002220, 1.000000000000004441 ) ) ;
#129597=CARTESIAN_POINT ( 'NONE',  ( 1.364683531249996529, 13.77604166700806765, 0.7879004041258405033 ) ) ;
#129599=EDGE_CURVE ( 'NONE', #162002, #142064, #146873, .T. ) ;
#129667=EDGE_CURVE ( 'NONE', #29485, #171094, #66474, .T. ) ;
#129717=EDGE_CURVE ( 'NONE', #152917, #1432, #10988, .T. ) ;
#129756=CARTESIAN_POINT ( 'NONE',  ( -1.500000000000015099, 12.97916666666666963, -0.8660254037844309360 ) ) ;
#129787=CARTESIAN_POINT ( 'NONE',  ( 0.7500000000000006661, 11.08333333333333393, 1.299038105676657340 ) ) ;
#129790=EDGE_CURVE ( 'NONE', #188147, #194295, #68256, .T. ) ;
#129794=CARTESIAN_POINT ( 'NONE',  ( 0.6823417656249934904, 8.942708333674733723, 1.181850606188764807 ) ) ;
#129802=CARTESIAN_POINT ( 'NONE',  ( -0.4153311931459069406, 3.780155993257306335, -0.4999999999999988343 ) ) ;
#129828=CARTESIAN_POINT ( 'NONE',  ( -1.402160292154681736E-14, 10.48437500034139624, 1.575800808251682339 ) ) ;
#129842=FACE_OUTER_BOUND ( 'NONE', #23855, .T. ) ;
#129850=CARTESIAN_POINT ( 'NONE',  ( 0.000000000000000000, 0.000000000000000000, 0.000000000000000000 ) ) ;
#129898=CARTESIAN_POINT ( 'NONE',  ( -1.500000000000015099, 13.51041666734946034, -0.8660254037844309360 ) ) ;
#129932=CARTESIAN_POINT ( 'NONE',  ( 0.6823417656249969321, 8.526041667008064096, -1.181850606188757036 ) ) ;
#129941=DIRECTION ( 'NONE',  ( 0.000000000000000000, 0.000000000000000000, -1.000000000000000000 ) ) ;
#129946=CARTESIAN_POINT ( 'NONE',  ( 1.500000000000001332, 10.90625000068279249, 0.000000000000000000 ) ) ;
#130039=CARTESIAN_POINT ( 'NONE',  ( 1.364683531249996529, 11.96354166700806765, 0.7879004041258403923 ) ) ;
#130080=CARTESIAN_POINT ( 'NONE',  ( -1.316594279187295768, 13.29598046972190595, -0.6183304965053929569 ) ) ;
#130084=ORIENTED_EDGE ( 'NONE', *, *, #129717, .T. ) ;
#130108=CARTESIAN_POINT ( 'NONE',  ( 0.4019237886466884846, 11.67633545031536535, -1.499999999999994449 ) ) ;
#130155=CARTESIAN_POINT ( 'NONE',  ( -1.500000000000015099, 9.760416667349465669, -0.8660254037844309360 ) ) ;
#130189=CARTESIAN_POINT ( 'NONE',  ( -8.012344526598182026E-15, 12.79687500034139802, -1.575800808251669460 ) ) ;
#130229=ORIENTED_EDGE ( 'NONE', *, *, #184537, .T. ) ;
#130283=CARTESIAN_POINT ( 'NONE',  ( 1.499999999999993117, 10.10416666666667140, 0.8660254037844408170 ) ) ;
#130340=CARTESIAN_POINT ( 'NONE',  ( -0.6823417656250039265, 12.38020833367473017, -1.181850606188755259 ) ) ;
#130378=ORIENTED_EDGE ( 'NONE', *, *, #158993, .T. ) ;
#130386=DIRECTION ( 'NONE',  ( 0.000000000000000000, -1.000000000000000000, 0.000000000000000000 ) ) ;
#130405=CARTESIAN_POINT ( 'NONE',  ( -8.012344526598182026E-15, 10.10937500034140157, -1.575800808251669460 ) ) ;
#130434=CARTESIAN_POINT ( 'NONE',  ( 1.499999999999996891, 12.14583333333333748, -0.8660254037844378194 ) ) ;
#130446=CARTESIAN_POINT ( 'NONE',  ( 1.499999999999993117, 10.13541666734946745, 0.8660254037844409281 ) ) ;
#130500=CARTESIAN_POINT ( 'NONE',  ( -0.5997958527293503206, 4.283086937630856461, -0.2585301179639542535 ) ) ;
#130545=CARTESIAN_POINT ( 'NONE',  ( 1.300073763039447883, 4.107155158418582808, -0.4337670944212108082 ) ) ;
#130564=CARTESIAN_POINT ( 'NONE',  ( -1.400320522945621482, 3.349376740025014954, -0.06109695461879691841 ) ) ;
#130583=CARTESIAN_POINT ( 'NONE',  ( -1.364683531250010740, 9.880208333674728394, 0.7879004041258445001 ) ) ;
#130652=CARTESIAN_POINT ( 'NONE',  ( -1.364683531250010295, 14.69270833367472839, 0.7879004041258445001 ) ) ;
#130799=B_SPLINE_CURVE_WITH_KNOTS ( 'NONE', 3,
 ( #174929, #75271, #77398, #158660, #143514, #209510, #61151, #44928 ),
 .UNSPECIFIED., .F., .F.,
 ( 4, 2, 2, 4 ),
 ( 2.544396950703400505E-07, 0.0002984430161323410840, 0.0005966315925696118964, 0.001193008745444153196 ),
 .UNSPECIFIED. ) ;
#130834=CARTESIAN_POINT ( 'NONE',  ( -1.500000000000001110, 10.52083333333333037, 0.8660254037844419273 ) ) ;
#130839=CARTESIAN_POINT ( 'NONE',  ( 1.364683531249997417, 9.484375000341396245, 2.602085213965210642E-15 ) ) ;
#130872=CARTESIAN_POINT ( 'NONE',  ( 1.364683531250000748, 10.06770833367473017, -0.7879004041258355073 ) ) ;
#130888=CARTESIAN_POINT ( 'NONE',  ( 0.4019237886466847653, 10.82366454968463110, 1.499999999999997113 ) ) ;
#130948=CARTESIAN_POINT ( 'NONE',  ( 0.7500000000000006661, 12.86458333401613352, 1.299038105676657340 ) ) ;
#130949=EDGE_LOOP ( 'NONE', ( #208112, #167079, #68961, #154270, #13270 ) ) ;
#130982=CARTESIAN_POINT ( 'NONE',  ( -0.6823417656250003738, 8.401041667008064096, 1.181850606188754593 ) ) ;
#131089=AXIS2_PLACEMENT_3D ( 'NONE', #179375, #28848, #14706 ) ;
#131105=VECTOR ( 'NONE', #31332, 1000.000000000000114 ) ;
#131136=CARTESIAN_POINT ( 'NONE',  ( 3.834746474454188013E-15, 12.09375000068279604, 1.500000000000001554 ) ) ;
#131148=CARTESIAN_POINT ( 'NONE',  ( 0.7500000000000006661, 9.166666666666669627, -1.299038105676657340 ) ) ;
#131191=CARTESIAN_POINT ( 'NONE',  ( 4.344593448898664693E-13, 13.36537488277823371, -1.375075632470054154 ) ) ;
#131216=EDGE_LOOP ( 'NONE', ( #116702, #13340, #11721, #115490 ) ) ;
#131240=CARTESIAN_POINT ( 'NONE',  ( -1.364683531250010295, 13.63020833367473017, 0.7879004041258445001 ) ) ;
#131252=CARTESIAN_POINT ( 'NONE',  ( -1.467639082483196855, 4.376379912524843263, 0.3198401300024801830 ) ) ;
#131292=EDGE_LOOP ( 'NONE', ( #52247, #127346, #112562, #177895 ) ) ;
#131381=CARTESIAN_POINT ( 'NONE',  ( -1.364683531250000748, 12.67187500034139980, 0.000000000000000000 ) ) ;
#131438=CARTESIAN_POINT ( 'NONE',  ( 0.6823417656249934904, 10.25520833367472839, 1.181850606188764807 ) ) ;
#131458=VERTEX_POINT ( 'NONE', #194837 ) ;
#131467=CARTESIAN_POINT ( 'NONE',  ( 0.4019237886466814902, 12.07366454968463110, 1.499999999999999334 ) ) ;
#131480=CARTESIAN_POINT ( 'NONE',  ( 0.7500000000000006661, 9.447916667349467446, -1.299038105676657340 ) ) ;
#131487=VECTOR ( 'NONE', #60494, 1000.000000000000000 ) ;
#131621=CARTESIAN_POINT ( 'NONE',  ( 1.364683531249996529, 9.463541667008062319, 0.7879004041258403923 ) ) ;
#131641=EDGE_LOOP ( 'NONE', ( #132540, #103870, #122599, #54598, #98439, #30723, #105224, #187087, #195811, #143142, #65558, #86980, #143876, #109960, #44962, #39974, #190092, #123228, #144260, #102999, #188608, #161649, #9741, #145236, #98978, #210010, #196239, #195458, #194456, #180117, #169343, #141742, #95421, #19465, #165809, #57628, #103292, #174001, #182208, #161530, #67138, #145270, #126089, #179676 ) ) ;
#131688=CARTESIAN_POINT ( 'NONE',  ( -0.6823417656250003738, 14.71354166700806410, 1.181850606188754593 ) ) ;
#131746=CARTESIAN_POINT ( 'NONE',  ( 0.7500000000000006661, 8.697916667349467446, -1.299038105676657340 ) ) ;
#131766=LINE ( 'NONE', #179422, #30205 ) ;
#131801=CARTESIAN_POINT ( 'NONE',  ( -1.115562610750309283E-14, 11.56249999999999822, 1.500000000000001554 ) ) ;
#131833=ORIENTED_EDGE ( 'NONE', *, *, #121592, .F. ) ;
#131871=CARTESIAN_POINT ( 'NONE',  ( -1.402160292154681736E-14, 10.56250000000000178, 1.732050807568881190 ) ) ;
#131876=CARTESIAN_POINT ( 'NONE',  ( 1.364683531250000303, 8.755208333674731946, -0.7879004041258355073 ) ) ;
#131877=ORIENTED_EDGE ( 'NONE', *, *, #10916, .F. ) ;
#131912=CARTESIAN_POINT ( 'NONE',  ( -0.6823417656250039265, 11.13020833367473017, -1.181850606188755259 ) ) ;
#131913=ORIENTED_EDGE ( 'NONE', *, *, #145950, .F. ) ;
#131989=CARTESIAN_POINT ( 'NONE',  ( -1.500000000000001110, 12.30208333401612641, 0.8660254037844419273 ) ) ;
#132002=DIRECTION ( 'NONE',  ( 0.000000000000000000, 0.000000000000000000, 1.000000000000000000 ) ) ;
#132063=CARTESIAN_POINT ( 'NONE',  ( 1.455271222711090884, 3.352338309680428896, 0.3949897977301484731 ) ) ;
#132203=CARTESIAN_POINT ( 'NONE',  ( -1.500000000000015099, 10.01041666734946745, -0.8660254037844309360 ) ) ;
#132265=DIRECTION ( 'NONE',  ( -0.4999999999999999445, 0.000000000000000000, 0.8660254037844387076 ) ) ;
#132274=CARTESIAN_POINT ( 'NONE',  ( 0.6823417656249969321, 12.02604166700806054, -1.181850606188757036 ) ) ;
#132430=CARTESIAN_POINT ( 'NONE',  ( -0.6823417656250003738, 12.21354166700806765, 1.181850606188754593 ) ) ;
#132479=B_SPLINE_CURVE_WITH_KNOTS ( 'NONE', 3,
 ( #206978, #140968, #186462, #203764, #124763, #105246, #107424, #38098, #205912, #73786 ),
 .UNSPECIFIED., .F., .F.,
 ( 4, 2, 2, 2, 4 ),
 ( 0.000000000000000000, 0.0005407846995530511116, 0.001081569399106102223, 0.001622354098659153226, 0.002163138798212204447 ),
 .UNSPECIFIED. ) ;
#132494=CARTESIAN_POINT ( 'NONE',  ( -0.6823417656250039265, 10.88020833367472839, -1.181850606188755259 ) ) ;
#132538=CARTESIAN_POINT ( 'NONE',  ( -1.500000000000015099, 9.260416667349463893, -0.8660254037844309360 ) ) ;
#132540=ORIENTED_EDGE ( 'NONE', *, *, #98818, .F. ) ;
#132613=VERTEX_POINT ( 'NONE', #56179 ) ;
#132738=CARTESIAN_POINT ( 'NONE',  ( -0.6823417656250003738, 14.21354166700806232, 1.181850606188754593 ) ) ;
#132788=CIRCLE ( 'NONE', #122348, 0.1000000000000000333 ) ;
#132797=CARTESIAN_POINT ( 'NONE',  ( -2.788906526875773208E-15, 8.718750000682796042, -1.499999999999998446 ) ) ;
#132923=CARTESIAN_POINT ( 'NONE',  ( 0.7500000000000006661, 10.83333333333333393, 1.299038105676657340 ) ) ;
#132928=CARTESIAN_POINT ( 'NONE',  ( 1.364683531249997417, 15.04687500034139447, 2.602085213965210642E-15 ) ) ;
#132972=CARTESIAN_POINT ( 'NONE',  ( -1.364683531250000748, 11.17187500034139802, 0.000000000000000000 ) ) ;
#132999=DIRECTION ( 'NONE',  ( 0.000000000000000000, 0.000000000000000000, -1.000000000000000000 ) ) ;
#133041=DIRECTION ( 'NONE',  ( 0.000000000000000000, -1.000000000000000000, 0.000000000000000000 ) ) ;
#133045=CARTESIAN_POINT ( 'NONE',  ( -0.7500000000000179856, 13.07291666734946389, 1.299038105676658228 ) ) ;
#133138=CARTESIAN_POINT ( 'NONE',  ( 1.364683531249997417, 12.98437500034139980, 2.602085213965210642E-15 ) ) ;
#133190=CARTESIAN_POINT ( 'NONE',  ( -8.012344526598182026E-15, 11.54687500034139980, -1.575800808251669460 ) ) ;
#133269=DIRECTION ( 'NONE',  ( 0.000000000000000000, 0.000000000000000000, -1.000000000000000000 ) ) ;
#133306=VERTEX_POINT ( 'NONE', #17554 ) ;
#133339=CARTESIAN_POINT ( 'NONE',  ( -1.364683531250000748, 11.35937500034139802, 0.000000000000000000 ) ) ;
#133369=CARTESIAN_POINT ( 'NONE',  ( 0.3667750149253126701, 13.29281888235296094, 1.403446231478199246 ) ) ;
#133382=VERTEX_POINT ( 'NONE', #64212 ) ;
#133492=CARTESIAN_POINT ( 'NONE',  ( 1.364683531250000303, 11.81770833367472839, -0.7879004041258355073 ) ) ;
#133555=CARTESIAN_POINT ( 'NONE',  ( -0.6823417656250003738, 10.71354166700806765, 1.181850606188754593 ) ) ;
#133571=CARTESIAN_POINT ( 'NONE',  ( 0.4019237886466884846, 9.707585450998170273, -1.499999999999994449 ) ) ;
#133601=CARTESIAN_POINT ( 'NONE',  ( -1.500000000000015099, 9.010416667349463893, -0.8660254037844309360 ) ) ;
#133700=CARTESIAN_POINT ( 'NONE',  ( -1.500000000000015099, 9.229166666666667851, -0.8660254037844309360 ) ) ;
#133739=CARTESIAN_POINT ( 'NONE',  ( -0.6823417656250003738, 8.401041667008064096, 1.181850606188754593 ) ) ;
#133765=CARTESIAN_POINT ( 'NONE',  ( 1.220146605508150803E-14, 9.687500000000000000, -1.499999999999998446 ) ) ;
#133805=CARTESIAN_POINT ( 'NONE',  ( -1.364683531250000748, 14.42187500034139447, 0.000000000000000000 ) ) ;
#133859=ADVANCED_FACE ( 'NONE', ( #65276 ), #170333, .F. ) ;
#133970=( BOUNDED_SURFACE ( )  B_SPLINE_SURFACE ( 3, 2, ( 
 ( #173576, #191903, #56597 ),
 ( #5665, #207096, #104283 ),
 ( #124875, #204946, #122760 ),
 ( #188720, #137859, #105366 ),
 ( #170329, #140005, #21915 ),
 ( #25145, #203880, #55524 ),
 ( #187644, #79238, #176742 ),
 ( #109685, #196194, #113948 ),
 ( #163699, #111812, #177817 ),
 ( #128087, #47837, #213472 ),
 ( #29433, #211357, #95524 ),
 ( #127016, #44627, #179944 ),
 ( #93385, #144295, #15282 ),
 ( #192975, #146401, #131252 ),
 ( #31567, #145357, #112875 ),
 ( #161574, #13161, #110744 ),
 ( #62982, #94451, #65095 ),
 ( #45697, #129150, #209213 ) ),
 .UNSPECIFIED., .F., .F., .T. ) 
 B_SPLINE_SURFACE_WITH_KNOTS ( ( 4, 2, 2, 2, 2, 2, 2, 2, 4 ),
 ( 3, 3 ),
 ( 0.000000000000000000, 0.0002366965742690630467, 0.0004733931485381260933, 0.0007100897228071891129, 0.0009467862970762521866, 0.001183482871345315152, 0.001420179445614378226, 0.001656876019883441300, 0.001893572594152504373 ),
 ( 0.000000000000000000, 1.000000000000000000 ),
 .UNSPECIFIED. ) 
 GEOMETRIC_REPRESENTATION_ITEM ( )  RATIONAL_B_SPLINE_SURFACE ( (
 ( 1.000000000000000000, 0.5647844906712726765, 1.000000000000000000),
 ( 1.000000000000000000, 0.5466263600439149606, 1.000000000000000000),
 ( 1.000000000000000000, 0.5350732119542429555, 1.000000000000000000),
 ( 1.000000000000000000, 0.5340116227283870920, 1.000000000000000000),
 ( 1.000000000000000000, 0.5448366076419293158, 1.000000000000000000),
 ( 1.000000000000000000, 0.5794957582367121773, 1.000000000000000000),
 ( 1.000000000000000000, 0.6029004271910476387, 1.000000000000000000),
 ( 1.000000000000000000, 0.6471109807880470743, 1.000000000000000000),
 ( 1.000000000000000000, 0.6680936278988007793, 1.000000000000000000),
 ( 1.000000000000000000, 0.6979136174567561746, 1.000000000000000000),
 ( 1.000000000000000000, 0.7066420332305399787, 1.000000000000000000),
 ( 1.000000000000000000, 0.7075346919462069950, 1.000000000000000000),
 ( 1.000000000000000000, 0.6996296472763622321, 1.000000000000000000),
 ( 1.000000000000000000, 0.6710614938507052374, 1.000000000000000000),
 ( 1.000000000000000000, 0.6504127778617917466, 1.000000000000000000),
 ( 1.000000000000000000, 0.6064966788547884180, 1.000000000000000000),
 ( 1.000000000000000000, 0.5828236970731401900, 1.000000000000000000),
 ( 1.000000000000000000, 0.5649783097559288869, 1.000000000000000000) ) ) 
 REPRESENTATION_ITEM ( '' )  SURFACE ( )  );
#133974=CARTESIAN_POINT ( 'NONE',  ( 1.499999999999993117, 11.88541666734946034, 0.8660254037844408170 ) ) ;
#133995=CARTESIAN_POINT ( 'NONE',  ( 1.364683531250000748, 11.75520833367473017, -0.7879004041258355073 ) ) ;
#134001=CARTESIAN_POINT ( 'NONE',  ( 1.499999999999997113, 10.89583333333333215, -0.8660254037844378194 ) ) ;
#134045=CARTESIAN_POINT ( 'NONE',  ( 1.364683531249996529, 9.776041667008064096, 0.7879004041258403923 ) ) ;
#134099=CARTESIAN_POINT ( 'NONE',  ( 0.7500000000000006661, 8.666666666666669627, -1.299038105676657340 ) ) ;
#134103=CARTESIAN_POINT ( 'NONE',  ( 1.499999999999993117, 12.35416666666666607, 0.8660254037844408170 ) ) ;
#134116=CARTESIAN_POINT ( 'NONE',  ( -1.402160292154681736E-14, 13.09375000068280315, 1.732050807568881190 ) ) ;
#134126=CARTESIAN_POINT ( 'NONE',  ( -1.500000000000015099, 12.72916666666666785, -0.8660254037844309360 ) ) ;
#134201=CARTESIAN_POINT ( 'NONE',  ( -1.402160292154681736E-14, 12.92187500034139980, 1.575800808251682339 ) ) ;
#134203=AXIS2_PLACEMENT_3D ( 'NONE', #151486, #201260, #1987 ) ;
#134256=CARTESIAN_POINT ( 'NONE',  ( 1.364683531249996529, 11.96354166700806765, 0.7879004041258405033 ) ) ;
#134328=CARTESIAN_POINT ( 'NONE',  ( -0.7500000000000179856, 10.29166666666667140, 1.299038105676658228 ) ) ;
#134372=CARTESIAN_POINT ( 'NONE',  ( 0.000000000000000000, 13.20000000000000284, 0.000000000000000000 ) ) ;
#134375=ORIENTED_EDGE ( 'NONE', *, *, #5890, .F. ) ;
#134406=CARTESIAN_POINT ( 'NONE',  ( 0.6823417656249969321, 12.27604166700806054, -1.181850606188757036 ) ) ;
#134413=DIRECTION ( 'NONE',  ( -0.000000000000000000, 1.000000000000000000, -0.000000000000000000 ) ) ;
#134419=EDGE_CURVE ( 'NONE', #28009, #78671, #201668, .T. ) ;
#134437=CARTESIAN_POINT ( 'NONE',  ( 1.414375913850415278, 13.32373988190677139, 0.1231264505149970989 ) ) ;
#134554=CARTESIAN_POINT ( 'NONE',  ( -8.012344526598182026E-15, 11.60937500034140157, -1.575800808251669460 ) ) ;
#134620=CARTESIAN_POINT ( 'NONE',  ( -8.012344526598182026E-15, 9.109375000341398021, -1.575800808251669460 ) ) ;
#134645=CARTESIAN_POINT ( 'NONE',  ( 0.4019237886466816012, 12.17633545031537068, -1.499999999999998668 ) ) ;
#134660=CARTESIAN_POINT ( 'NONE',  ( -1.500000000000015099, 8.510416667349460340, -0.8660254037844309360 ) ) ;
#134729=CARTESIAN_POINT ( 'NONE',  ( 0.7500000000000006661, 10.66666666666666430, -1.299038105676657340 ) ) ;
#134793=CARTESIAN_POINT ( 'NONE',  ( -8.012344526598182026E-15, 8.546875000341403350, -1.575800808251669460 ) ) ;
#134795=CARTESIAN_POINT ( 'NONE',  ( -1.453605123272271094, 13.24045051524828942, -0.3701785320580647798 ) ) ;
#134862=CARTESIAN_POINT ( 'NONE',  ( -0.6823417656250003738, 12.71354166700806942, 1.181850606188754593 ) ) ;
#134944=CARTESIAN_POINT ( 'NONE',  ( -1.500000000000001110, 11.05208333401613707, 0.8660254037844418162 ) ) ;
#135044=CARTESIAN_POINT ( 'NONE',  ( -8.012344526598182026E-15, 11.79687500034140157, -1.575800808251669460 ) ) ;
#135049=CARTESIAN_POINT ( 'NONE',  ( -6.009258394948636914E-15, 10.18750000000000000, -1.732050807568875195 ) ) ;
#135057=VERTEX_POINT ( 'NONE', #99678 ) ;
#135097=CARTESIAN_POINT ( 'NONE',  ( -1.364683531250000748, 9.421875000341396245, 0.000000000000000000 ) ) ;
#135171=CARTESIAN_POINT ( 'NONE',  ( 1.499999999999993117, 13.13541666734946745, 0.8660254037844409281 ) ) ;
#135261=CARTESIAN_POINT ( 'NONE',  ( -1.364683531250014514, 13.33854166700806587, -0.7879004041258335089 ) ) ;
#135275=EDGE_CURVE ( 'NONE', #33711, #29614, #213247, .T. ) ;
#135280=CARTESIAN_POINT ( 'NONE',  ( 1.406470046317633615, 3.337112123497550265, 0.01120553378792966959 ) ) ;
#135303=CARTESIAN_POINT ( 'NONE',  ( -0.7500000000000179856, 14.04166666666666785, 1.299038105676658228 ) ) ;
#135310=CARTESIAN_POINT ( 'NONE',  ( -1.402160292154681736E-14, 12.17187500034140335, 1.575800808251682339 ) ) ;
#135375=CARTESIAN_POINT ( 'NONE',  ( -0.7500000000000006661, 10.20833333333333393, -1.299038105676657340 ) ) ;
#135447=CARTESIAN_POINT ( 'NONE',  ( -1.364683531250000748, 11.85937500034139802, 0.000000000000000000 ) ) ;
#135503=ORIENTED_EDGE ( 'NONE', *, *, #207358, .F. ) ;
#135565=ORIENTED_EDGE ( 'NONE', *, *, #139460, .F. ) ;
#135576=ORIENTED_EDGE ( 'NONE', *, *, #80209, .F. ) ;
#135584=EDGE_CURVE ( 'NONE', #112702, #33711, #20929, .T. ) ;
#135597=CARTESIAN_POINT ( 'NONE',  ( -1.364683531250014514, 11.65104166700806587, -0.7879004041258335089 ) ) ;
#135623=CARTESIAN_POINT ( 'NONE',  ( -1.364683531250014514, 15.33854166700806587, -0.7879004041258335089 ) ) ;
#135664=CARTESIAN_POINT ( 'NONE',  ( -1.364683531250014514, 9.151041667008060543, -0.7879004041258335089 ) ) ;
#135667=ADVANCED_FACE ( 'NONE', ( #35730 ), #36793, .T. ) ;
#135706=CARTESIAN_POINT ( 'NONE',  ( 0.7500000000000006661, 8.447916667349467446, -1.299038105676657340 ) ) ;
#135909=CARTESIAN_POINT ( 'NONE',  ( 0.6823417656249969321, 13.08854166700806942, -1.181850606188757036 ) ) ;
#136029=ORIENTED_EDGE ( 'NONE', *, *, #167459, .T. ) ;
#136035=ORIENTED_EDGE ( 'NONE', *, *, #160143, .T. ) ;
#136091=DIRECTION ( 'NONE',  ( -1.000000000000000000, 0.000000000000000000, 1.665334536937734811E-16 ) ) ;
#136099=CARTESIAN_POINT ( 'NONE',  ( -0.6823417656250003738, 11.90104166700806054, 1.181850606188754593 ) ) ;
#136103=CARTESIAN_POINT ( 'NONE',  ( 0.7500000000000006661, 9.416666666666669627, -1.299038105676657340 ) ) ;
#136105=CARTESIAN_POINT ( 'NONE',  ( -1.402160292154681736E-14, 9.062500000000003553, 1.732050807568881190 ) ) ;
#136118=ORIENTED_EDGE ( 'NONE', *, *, #32262, .F. ) ;
#136157=CARTESIAN_POINT ( 'NONE',  ( 0.6823417656249969321, 9.338541667008065872, -1.181850606188757036 ) ) ;
#136163=CARTESIAN_POINT ( 'NONE',  ( -0.7500000000000006661, 10.23958333401612997, -1.299038105676657340 ) ) ;
#136210=FACE_OUTER_BOUND ( 'NONE', #186096, .T. ) ;
#136227=DIRECTION ( 'NONE',  ( 1.000000000000000000, 0.000000000000000000, 0.000000000000000000 ) ) ;
#136228=CARTESIAN_POINT ( 'NONE',  ( 0.7500000000000006661, 11.11458333401613174, 1.299038105676657340 ) ) ;
#136278=CARTESIAN_POINT ( 'NONE',  ( -1.115562610750309283E-14, 11.34375000068279604, 1.500000000000001554 ) ) ;
#136318=CARTESIAN_POINT ( 'NONE',  ( -1.402160292154681736E-14, 13.67187500034139447, 1.575800808251682339 ) ) ;
#136364=CARTESIAN_POINT ( 'NONE',  ( 0.7500000000000006661, 13.33333333333333570, 1.299038105676657340 ) ) ;
#136371=CARTESIAN_POINT ( 'NONE',  ( 1.364683531250000303, 12.25520833367473195, -0.7879004041258355073 ) ) ;
#136419=CARTESIAN_POINT ( 'NONE',  ( 0.6823417656249969321, 12.83854166700806942, -1.181850606188757036 ) ) ;
#136517=CARTESIAN_POINT ( 'NONE',  ( 1.364683531249996529, 11.46354166700806410, 0.7879004041258405033 ) ) ;
#136525=CARTESIAN_POINT ( 'NONE',  ( -0.4019237886466871523, 8.979914550367425363, -1.499999999999998668 ) ) ;
#136667=CARTESIAN_POINT ( 'NONE',  ( 1.364683531250000303, 10.81770833367473195, -0.7879004041258355073 ) ) ;
#136723=DIRECTION ( 'NONE',  ( 0.000000000000000000, 0.000000000000000000, -1.000000000000000000 ) ) ;
#136731=CARTESIAN_POINT ( 'NONE',  ( 1.364683531249997417, 8.796875000341403350, 2.602085213965210642E-15 ) ) ;
#136772=CARTESIAN_POINT ( 'NONE',  ( 1.500000000000001332, 8.656250000682797818, 0.000000000000000000 ) ) ;
#136917=CARTESIAN_POINT ( 'NONE',  ( -8.012344526598182026E-15, 8.546875000341403350, -1.575800808251669460 ) ) ;
#136980=CARTESIAN_POINT ( 'NONE',  ( 1.364683531249997417, 12.54687500034139980, 2.602085213965210642E-15 ) ) ;
#137014=CYLINDRICAL_SURFACE ( 'NONE', #186377, 0.5000000000000003331 ) ;
#137064=CARTESIAN_POINT ( 'NONE',  ( 1.220146605508150803E-14, 9.468750000682799595, -1.499999999999998446 ) ) ;
#137090=CARTESIAN_POINT ( 'NONE',  ( 1.499999999999996891, 12.92708333401612997, -0.8660254037844378194 ) ) ;
#137092=SHAPE_REPRESENTATION ( 'positive pin', ( #200407 ), #197031 ) ;
#137094=VECTOR ( 'NONE', #121889, 1000.000000000000000 ) ;
#137104=CARTESIAN_POINT ( 'NONE',  ( -2.788906526875773208E-15, 11.96875000068279604, -1.499999999999998446 ) ) ;
#137145=CARTESIAN_POINT ( 'NONE',  ( 1.500000000000001332, 8.906250000682797818, 0.000000000000000000 ) ) ;
#137151=CARTESIAN_POINT ( 'NONE',  ( 1.382866120668046150, 4.316195966766219527, 0.2144190051505707739 ) ) ;
#137172=CARTESIAN_POINT ( 'NONE',  ( -0.6823417656250003738, 12.65104166700806232, 1.181850606188754593 ) ) ;
#137177=CARTESIAN_POINT ( 'NONE',  ( 1.499999999999997113, 10.14583333333333570, -0.8660254037844378194 ) ) ;
#137214=EDGE_LOOP ( 'NONE', ( #210466, #46879, #355, #209000 ) ) ;
#137231=CARTESIAN_POINT ( 'NONE',  ( 0.6823417656249934904, 8.755208333674733723, 1.181850606188764807 ) ) ;
#137300=CYLINDRICAL_SURFACE ( 'NONE', #4549, 1.500000000000000222 ) ;
#137302=CYLINDRICAL_SURFACE ( 'NONE', #34087, 0.5000000000000003331 ) ;
#137349=CARTESIAN_POINT ( 'NONE',  ( -0.4019237886467001974, 11.33258545099816317, 1.500000000000001998 ) ) ;
#137373=( BOUNDED_CURVE ( )  B_SPLINE_CURVE ( 2, ( #71476, #155962, #88838, #188446, #7548 ),
 .UNSPECIFIED., .F., .T. ) 
 B_SPLINE_CURVE_WITH_KNOTS ( ( 3, 2, 3 ),
 ( 0.2915250305792598251, 0.2916666666666666852, 0.2946428571428571508 ),
 .UNSPECIFIED. ) 
 CURVE ( )  GEOMETRIC_REPRESENTATION_ITEM ( )  RATIONAL_B_SPLINE_CURVE ( ( 0.9937758973840666865, 0.9968120928798591684, 1.000000000000000000, 0.9330127018922194093, 0.9330127018922194093 ) ) 
 REPRESENTATION_ITEM ( '' )  );
#137388=CARTESIAN_POINT ( 'NONE',  ( 1.364683531249996529, 13.46354166700806765, 0.7879004041258405033 ) ) ;
#137407=LINE ( 'NONE', #5220, #199899 ) ;
#137431=CARTESIAN_POINT ( 'NONE',  ( -6.009258394948636914E-15, 13.68750000000000178, -1.732050807568875195 ) ) ;
#137439=CARTESIAN_POINT ( 'NONE',  ( -1.364683531250000748, 11.60937500034139802, 0.000000000000000000 ) ) ;
#137487=CARTESIAN_POINT ( 'NONE',  ( -1.364683531250010740, 12.94270833367473550, 0.7879004041258445001 ) ) ;
#137504=CARTESIAN_POINT ( 'NONE',  ( -0.4019237886466871523, 10.19866454968463110, -1.499999999999998668 ) ) ;
#137512=CARTESIAN_POINT ( 'NONE',  ( -8.012344526598182026E-15, 12.79687500034139802, -1.575800808251669460 ) ) ;
#137525=DIRECTION ( 'NONE',  ( 0.000000000000000000, 0.000000000000000000, 1.000000000000000000 ) ) ;
#137586=CARTESIAN_POINT ( 'NONE',  ( -8.012344526598182026E-15, 9.796875000341399797, -1.575800808251669460 ) ) ;
#137592=CARTESIAN_POINT ( 'NONE',  ( -1.500000000000008216, 9.031250000682797818, 3.469446951953614189E-15 ) ) ;
#137646=ORIENTED_EDGE ( 'NONE', *, *, #125292, .T. ) ;
#137668=DIRECTION ( 'NONE',  ( 0.000000000000000000, 0.000000000000000000, 1.000000000000000000 ) ) ;
#137698=CARTESIAN_POINT ( 'NONE',  ( -1.115562610750309283E-14, 11.06250000000000178, 1.500000000000001554 ) ) ;
#137736=CARTESIAN_POINT ( 'NONE',  ( -8.012344526598182026E-15, 11.35937500034139980, -1.575800808251669460 ) ) ;
#137761=CARTESIAN_POINT ( 'NONE',  ( 1.364683531249997417, 13.98437500034140157, 2.602085213965210642E-15 ) ) ;
#137803=CARTESIAN_POINT ( 'NONE',  ( 1.364683531249996529, 8.526041667008065872, 0.7879004041258405033 ) ) ;
#137809=CARTESIAN_POINT ( 'NONE',  ( -1.455271222711091106, 4.347661690319585048, 0.3949897977301430885 ) ) ;
#137847=CARTESIAN_POINT ( 'NONE',  ( -1.402160292154681736E-14, 15.17187500034140157, 1.575800808251682339 ) ) ;
#137859=CARTESIAN_POINT ( 'NONE',  ( -1.422919017935815766, 3.902251674285432514, -0.5004465702263605209 ) ) ;
#137883=CYLINDRICAL_SURFACE ( 'NONE', #129185, 2.000000000000000000 ) ;
#137909=CARTESIAN_POINT ( 'NONE',  ( 1.499999999999993117, 11.38541666734946567, 0.8660254037844408170 ) ) ;
#137916=CARTESIAN_POINT ( 'NONE',  ( 0.7500000000000006661, 10.58333333333333393, 1.299038105676657340 ) ) ;
#137925=ORIENTED_EDGE ( 'NONE', *, *, #175342, .T. ) ;
#137942=VERTEX_POINT ( 'NONE', #79715 ) ;
#137985=CARTESIAN_POINT ( 'NONE',  ( 0.6823417656249934904, 14.50520833367473195, 1.181850606188764807 ) ) ;
#138047=CARTESIAN_POINT ( 'NONE',  ( -1.364683531250010295, 13.19270833367472839, 0.7879004041258445001 ) ) ;
#138173=CARTESIAN_POINT ( 'NONE',  ( -1.264911064067355984, 3.850000000000006306, -0.5000000000000004441 ) ) ;
#138238=CARTESIAN_POINT ( 'NONE',  ( -0.6823417656250039265, 10.81770833367473550, -1.181850606188755259 ) ) ;
#138245=CARTESIAN_POINT ( 'NONE',  ( -6.009258394948636914E-15, 9.687499999999996447, -1.732050807568875195 ) ) ;
#138293=CARTESIAN_POINT ( 'NONE',  ( -1.402160292154681736E-14, 9.484375000341398021, 1.575800808251682339 ) ) ;
#138307=CARTESIAN_POINT ( 'NONE',  ( -0.7500000000000006661, 12.48958333401613352, -1.299038105676657340 ) ) ;
#138343=CYLINDRICAL_SURFACE ( 'NONE', #203373, 1.500000000000000222 ) ;
#138497=CARTESIAN_POINT ( 'NONE',  ( -1.500000000000015099, 13.97916666666666607, -0.8660254037844309360 ) ) ;
#138502=CARTESIAN_POINT ( 'NONE',  ( 1.364683531249997417, 9.984375000341398021, 2.602085213965210642E-15 ) ) ;
#138508=ORIENTED_EDGE ( 'NONE', *, *, #208007, .T. ) ;
#138575=CARTESIAN_POINT ( 'NONE',  ( 0.6823417656249969321, 13.27604166700806232, -1.181850606188757036 ) ) ;
#138630=( BOUNDED_CURVE ( )  B_SPLINE_CURVE ( 2, ( #32849, #134645, #102112, #130434, #149808, #166048, #180171, #131467, #168182 ),
 .UNSPECIFIED., .F., .T. ) 
 B_SPLINE_CURVE_WITH_KNOTS ( ( 3, 2, 2, 2, 3 ),
 ( 0.4732142857142856984, 0.4761904761904761640, 0.4821428571428571508, 0.4880952380952380820, 0.4910714285714285476 ),
 .UNSPECIFIED. ) 
 CURVE ( )  GEOMETRIC_REPRESENTATION_ITEM ( )  RATIONAL_B_SPLINE_CURVE ( ( 0.9330127018922194093, 0.9330127018922194093, 1.000000000000000000, 0.8660254037844387076, 1.000000000000000000, 0.8660254037844387076, 1.000000000000000000, 0.9330127018922199644, 0.9330127018922194093 ) ) 
 REPRESENTATION_ITEM ( '' )  );
#138650=CARTESIAN_POINT ( 'NONE',  ( -1.364683531250000748, 10.35937500034139802, 0.000000000000000000 ) ) ;
#138766=CARTESIAN_POINT ( 'NONE',  ( -1.500000000000015099, 10.97916666666666785, -0.8660254037844309360 ) ) ;
#138799=CARTESIAN_POINT ( 'NONE',  ( 1.364683531250000303, 11.06770833367473550, -0.7879004041258355073 ) ) ;
#138820=CARTESIAN_POINT ( 'NONE',  ( 0.4841233049523195886, 3.595619050313132448, 0.4351758553768796944 ) ) ;
#138825=CARTESIAN_POINT ( 'NONE',  ( -1.364683531250010295, 14.63020833367473550, 0.7879004041258445001 ) ) ;
#138843=CARTESIAN_POINT ( 'NONE',  ( 1.499999999999996891, 9.927083334016131744, -0.8660254037844378194 ) ) ;
#138857=ORIENTED_EDGE ( 'NONE', *, *, #36800, .F. ) ;
#138871=CARTESIAN_POINT ( 'NONE',  ( 1.364683531250000303, 9.067708333674733723, -0.7879004041258355073 ) ) ;
#138877=CARTESIAN_POINT ( 'NONE',  ( -1.378881877344243945, 4.087185210397143109, 0.5904953584335903560 ) ) ;
#138918=CARTESIAN_POINT ( 'NONE',  ( 0.6823417656249969321, 14.77604166700806410, -1.181850606188757036 ) ) ;
#139056=CARTESIAN_POINT ( 'NONE',  ( -0.6823417656250039265, 8.567708333674733723, -1.181850606188755259 ) ) ;
#139062=( BOUNDED_CURVE ( )  B_SPLINE_CURVE ( 2, ( #88490, #6130, #201128, #72199, #23453, #1855, #138307, #171859, #52766 ),
 .UNSPECIFIED., .F., .T. ) 
 B_SPLINE_CURVE_WITH_KNOTS ( ( 3, 2, 2, 2, 3 ),
 ( 0.3839285714285713969, 0.3869047619047619180, 0.3928571428571428492, 0.3988095238095238360, 0.4017857142857143016 ),
 .UNSPECIFIED. ) 
 CURVE ( )  GEOMETRIC_REPRESENTATION_ITEM ( )  RATIONAL_B_SPLINE_CURVE ( ( 0.9330127018922194093, 0.9330127018922187432, 1.000000000000000000, 0.8660254037844387076, 1.000000000000000000, 0.8660254037844387076, 1.000000000000000000, 0.9330127018922194093, 0.9330127018922194093 ) ) 
 REPRESENTATION_ITEM ( '' )  );
#139065=AXIS2_PLACEMENT_3D ( 'NONE', #33668, #134413, #167943 ) ;
#139114=CARTESIAN_POINT ( 'NONE',  ( -1.402160292154681736E-14, 12.48437500034139624, 1.575800808251682339 ) ) ;
#139162=CARTESIAN_POINT ( 'NONE',  ( -0.6681007961528204753, -4.204658361604701966, 0.8428154764861340853 ) ) ;
#139208=AXIS2_PLACEMENT_3D ( 'NONE', #111541, #127824, #129941 ) ;
#139290=CYLINDRICAL_SURFACE ( 'NONE', #9898, 1.500000000000000222 ) ;
#139297=DIRECTION ( 'NONE',  ( 0.000000000000000000, 0.000000000000000000, 1.000000000000000000 ) ) ;
#139307=CARTESIAN_POINT ( 'NONE',  ( -1.402160292154681736E-14, 10.92187500034139802, 1.575800808251682339 ) ) ;
#139335=CARTESIAN_POINT ( 'NONE',  ( -3.602337597214539753E-15, 11.84375000068279604, 1.500000000000001554 ) ) ;
#139352=ORIENTED_EDGE ( 'NONE', *, *, #55232, .F. ) ;
#139364=CARTESIAN_POINT ( 'NONE',  ( -0.6823417656250003738, 8.463541667008064096, 1.181850606188754593 ) ) ;
#139385=CARTESIAN_POINT ( 'NONE',  ( 0.7500000000000006661, 13.16666666666666607, -1.299038105676657340 ) ) ;
#139460=EDGE_CURVE ( 'NONE', #209493, #178739, #138630, .T. ) ;
#139483=UNCERTAINTY_MEASURE_WITH_UNIT (LENGTH_MEASURE( 1.000000000000000082E-05 ), #111266, 'distance_accuracy_value', 'NONE');
#139525=CARTESIAN_POINT ( 'NONE',  ( -0.7500000000000006661, 12.45833333333333570, -1.299038105676657340 ) ) ;
#139573=CARTESIAN_POINT ( 'NONE',  ( -1.402160292154681736E-14, 14.06250000000000355, 1.732050807568881190 ) ) ;
#139579=CARTESIAN_POINT ( 'NONE',  ( -0.6823417656250039265, 10.56770833367473550, -1.181850606188755259 ) ) ;
#139627=CARTESIAN_POINT ( 'NONE',  ( 1.364683531249996529, 12.02604166700806587, 0.7879004041258403923 ) ) ;
#139695=CARTESIAN_POINT ( 'NONE',  ( -6.009258394948636914E-15, 15.21875000068279782, -1.732050807568875195 ) ) ;
#139729=CARTESIAN_POINT ( 'NONE',  ( -0.6823417656250003738, 10.65104166700806765, 1.181850606188754593 ) ) ;
#139831=DIRECTION ( 'NONE',  ( 0.000000000000000000, 0.000000000000000000, 1.000000000000000000 ) ) ;
#139874=CARTESIAN_POINT ( 'NONE',  ( 0.6823417656249969321, 9.588541667008065872, -1.181850606188757036 ) ) ;
#139889=VERTEX_POINT ( 'NONE', #39247 ) ;
#139896=CARTESIAN_POINT ( 'NONE',  ( 1.499999999999996891, 9.177083334016128191, -0.8660254037844378194 ) ) ;
#139899=CARTESIAN_POINT ( 'NONE',  ( 1.364683531249996529, 14.71354166700806410, 0.7879004041258405033 ) ) ;
#139902=VECTOR ( 'NONE', #22933, 1000.000000000000000 ) ;
#139947=CARTESIAN_POINT ( 'NONE',  ( 1.500000000000001332, 14.37499999999999822, 0.000000000000000000 ) ) ;
#139995=CARTESIAN_POINT ( 'NONE',  ( 1.364683531250000303, 14.50520833367473372, -0.7879004041258355073 ) ) ;
#140005=CARTESIAN_POINT ( 'NONE',  ( -1.424698021954212912, 3.957288782964809570, -0.4926413923218403434 ) ) ;
#140090=CARTESIAN_POINT ( 'NONE',  ( -1.355377658251182726, 3.766337118550212359, 0.6426130056881884656 ) ) ;
#140135=CARTESIAN_POINT ( 'NONE',  ( -1.364683531250014514, 14.65104166700806410, -0.7879004041258335089 ) ) ;
#140144=CARTESIAN_POINT ( 'NONE',  ( 0.7500000000000006661, 12.44791666734946389, -1.299038105676657340 ) ) ;
#140177=ORIENTED_EDGE ( 'NONE', *, *, #34340, .T. ) ;
#140188=DIRECTION ( 'NONE',  ( 0.000000000000000000, -1.000000000000000000, 0.000000000000000000 ) ) ;
#140201=CARTESIAN_POINT ( 'NONE',  ( -0.6823417656250039265, 11.63020833367473017, -1.181850606188755259 ) ) ;
#140244=CARTESIAN_POINT ( 'NONE',  ( -0.7500000000000179856, 11.57291666734946212, 1.299038105676658228 ) ) ;
#140315=EDGE_CURVE ( 'NONE', #12932, #170920, #130799, .T. ) ;
#140351=( BOUNDED_CURVE ( )  B_SPLINE_CURVE ( 2, ( #5198, #55056, #71273, #188239, #170928, #169861, #139525, #37736, #205551 ),
 .UNSPECIFIED., .F., .T. ) 
 B_SPLINE_CURVE_WITH_KNOTS ( ( 3, 2, 2, 2, 3 ),
 ( 0.4196428571428570953, 0.4226190476190476164, 0.4285714285714285476, 0.4345238095238095344, 0.4375000000000000000 ),
 .UNSPECIFIED. ) 
 CURVE ( )  GEOMETRIC_REPRESENTATION_ITEM ( )  RATIONAL_B_SPLINE_CURVE ( ( 0.9330127018922194093, 0.9330127018922180770, 1.000000000000000000, 0.8660254037844387076, 1.000000000000000000, 0.8660254037844387076, 1.000000000000000000, 0.9330127018922194093, 0.9330127018922194093 ) ) 
 REPRESENTATION_ITEM ( '' )  );
#140366=AXIS2_PLACEMENT_3D ( 'NONE', #77393, #143510, #44924 ) ;
#140392=CARTESIAN_POINT ( 'NONE',  ( -1.402160292154681736E-14, 11.17187500034139802, 1.575800808251682339 ) ) ;
#140398=CARTESIAN_POINT ( 'NONE',  ( -0.7500000000000179856, 8.541666666666669627, 1.299038105676658228 ) ) ;
#140423=CARTESIAN_POINT ( 'NONE',  ( -0.4019237886466933696, 8.832585450998172050, 1.500000000000005995 ) ) ;
#140470=EDGE_CURVE ( 'NONE', #120384, #33125, #81632, .T. ) ;
#140539=( BOUNDED_CURVE ( )  B_SPLINE_CURVE ( 2, ( #18435, #97592, #47787, #203309, #64006, #130155, #90677, #88536, #92815 ),
 .UNSPECIFIED., .F., .T. ) 
 B_SPLINE_CURVE_WITH_KNOTS ( ( 3, 2, 2, 2, 3 ),
 ( 0.7767857142857143016, 0.7797619047619047672, 0.7857142857142856984, 0.7916666666666666297, 0.7946428571428572063 ),
 .UNSPECIFIED. ) 
 CURVE ( )  GEOMETRIC_REPRESENTATION_ITEM ( )  RATIONAL_B_SPLINE_CURVE ( ( 0.9330127018922194093, 0.9330127018922194093, 1.000000000000000000, 0.8660254037844387076, 1.000000000000000000, 0.8660254037844387076, 1.000000000000000000, 0.9330127018922180770, 0.9330127018922194093 ) ) 
 REPRESENTATION_ITEM ( '' )  );
#140657=CARTESIAN_POINT ( 'NONE',  ( 0.7500000000000006661, 12.66666666666666607, -1.299038105676657340 ) ) ;
#140662=CARTESIAN_POINT ( 'NONE',  ( 1.364683531249996529, 10.71354166700806942, 0.7879004041258405033 ) ) ;
#140687=CYLINDRICAL_SURFACE ( 'NONE', #100309, 1.500000000000000222 ) ;
#140707=CARTESIAN_POINT ( 'NONE',  ( 0.6823417656249934904, 11.50520833367473017, 1.181850606188764807 ) ) ;
#140734=CARTESIAN_POINT ( 'NONE',  ( 1.836970198721030181E-16, 13.49999999999999822, 1.500000000000000222 ) ) ;
#140753=ORIENTED_EDGE ( 'NONE', *, *, #111106, .F. ) ;
#140764=DIRECTION ( 'NONE',  ( 0.000000000000000000, -1.000000000000000000, 0.000000000000000000 ) ) ;
#140773=CARTESIAN_POINT ( 'NONE',  ( -1.500000000000008216, 14.78125000068279604, 3.469446951953614189E-15 ) ) ;
#140781=CYLINDRICAL_SURFACE ( 'NONE', #203126, 1.500000000000000222 ) ;
#140807=CARTESIAN_POINT ( 'NONE',  ( -0.6823417656250003738, 9.901041667008065872, 1.181850606188754593 ) ) ;
#140839=CARTESIAN_POINT ( 'NONE',  ( 1.133562540163749688, 13.34197803161386453, -0.8395043811131129852 ) ) ;
#140850=VERTEX_POINT ( 'NONE', #207019 ) ;
#140943=CARTESIAN_POINT ( 'NONE',  ( 0.4019237886466816012, 10.45758545099816672, -1.499999999999998668 ) ) ;
#140946=CARTESIAN_POINT ( 'NONE',  ( -1.500000000000015099, 11.72916666666666430, -0.8660254037844309360 ) ) ;
#140952=CARTESIAN_POINT ( 'NONE',  ( -2.788906526875773208E-15, 10.46875000068279604, -1.499999999999998446 ) ) ;
#140953=( BOUNDED_CURVE ( )  B_SPLINE_CURVE ( 2, ( #30031, #141688, #108147, #28963, #193586, #158965, #74513, #58260, #93987 ),
 .UNSPECIFIED., .F., .T. ) 
 B_SPLINE_CURVE_WITH_KNOTS ( ( 3, 2, 2, 2, 3 ),
 ( 0.7053571428571427937, 0.7083333333333333703, 0.7142857142857143016, 0.7202380952380952328, 0.7232142857142856984 ),
 .UNSPECIFIED. ) 
 CURVE ( )  GEOMETRIC_REPRESENTATION_ITEM ( )  RATIONAL_B_SPLINE_CURVE ( ( 0.9330127018922194093, 0.9330127018922180770, 1.000000000000000000, 0.8660254037844387076, 1.000000000000000000, 0.8660254037844387076, 1.000000000000000000, 0.9330127018922194093, 0.9330127018922194093 ) ) 
 REPRESENTATION_ITEM ( '' )  );
#140960=CARTESIAN_POINT ( 'NONE',  ( -1.364683531250010295, 9.942708333674728394, 0.7879004041258445001 ) ) ;
#140968=CARTESIAN_POINT ( 'NONE',  ( -0.7027773505823969868, 13.37576698399828246, -1.183650206560545426 ) ) ;
#140971=CARTESIAN_POINT ( 'NONE',  ( 0.000000000000000000, -4.500000000000003553, 0.000000000000000000 ) ) ;
#140985=CARTESIAN_POINT ( 'NONE',  ( 1.364683531250000303, 15.00520833367472839, -0.7879004041258355073 ) ) ;
#141006=CARTESIAN_POINT ( 'NONE',  ( 1.499999999999993117, 9.885416667349465669, 0.8660254037844408170 ) ) ;
#141023=CARTESIAN_POINT ( 'NONE',  ( -1.500000000000015099, 13.01041666734946567, -0.8660254037844309360 ) ) ;
#141033=CARTESIAN_POINT ( 'NONE',  ( -1.500000000000001110, 14.52083333333333215, 0.8660254037844419273 ) ) ;
#141075=CARTESIAN_POINT ( 'NONE',  ( 1.364683531249997417, 14.23437500034140157, 2.602085213965210642E-15 ) ) ;
#141077=ORIENTED_EDGE ( 'NONE', *, *, #61168, .T. ) ;
#141174=CARTESIAN_POINT ( 'NONE',  ( -2.788906526875773208E-15, 8.468750000682796042, -1.499999999999998446 ) ) ;
#141221=CARTESIAN_POINT ( 'NONE',  ( 1.364683531249996529, 14.02604166700806942, 0.7879004041258405033 ) ) ;
#141286=CARTESIAN_POINT ( 'NONE',  ( -0.6823417656250039265, 12.38020833367473017, -1.181850606188755259 ) ) ;
#141327=CARTESIAN_POINT ( 'NONE',  ( 0.7500000000000006661, 10.61458333401613174, 1.299038105676657340 ) ) ;
#141409=EDGE_CURVE ( 'NONE', #36526, #57617, #116524, .T. ) ;
#141455=CARTESIAN_POINT ( 'NONE',  ( -2.788906526875773208E-15, 8.937500000000001776, -1.499999999999998446 ) ) ;
#141471=CARTESIAN_POINT ( 'NONE',  ( 0.6823417656249934904, 10.19270833367473550, 1.181850606188764807 ) ) ;
#141503=CARTESIAN_POINT ( 'NONE',  ( -0.4019237886466871523, 8.479914550367427140, -1.499999999999998668 ) ) ;
#141530=CARTESIAN_POINT ( 'NONE',  ( -8.012344526598182026E-15, 8.609375000341403350, -1.575800808251669460 ) ) ;
#141550=CARTESIAN_POINT ( 'NONE',  ( 3.834746474454188013E-15, 13.06250000000000178, 1.500000000000001554 ) ) ;
#141688=CARTESIAN_POINT ( 'NONE',  ( -0.4019237886466933696, 10.55133545031537423, 1.500000000000005995 ) ) ;
#141697=VECTOR ( 'NONE', #212088, 1000.000000000000000 ) ;
#141731=CARTESIAN_POINT ( 'NONE',  ( -1.500000000000001110, 12.27083333333333925, 0.8660254037844419273 ) ) ;
#141737=CARTESIAN_POINT ( 'NONE',  ( -1.364683531250010295, 10.38020833367473195, 0.7879004041258445001 ) ) ;
#141742=ORIENTED_EDGE ( 'NONE', *, *, #153335, .T. ) ;
#141775=CARTESIAN_POINT ( 'NONE',  ( 0.6823417656249969321, 12.33854166700806765, -1.181850606188757036 ) ) ;
#141811=ORIENTED_EDGE ( 'NONE', *, *, #51634, .T. ) ;
#141846=CARTESIAN_POINT ( 'NONE',  ( 0.7500000000000006661, 14.36458333401613530, 1.299038105676657340 ) ) ;
#141876=CARTESIAN_POINT ( 'NONE',  ( 1.364683531249996529, 10.21354166700806587, 0.7879004041258405033 ) ) ;
#142013=DIRECTION ( 'NONE',  ( 0.000000000000000000, 0.000000000000000000, -1.000000000000000000 ) ) ;
#142020=CARTESIAN_POINT ( 'NONE',  ( -1.364683531250000748, 9.671875000341396245, 0.000000000000000000 ) ) ;
#142027=CARTESIAN_POINT ( 'NONE',  ( -0.8478968130440378559, 13.27085527049493230, 1.205503722529886135 ) ) ;
#142029=DIRECTION ( 'NONE',  ( 0.000000000000000000, 1.000000000000000000, 0.000000000000000000 ) ) ;
#142037=CARTESIAN_POINT ( 'NONE',  ( 0.6499431002536731894, 3.350073969687604958, 0.06915891592279559130 ) ) ;
#142064=VERTEX_POINT ( 'NONE', #58456 ) ;
#142087=EDGE_CURVE ( 'NONE', #110148, #19108, #137373, .T. ) ;
#142089=CARTESIAN_POINT ( 'NONE',  ( -1.402160292154681736E-14, 15.31250000000000000, 1.732050807568881190 ) ) ;
#142093=AXIS2_PLACEMENT_3D ( 'NONE', #100784, #2189, #132265 ) ;
#142132=CARTESIAN_POINT ( 'NONE',  ( -8.012344526598182026E-15, 14.79687500034140157, -1.575800808251669460 ) ) ;
#142223=CARTESIAN_POINT ( 'NONE',  ( -0.4019237886466871523, 12.19866454968463110, -1.499999999999998668 ) ) ;
#142231=( BOUNDED_CURVE ( )  B_SPLINE_CURVE ( 2, ( #131136, #98573, #49815, #16219, #214397, #66026, #115941, #90866, #70300 ),
 .UNSPECIFIED., .F., .T. ) 
 B_SPLINE_CURVE_WITH_KNOTS ( ( 3, 2, 2, 2, 3 ),
 ( 0.4553571428571427937, 0.4583333333333333148, 0.4642857142857143016, 0.4702380952380952328, 0.4732142857142856984 ),
 .UNSPECIFIED. ) 
 CURVE ( )  GEOMETRIC_REPRESENTATION_ITEM ( )  RATIONAL_B_SPLINE_CURVE ( ( 0.9330127018922194093, 0.9330127018922180770, 1.000000000000000000, 0.8660254037844387076, 1.000000000000000000, 0.8660254037844387076, 1.000000000000000000, 0.9330127018922194093, 0.9330127018922194093 ) ) 
 REPRESENTATION_ITEM ( '' )  );
#142260=PRODUCT_DEFINITION_SHAPE ( 'NONE', 'NONE',  #52109 ) ;
#142274=CARTESIAN_POINT ( 'NONE',  ( -8.012344526598182026E-15, 13.60937500034139447, -1.575800808251669460 ) ) ;
#142326=CARTESIAN_POINT ( 'NONE',  ( -2.788906526875773208E-15, 12.68749999999999822, -1.499999999999998446 ) ) ;
#142343=CARTESIAN_POINT ( 'NONE',  ( 1.364683531249996529, 11.77604166700806410, 0.7879004041258405033 ) ) ;
#142379=CARTESIAN_POINT ( 'NONE',  ( -0.7500000000000006661, 11.20833333333333393, -1.299038105676657340 ) ) ;
#142384=CARTESIAN_POINT ( 'NONE',  ( -1.402160292154681736E-14, 11.59375000068279427, 1.732050807568881190 ) ) ;
#142483=CARTESIAN_POINT ( 'NONE',  ( 1.352862181796068208, 4.252167665669599472, -0.3040832447043536058 ) ) ;
#142504=CARTESIAN_POINT ( 'NONE',  ( -1.362971619486218700, 3.697045066695971105, 0.6272962186313906230 ) ) ;
#142520=CARTESIAN_POINT ( 'NONE',  ( -1.364683531250010740, 10.13020833367472839, 0.7879004041258445001 ) ) ;
#142527=CARTESIAN_POINT ( 'NONE',  ( -0.7500000000000006661, 8.708333333333332149, -1.299038105676657340 ) ) ;
#142539=EDGE_LOOP ( 'NONE', ( #171808, #54270, #46379, #5620 ) ) ;
#142595=CARTESIAN_POINT ( 'NONE',  ( -1.364683531250000748, 15.42187500034139447, 0.000000000000000000 ) ) ;
#142603=CARTESIAN_POINT ( 'NONE',  ( 0.4019237886466816012, 13.17633545031536890, -1.499999999999998668 ) ) ;
#142719=CARTESIAN_POINT ( 'NONE',  ( 0.000000000000000000, -4.500000000000003553, 0.000000000000000000 ) ) ;
#142790=CARTESIAN_POINT ( 'NONE',  ( 0.7500000000000006661, 12.83333333333333570, 1.299038105676657340 ) ) ;
#142797=CARTESIAN_POINT ( 'NONE',  ( 0.6823417656249934904, 10.94270833367473550, 1.181850606188764807 ) ) ;
#142807=CARTESIAN_POINT ( 'NONE',  ( -1.115562610750309283E-14, 10.84375000068279604, 1.500000000000001554 ) ) ;
#142834=CARTESIAN_POINT ( 'NONE',  ( 1.364683531249997417, 11.54687500034139802, 2.602085213965210642E-15 ) ) ;
#142885=DIRECTION ( 'NONE',  ( 0.000000000000000000, 0.000000000000000000, 1.000000000000000000 ) ) ;
#142907=CARTESIAN_POINT ( 'NONE',  ( -1.500000000000001110, 14.30208333401613530, 0.8660254037844419273 ) ) ;
#142940=CARTESIAN_POINT ( 'NONE',  ( -1.364683531250010295, 9.380208333674735499, 0.7879004041258445001 ) ) ;
#142943=ORIENTED_EDGE ( 'NONE', *, *, #91910, .T. ) ;
#143041=CARTESIAN_POINT ( 'NONE',  ( 1.530808498934191324E-16, -1.500000000000001332, -1.249999999999999778 ) ) ;
#143096=CARTESIAN_POINT ( 'NONE',  ( 1.364683531249996529, 10.02604166700806587, 0.7879004041258405033 ) ) ;
#143103=CARTESIAN_POINT ( 'NONE',  ( -0.7511099776682679252, 13.27260870304410822, 1.266036383821782296 ) ) ;
#143111=VERTEX_POINT ( 'NONE', #45146 ) ;
#143117=CARTESIAN_POINT ( 'NONE',  ( 0.6384131795730921821, 3.364835436752191988, 0.1378994657016461289 ) ) ;
#143139=CARTESIAN_POINT ( 'NONE',  ( -1.115562610750309283E-14, 10.31250000000000000, 1.500000000000001554 ) ) ;
#143142=ORIENTED_EDGE ( 'NONE', *, *, #23723, .T. ) ;
#143166=CARTESIAN_POINT ( 'NONE',  ( 1.499999999999993117, 15.10416666666666430, 0.8660254037844409281 ) ) ;
#143213=CARTESIAN_POINT ( 'NONE',  ( 1.364683531250000303, 12.75520833367473550, -0.7879004041258355073 ) ) ;
#143252=CARTESIAN_POINT ( 'NONE',  ( -1.264911064067348656, 3.850000000000018296, 0.5000000000000064393 ) ) ;
#143307=CARTESIAN_POINT ( 'NONE',  ( -1.456203110946918233, 3.350064908098031147, 0.3915051095678106496 ) ) ;
#143325=CARTESIAN_POINT ( 'NONE',  ( 1.265302052550089540, 3.921372892477353655, -0.4993130731308050296 ) ) ;
#143348=CARTESIAN_POINT ( 'NONE',  ( 1.364683531250000303, 13.81770833367473017, -0.7879004041258355073 ) ) ;
#143413=CARTESIAN_POINT ( 'NONE',  ( 0.6823417656249934904, 11.50520833367473017, 1.181850606188764807 ) ) ;
#143455=CARTESIAN_POINT ( 'NONE',  ( -1.500000000000001110, 11.55208333401612997, 0.8660254037844419273 ) ) ;
#143510=DIRECTION ( 'NONE',  ( 1.665334536937734811E-16, 0.000000000000000000, 1.000000000000000000 ) ) ;
#143514=CARTESIAN_POINT ( 'NONE',  ( 0.8145602173408479363, -4.140925090156039268, 0.5891403177412622982 ) ) ;
#143561=CARTESIAN_POINT ( 'NONE',  ( 1.355678468426070982, 3.764857968299145430, 0.6419787906858488435 ) ) ;
#143581=CARTESIAN_POINT ( 'NONE',  ( -1.409285775387294715, 3.485450175183121946, 0.5173959003036648907 ) ) ;
#143600=CARTESIAN_POINT ( 'NONE',  ( -1.364683531250010740, 9.630208333674735499, 0.7879004041258445001 ) ) ;
#143676=CARTESIAN_POINT ( 'NONE',  ( -1.364683531250014514, 15.40104166700806765, -0.7879004041258335089 ) ) ;
#143687=CARTESIAN_POINT ( 'NONE',  ( 0.4019237886466847653, 13.07366454968462932, 1.499999999999997113 ) ) ;
#143865=CARTESIAN_POINT ( 'NONE',  ( -6.009258394948636914E-15, 12.43750000000000178, -1.732050807568875195 ) ) ;
#143871=CARTESIAN_POINT ( 'NONE',  ( 1.364683531249997417, 8.734375000341396245, 2.602085213965210642E-15 ) ) ;
#143876=ORIENTED_EDGE ( 'NONE', *, *, #80770, .T. ) ;
#143881=CARTESIAN_POINT ( 'NONE',  ( -0.4340280775911248834, 3.713184418947140575, 0.4851569899464777125 ) ) ;
#143909=CARTESIAN_POINT ( 'NONE',  ( 0.6823417656249934904, 12.00520833367473017, 1.181850606188764807 ) ) ;
#143921=FACE_OUTER_BOUND ( 'NONE', #23822, .T. ) ;
#143980=CARTESIAN_POINT ( 'NONE',  ( -0.7500000000000006661, 14.48958333401613530, -1.299038105676657340 ) ) ;
#144014=CARTESIAN_POINT ( 'NONE',  ( -1.364683531250014514, 9.338541667008062319, -0.7879004041258335089 ) ) ;
#144024=CARTESIAN_POINT ( 'NONE',  ( 0.7500000000000006661, 10.86458333401613174, 1.299038105676657340 ) ) ;
#144059=VERTEX_POINT ( 'NONE', #50993 ) ;
#144168=CARTESIAN_POINT ( 'NONE',  ( -0.6823417656250039265, 9.630208333674728394, -1.181850606188755259 ) ) ;
#144176=CARTESIAN_POINT ( 'NONE',  ( 3.834746474454188013E-15, 10.59375000068279604, 1.500000000000001554 ) ) ;
#144260=ORIENTED_EDGE ( 'NONE', *, *, #129599, .T. ) ;
#144265=CARTESIAN_POINT ( 'NONE',  ( -1.115562610750309283E-14, 11.06250000000000178, 1.500000000000001554 ) ) ;
#144284=CARTESIAN_POINT ( 'NONE',  ( 0.6823417656249934904, 12.69270833367473017, 1.181850606188764807 ) ) ;
#144295=CARTESIAN_POINT ( 'NONE',  ( -1.495015925693001790, 4.335188216343587086, 0.1395187543289083953 ) ) ;
#144401=CARTESIAN_POINT ( 'NONE',  ( 1.449478204280065352, 3.367485310445687663, 0.3909668688984510587 ) ) ;
#144423=CARTESIAN_POINT ( 'NONE',  ( -1.364683531250000748, 14.17187500034140157, 0.000000000000000000 ) ) ;
#144484=CARTESIAN_POINT ( 'NONE',  ( -0.6823417656250003738, 11.96354166700806765, 1.181850606188754593 ) ) ;
#144528=CARTESIAN_POINT ( 'NONE',  ( -0.7500000000000006661, 10.23958333401612997, -1.299038105676657340 ) ) ;
#144627=CARTESIAN_POINT ( 'NONE',  ( 1.393530502278612637, 4.337808571543051883, -0.1277288169565287124 ) ) ;
#144645=CARTESIAN_POINT ( 'NONE',  ( -1.449495214452822145, 3.367398793782839128, -0.3909641857570709811 ) ) ;
#144664=CARTESIAN_POINT ( 'NONE',  ( -1.364683531250010740, 8.880208333674731946, 0.7879004041258445001 ) ) ;
#144837=( BOUNDED_CURVE ( )  B_SPLINE_CURVE ( 2, ( #121451, #24914, #91018, #105136, #175461, #157080, #187421, #39051, #171176 ),
 .UNSPECIFIED., .F., .T. ) 
 B_SPLINE_CURVE_WITH_KNOTS ( ( 3, 2, 2, 2, 3 ),
 ( 0.4910714285714285476, 0.4940476190476190688, 0.5000000000000000000, 0.5059523809523809312, 0.5089285714285713969 ),
 .UNSPECIFIED. ) 
 CURVE ( )  GEOMETRIC_REPRESENTATION_ITEM ( )  RATIONAL_B_SPLINE_CURVE ( ( 0.9330127018922194093, 0.9330127018922187432, 1.000000000000000000, 0.8660254037844387076, 1.000000000000000000, 0.8660254037844387076, 1.000000000000000000, 0.9330127018922194093, 0.9330127018922194093 ) ) 
 REPRESENTATION_ITEM ( '' )  );
#144866=CARTESIAN_POINT ( 'NONE',  ( -0.7500000000000006661, 8.958333333333332149, -1.299038105676657340 ) ) ;
#144871=ORIENTED_EDGE ( 'NONE', *, *, #105563, .F. ) ;
#144924=CARTESIAN_POINT ( 'NONE',  ( -0.7500000000000179856, 12.54166666666666607, 1.299038105676658228 ) ) ;
#144929=CARTESIAN_POINT ( 'NONE',  ( -0.6823417656250003738, 9.901041667008065872, 1.181850606188754593 ) ) ;
#144963=CARTESIAN_POINT ( 'NONE',  ( 0.6823417656249969321, 10.83854166700806765, -1.181850606188757036 ) ) ;
#145036=CARTESIAN_POINT ( 'NONE',  ( -1.500000000000015099, 13.76041666734946212, -0.8660254037844309360 ) ) ;
#145038=ORIENTED_EDGE ( 'NONE', *, *, #55232, .T. ) ;
#145073=CARTESIAN_POINT ( 'NONE',  ( -1.364683531250000748, 9.359375000341396245, 0.000000000000000000 ) ) ;
#145236=ORIENTED_EDGE ( 'NONE', *, *, #108943, .T. ) ;
#145253=CARTESIAN_POINT ( 'NONE',  ( 1.500095892183267887, 4.450208832515674118, 0.08036760724049675508 ) ) ;
#145270=ORIENTED_EDGE ( 'NONE', *, *, #154049, .F. ) ;
#145285=ORIENTED_EDGE ( 'NONE', *, *, #58887, .F. ) ;
#145343=CARTESIAN_POINT ( 'NONE',  ( 1.364683531250000303, 13.25520833367472839, -0.7879004041258355073 ) ) ;
#145352=ADVANCED_FACE ( 'NONE', ( #172188 ), #140781, .T. ) ;
#145357=CARTESIAN_POINT ( 'NONE',  ( -1.466385952843404006, 4.235368455307408908, 0.3259651399136407890 ) ) ;
#145438=CARTESIAN_POINT ( 'NONE',  ( -0.7500000000000179856, 12.29166666666666607, 1.299038105676658228 ) ) ;
#145443=ADVANCED_FACE ( 'NONE', ( #21615 ), #204646, .T. ) ;
#145448=( BOUNDED_CURVE ( )  B_SPLINE_CURVE ( 2, ( #40410, #25198, #92381, #120655, #104336, #137909, #158415, #58777, #26262 ),
 .UNSPECIFIED., .F., .T. ) 
 B_SPLINE_CURVE_WITH_KNOTS ( ( 3, 2, 2, 2, 3 ),
 ( 0.5446428571428572063, 0.5476190476190476719, 0.5535714285714286031, 0.5595238095238095344, 0.5625000000000000000 ),
 .UNSPECIFIED. ) 
 CURVE ( )  GEOMETRIC_REPRESENTATION_ITEM ( )  RATIONAL_B_SPLINE_CURVE ( ( 0.9330127018922194093, 0.9330127018922206306, 1.000000000000000000, 0.8660254037844387076, 1.000000000000000000, 0.8660254037844387076, 1.000000000000000000, 0.9330127018922194093, 0.9330127018922194093 ) ) 
 REPRESENTATION_ITEM ( '' )  );
#145470=CARTESIAN_POINT ( 'NONE',  ( 1.466385952843407559, 3.464631544692571286, 0.3259651399136304639 ) ) ;
#145493=CARTESIAN_POINT ( 'NONE',  ( -8.012344526598182026E-15, 13.85937500034139447, -1.575800808251669460 ) ) ;
#145553=CARTESIAN_POINT ( 'NONE',  ( -0.6823417656250003738, 10.96354166700806765, 1.181850606188754593 ) ) ;
#145596=CARTESIAN_POINT ( 'NONE',  ( 1.500000000000001332, 9.906250000682799595, 0.000000000000000000 ) ) ;
#145606=CARTESIAN_POINT ( 'NONE',  ( -1.115562610750309283E-14, 10.09375000068279782, 1.500000000000001554 ) ) ;
#145698=CARTESIAN_POINT ( 'NONE',  ( 1.424678450204434510, 3.957108020605633047, 0.4927150456334776774 ) ) ;
#145718=CARTESIAN_POINT ( 'NONE',  ( -1.422919657202418087, 3.798112692695652104, 0.5004438751493026638 ) ) ;
#145735=CARTESIAN_POINT ( 'NONE',  ( 1.364683531249997417, 9.234375000341396245, 2.602085213965210642E-15 ) ) ;
#145836=CARTESIAN_POINT ( 'NONE',  ( 0.000000000000000000, 13.49999999999999822, 0.000000000000000000 ) ) ;
#145855=ADVANCED_FACE ( 'NONE', ( #9665 ), #173264, .T. ) ;
#145950=EDGE_CURVE ( 'NONE', #128668, #180412, #175390, .T. ) ;
#145981=CARTESIAN_POINT ( 'NONE',  ( 0.7500000000000006661, 10.58333333333333393, 1.299038105676657340 ) ) ;
#145986=CARTESIAN_POINT ( 'NONE',  ( -0.6823417656250039265, 9.567708333674735499, -1.181850606188755259 ) ) ;
#146020=CARTESIAN_POINT ( 'NONE',  ( -1.402160292154681736E-14, 10.73437500034139624, 1.575800808251682339 ) ) ;
#146056=CARTESIAN_POINT ( 'NONE',  ( -1.500000000000001110, 10.02083333333333393, 0.8660254037844418162 ) ) ;
#146061=EDGE_CURVE ( 'NONE', #60352, #94456, #93087, .T. ) ;
#146092=CARTESIAN_POINT ( 'NONE',  ( -1.402160292154681736E-14, 13.84375000068279782, 1.732050807568881190 ) ) ;
#146125=CARTESIAN_POINT ( 'NONE',  ( -8.012344526598182026E-15, 9.546875000341399797, -1.575800808251669460 ) ) ;
#146134=CARTESIAN_POINT ( 'NONE',  ( 1.500000000000001332, 11.15625000068279427, 0.000000000000000000 ) ) ;
#146139=CARTESIAN_POINT ( 'NONE',  ( 0.4019237886466816012, 10.95758545099816317, -1.499999999999998668 ) ) ;
#146146=FACE_OUTER_BOUND ( 'NONE', #158219, .T. ) ;
#146280=CARTESIAN_POINT ( 'NONE',  ( -1.402160292154681736E-14, 8.984375000341396245, 1.575800808251682339 ) ) ;
#146364=ORIENTED_EDGE ( 'NONE', *, *, #93138, .T. ) ;
#146388=CARTESIAN_POINT ( 'NONE',  ( 0.6823417656249969321, 13.52604166700806232, -1.181850606188757036 ) ) ;
#146401=CARTESIAN_POINT ( 'NONE',  ( -1.478151113144027251, 4.278273110089232389, 0.2686735943297190454 ) ) ;
#146436=EDGE_CURVE ( 'NONE', #19108, #211395, #88557, .T. ) ;
#146507=ORIENTED_EDGE ( 'NONE', *, *, #7130, .T. ) ;
#146542=CARTESIAN_POINT ( 'NONE',  ( -0.6823417656250003738, 12.96354166700806942, 1.181850606188754593 ) ) ;
#146587=CARTESIAN_POINT ( 'NONE',  ( 0.000000000000000000, -4.517653975874099892, 0.000000000000000000 ) ) ;
#146601=CARTESIAN_POINT ( 'NONE',  ( -0.6823417656250003738, 10.46354166700806587, 1.181850606188754593 ) ) ;
#146644=CARTESIAN_POINT ( 'NONE',  ( -1.500000000000015099, 9.510416667349463893, -0.8660254037844309360 ) ) ;
#146727=EDGE_CURVE ( 'NONE', #170765, #180412, #57187, .T. ) ;
#146748=CARTESIAN_POINT ( 'NONE',  ( 1.317902950743182089, 4.161287538672367781, -0.3966175983076890010 ) ) ;
#146786=CARTESIAN_POINT ( 'NONE',  ( 0.6823417656249969321, 9.026041667008065872, -1.181850606188757036 ) ) ;
#146802=ORIENTED_EDGE ( 'NONE', *, *, #177186, .T. ) ;
#146855=CARTESIAN_POINT ( 'NONE',  ( -0.6823417656250039265, 14.38020833367473195, -1.181850606188755259 ) ) ;
#146873=( BOUNDED_CURVE ( )  B_SPLINE_CURVE ( 2, ( #197211, #79206, #97613, #194013, #114965, #211324, #163670, #62949, #144265 ),
 .UNSPECIFIED., .F., .T. ) 
 B_SPLINE_CURVE_WITH_KNOTS ( ( 3, 2, 2, 2, 3 ),
 ( 0.6160714285714286031, 0.6190476190476190688, 0.6250000000000000000, 0.6309523809523809312, 0.6339285714285713969 ),
 .UNSPECIFIED. ) 
 CURVE ( )  GEOMETRIC_REPRESENTATION_ITEM ( )  RATIONAL_B_SPLINE_CURVE ( ( 0.9330127018922194093, 0.9330127018922194093, 1.000000000000000000, 0.8660254037844387076, 1.000000000000000000, 0.8660254037844387076, 1.000000000000000000, 0.9330127018922194093, 0.9330127018922194093 ) ) 
 REPRESENTATION_ITEM ( '' )  );
#146874=ORIENTED_EDGE ( 'NONE', *, *, #140470, .F. ) ;
#147037=CARTESIAN_POINT ( 'NONE',  ( -1.500000000000001110, 11.02083333333333393, 0.8660254037844419273 ) ) ;
#147042=CARTESIAN_POINT ( 'NONE',  ( -8.012344526598182026E-15, 9.046875000341405126, -1.575800808251669460 ) ) ;
#147051=CARTESIAN_POINT ( 'NONE',  ( -0.6383513625407253311, 3.364918466673215924, -0.1381026099400331497 ) ) ;
#147061=CARTESIAN_POINT ( 'NONE',  ( -1.266973501737287178, 3.781478720974876140, -0.4964169966120759447 ) ) ;
#147078=CARTESIAN_POINT ( 'NONE',  ( -8.012344526598182026E-15, 10.60937500034139624, -1.575800808251669460 ) ) ;
#147091=DIRECTION ( 'NONE',  ( 1.000000000000000000, 0.000000000000000000, 0.000000000000000000 ) ) ;
#147147=CARTESIAN_POINT ( 'NONE',  ( 0.7500000000000006661, 11.94791666734946389, -1.299038105676657340 ) ) ;
#147181=CARTESIAN_POINT ( 'NONE',  ( -8.012344526598182026E-15, 8.796875000341401574, -1.575800808251669460 ) ) ;
#147326=CARTESIAN_POINT ( 'NONE',  ( -8.012344526598182026E-15, 8.859375000341405126, -1.575800808251669460 ) ) ;
#147344=CARTESIAN_POINT ( 'NONE',  ( 0.4019237886466847653, 9.073664549684629321, 1.499999999999997113 ) ) ;
#147401=CARTESIAN_POINT ( 'NONE',  ( -1.500000000000008216, 8.390625000341399797, 3.469446951953614189E-15 ) ) ;
#147411=VERTEX_POINT ( 'NONE', #115822 ) ;
#147436=CARTESIAN_POINT ( 'NONE',  ( -1.364683531250014514, 13.33854166700806587, -0.7879004041258335089 ) ) ;
#147564=VERTEX_POINT ( 'NONE', #83245 ) ;
#147586=CARTESIAN_POINT ( 'NONE',  ( 1.364683531249996529, 13.02604166700806410, 0.7879004041258405033 ) ) ;
#147651=CARTESIAN_POINT ( 'NONE',  ( -1.402160292154681736E-14, 10.73437500034139802, 1.575800808251682339 ) ) ;
#147692=CARTESIAN_POINT ( 'NONE',  ( -0.7500000000000179856, 10.07291666734946922, 1.299038105676658228 ) ) ;
#147745=CARTESIAN_POINT ( 'NONE',  ( -0.4841233049523207543, 4.104380949686882829, 0.4351758553768784177 ) ) ;
#147833=CARTESIAN_POINT ( 'NONE',  ( 1.364683531249997417, 9.484375000341396245, 2.602085213965210642E-15 ) ) ;
#147834=DIRECTION ( 'NONE',  ( 0.000000000000000000, -1.000000000000000000, 0.000000000000000000 ) ) ;
#147856=ORIENTED_EDGE ( 'NONE', *, *, #114075, .T. ) ;
#147861=DIRECTION ( 'NONE',  ( 0.000000000000000000, -1.000000000000000000, 0.000000000000000000 ) ) ;
#147863=( BOUNDED_CURVE ( )  B_SPLINE_CURVE ( 2, ( #126393, #192352, #176140, #102327, #116508, #3727, #181443, #19997, #119713 ),
 .UNSPECIFIED., .F., .T. ) 
 B_SPLINE_CURVE_WITH_KNOTS ( ( 3, 2, 2, 2, 3 ),
 ( 0.3660714285714286031, 0.3690476190476190688, 0.3750000000000000000, 0.3809523809523809312, 0.3839285714285713969 ),
 .UNSPECIFIED. ) 
 CURVE ( )  GEOMETRIC_REPRESENTATION_ITEM ( )  RATIONAL_B_SPLINE_CURVE ( ( 0.9330127018922194093, 0.9330127018922199644, 1.000000000000000000, 0.8660254037844387076, 1.000000000000000000, 0.8660254037844387076, 1.000000000000000000, 0.9330127018922199644, 0.9330127018922194093 ) ) 
 REPRESENTATION_ITEM ( '' )  );
#147876=ORIENTED_EDGE ( 'NONE', *, *, #47895, .T. ) ;
#147903=CARTESIAN_POINT ( 'NONE',  ( -1.364683531250000748, 14.17187500034140157, 0.000000000000000000 ) ) ;
#147941=( BOUNDED_SURFACE ( )  B_SPLINE_SURFACE ( 1, 2, ( 
 ( #148669, #135623, #53291, #85793, #99916, #151873, #185411, #37029, #103115, #20766, #165977, #86860, #152925, #4503, #120507, #186482, #38115, #140985, #89012, #39179, #22896, #155065, #6653, #87925, #72730, #203781, #205930, #204845, #40251, #190738, #91148, #139899, #90076, #42402, #172386, #138825, #57563, #187549, #107443, #7722, #8800, #154000, #56498, #157203, #170236, #21820, #122656, #188619, #106362, #25047, #5568, #206995, #173468, #189683, #74879, #123720, #23974, #58626, #121578, #124779, #105263, #171304, #156139, #73805, #41335, #71647, #137761, #55425, #152550, #120129, #169862, #69138, #203404, #153627, #200211, #70205, #100598, #102742, #51863, #2000, #121208, #136318, #67000, #183977, #185031, #167736, #150436, #166674, #186105, #117985, #187177, #137388, #21451, #18264, #86485, #170929, #4137, #135261, #38805, #50782, #104887, #199137, #116910, #35588, #202336, #201274, #22526, #53988, #68065, #149354, #37737, #934, #55057, #101667, #133138, #19336, #182910, #134201, #87559, #168797, #119047, #34526, #85415, #151498, #84348, #3068, #52914, #5199, #20404, #36657, #103813, #71274, #101719, #120179, #100650, #35640, #167790, #19385, #84402, #71324, #186155, #169912, #67053, #52962, #70257, #51914, #149407, #68120, #121256, #136371, #2049, #55110, #150490, #135310, #37789, #21501, #202390, #988, #199190, #103863, #50838, #87609, #151550, #134256, #85464, #153679, #3119, #18319, #54042, #69189, #201324, #20452, #83319, #34578, #119100, #5249, #200263, #187228, #118037, #185082, #137439, #203455, #38857, #133190, #116965, #104941, #182963, #170981, #36706, #184024, #102793, #166728, #168849, #86535, #152601, #4187, #74562, #174219, #22580, #188293, #90826, #59370, #58308, #39933, #56175, #25794, #124464, #24723, #190423, #156888, #204525, #122336, #142797, #23657, #42080, #108195, #75627, #92965, #106041, #172064, #73479, #89768, #155814, #140662, #60431, #7398, #206677, #57243, #8476, #91903, #139579, #88686, #6329, #157959, #110327, #76681, #208802, #72402, #9552, #141737, #207744, #125528, #205605, #107119, #154746, #191486, #43155, #123403, #189367, #109267, #41009, #175275, #26861, #173142, #159011, #10605, #126591, #192552, #138502, #44207, #210936, #82007, #144929, #29010, #12732, #62561, #78806, #160073, #128725, #127668, #163278, #112454, #79876, #197885, #180580, #97225, #195773, #49515, #145986, #194697, #14861, #177397, #130839, #113526, #164336, #11675, #46339, #213064, #193630, #178466, #30076, #96167, #95097, #15924, #64694, #48472, #77750, #211998, #80950, #162217, #27939, #161145, #214100, #147042, #63638, #196831, #13804, #94034, #129794, #65729, #114589, #47412, #148097, #179533, #31152, #32201, #98277, #131876, #143871, #209864, #176332, #61502, #45272, #111393, #116701, #54588, #139056, #136917, #50579, #171532, #120735, #170462, #55651, #115634, #66789, #186708, #155293 ),
 ( #16986, #40488, #83066, #723, #100394, #202944, #104413, #70804, #22047, #89242, #121807, #6876, #205083, #38337, #172620, #122893, #169401, #39406, #132928, #71875, #20987, #182701, #90299, #105500, #33259, #153154, #154226, #88158, #34319, #198934, #72954, #87084, #156369, #106592, #56725, #4729, #187774, #140135, #23125, #5798, #7953, #149143, #74045, #165391, #137985, #204002, #188852, #24196, #206161, #181630, #99342, #79374, #94581, #95658, #177952, #108743, #161709, #158496, #13301, #58855, #144423, #11152, #27416, #25280, #42634, #125011, #9036, #141221, #174769, #128222, #77229, #75110, #43697, #160624, #127144, #145493, #10095, #143348, #60991, #209343, #28490, #91382, #193116, #111950, #110873, #207231, #76169, #142274, #208285, #190968, #45829, #12225, #210425, #41563, #93514, #44765, #26344, #123949, #92457, #57789, #176878, #59916, #29566, #126073, #109814, #78298, #62067, #194184, #189918, #173705, #107676, #157442, #192034, #175823, #159556, #147586, #17537, #15417, #146542, #50077, #213604, #49018, #148646, #211488, #162774, #65230, #33812, #32753, #14352, #30641, #212, #98835, #131381, #164885, #197377, #179023, #96725, #117262, #212560, #16479, #82559, #116198, #67347, #80442, #64199, #47973, #130340, #196329, #115137, #34865, #114089, #181132, #31703, #66283, #132430, #180080, #63125, #195265, #198431, #84700, #51139, #183261, #46899, #182185, #99891, #165953, #83626, #97778, #81507, #129289, #149709, #1289, #163838, #133492, #199495, #100939, #167026, #18621, #113014, #102020, #88986, #135597, #103088, #134554, #200557, #185387, #56470, #119398, #3423, #201618, #37006, #53267, #52205, #169145, #168088, #137736, #86834, #54342, #172359, #155039, #71623, #170209, #23948, #120481, #20739, #203755, #151846, #105237, #87902, #138799, #118331, #152898, #187524, #55399, #4477, #2350, #70548, #188594, #121553, #69489, #122632, #136667, #202692, #171278, #22870, #39155, #68426, #184316, #6625, #35940, #72704, #186453, #38090, #104161, #204819, #21793, #85766, #40226, #153975, #5542, #106337, #150787, #19688, #158253, #126887, #125821, #107417, #123697, #93261, #191782, #92203, #43438, #9841, #57539, #189658, #210160, #91121, #109562, #175566, #143096, #160367, #173442, #41309, #140960, #25021, #157180, #208035, #127970, #74858, #59662, #124756, #75917, #27157, #8775, #90053, #73778, #142020, #177692, #144168, #61801, #139874, #159295, #10894, #76969, #209089, #206971, #174512, #156112, #60724, #192845, #58601, #190716, #44504, #42378, #110621, #176621, #108488, #26087, #28233, #94326, #11970, #205905, #78044, #193922, #45568, #111685, #7695, #80174, #63925, #146280, #13029, #196075, #194995, #16212, #179821, #147326, #50876, #33553, #164627, #48757, #116998, #213354, #212292, #82296, #30377, #198174, #180871, #17281, #79106, #47707, #66019, #46629, #113822, #31440, #97519, #96463, #83357 ) ),
 .UNSPECIFIED., .F., .F., .T. ) 
 B_SPLINE_SURFACE_WITH_KNOTS ( ( 2, 2 ),
 ( 3, 2, 2, 2, 2, 2, 2, 2, 2, 2, 2, 2, 2, 2, 2, 2, 2, 2, 2, 2, 2, 2, 2, 2, 2, 2, 2, 2, 2, 2, 2, 2, 2, 2, 2, 2, 2, 2, 2, 2, 2, 2, 2, 2, 2, 2, 2, 2, 2, 2, 2, 2, 2, 2, 2, 2, 2, 2, 2, 2, 2, 2, 2, 2, 2, 2, 2, 2, 2, 2, 2, 2, 2, 2, 2, 2, 2, 2, 2, 2, 2, 2, 2, 2, 2, 2, 2, 2, 2, 2, 2, 2, 2, 2, 2, 2, 2, 2, 2, 2, 2, 2, 2, 2, 2, 2, 2, 2, 2, 2, 2, 2, 2, 2, 2, 2, 2, 2, 2, 2, 2, 2, 2, 2, 2, 2, 2, 2, 2, 2, 2, 2, 2, 2, 2, 2, 2, 2, 2, 2, 2, 2, 2, 2, 2, 2, 2, 2, 2, 2, 2, 2, 2, 2, 2, 2, 2, 2, 2, 2, 2, 2, 2, 2, 2, 2, 2, 2, 3 ),
 ( 0.000000000000000000, 1.000000000000000000 ),
 ( 0.000000000000000000, 0.005952380952380952051, 0.01190476190476190410, 0.01785714285714285615, 0.02380952380952380820, 0.02976190476190476025, 0.03571428571428571230, 0.04166666666666666435, 0.04761904761904761640, 0.05357142857142856845, 0.05952380952380952051, 0.06547619047619047949, 0.07142857142857142461, 0.07738095238095238360, 0.08333333333333332871, 0.08928571428571428770, 0.09523809523809523281, 0.1011904761904761918, 0.1071428571428571369, 0.1130952380952380959, 0.1190476190476190410, 0.1250000000000000000, 0.1309523809523809590, 0.1369047619047619180, 0.1428571428571428492, 0.1488095238095238082, 0.1547619047619047672, 0.1607142857142857262, 0.1666666666666666574, 0.1726190476190476164, 0.1785714285714285754, 0.1845238095238095344, 0.1904761904761904656, 0.1964285714285714246, 0.2023809523809523836, 0.2083333333333333426, 0.2142857142857142738, 0.2202380952380952328, 0.2261904761904761918, 0.2321428571428571508, 0.2380952380952380820, 0.2440476190476190410, 0.2500000000000000000, 0.2559523809523809312, 0.2619047619047619180, 0.2678571428571428492, 0.2738095238095238360, 0.2797619047619047672, 0.2857142857142856984, 0.2916666666666666852, 0.2976190476190476164, 0.3035714285714285476, 0.3095238095238095344, 0.3154761904761904656, 0.3214285714285714524, 0.3273809523809523836, 0.3333333333333333148, 0.3392857142857143016, 0.3452380952380952328, 0.3511904761904761640, 0.3571428571428571508, 0.3630952380952380820, 0.3690476190476190688, 0.3750000000000000000, 0.3809523809523809312, 0.3869047619047619180, 0.3928571428571428492, 0.3988095238095238360, 0.4047619047619047672, 0.4107142857142856984, 0.4166666666666666852, 0.4226190476190476164, 0.4285714285714285476, 0.4345238095238095344, 0.4404761904761904656, 0.4464285714285714524, 0.4523809523809523836, 0.4583333333333333148, 0.4642857142857143016, 0.4702380952380952328, 0.4761904761904761640, 0.4821428571428571508, 0.4880952380952380820, 0.4940476190476190688, 0.5000000000000000000, 0.5059523809523809312, 0.5119047619047618625, 0.5178571428571429047, 0.5238095238095238360, 0.5297619047619047672, 0.5357142857142856984, 0.5416666666666666297, 0.5476190476190476719, 0.5535714285714286031, 0.5595238095238095344, 0.5654761904761904656, 0.5714285714285713969, 0.5773809523809523281, 0.5833333333333333703, 0.5892857142857143016, 0.5952380952380952328, 0.6011904761904761640, 0.6071428571428570953, 0.6130952380952381375, 0.6190476190476190688, 0.6250000000000000000, 0.6309523809523809312, 0.6369047619047618625, 0.6428571428571429047, 0.6488095238095238360, 0.6547619047619047672, 0.6607142857142856984, 0.6666666666666666297, 0.6726190476190476719, 0.6785714285714286031, 0.6845238095238095344, 0.6904761904761904656, 0.6964285714285713969, 0.7023809523809523281, 0.7083333333333333703, 0.7142857142857143016, 0.7202380952380952328, 0.7261904761904761640, 0.7321428571428570953, 0.7380952380952381375, 0.7440476190476190688, 0.7500000000000000000, 0.7559523809523809312, 0.7619047619047618625, 0.7678571428571429047, 0.7738095238095238360, 0.7797619047619047672, 0.7857142857142856984, 0.7916666666666666297, 0.7976190476190476719, 0.8035714285714286031, 0.8095238095238095344, 0.8154761904761904656, 0.8214285714285713969, 0.8273809523809523281, 0.8333333333333333703, 0.8392857142857143016, 0.8452380952380952328, 0.8511904761904761640, 0.8571428571428570953, 0.8630952380952381375, 0.8690476190476190688, 0.8750000000000000000, 0.8809523809523809312, 0.8869047619047618625, 0.8928571428571429047, 0.8988095238095238360, 0.9047619047619047672, 0.9107142857142856984, 0.9166666666666666297, 0.9226190476190476719, 0.9285714285714286031, 0.9345238095238095344, 0.9404761904761904656, 0.9464285714285713969, 0.9523809523809523281, 0.9583333333333333703, 0.9642857142857143016, 0.9702380952380952328, 0.9761904761904761640, 0.9821428571428570953, 0.9880952380952381375, 0.9940476190476190688, 1.000000000000000000 ),
 .UNSPECIFIED. ) 
 GEOMETRIC_REPRESENTATION_ITEM ( )  RATIONAL_B_SPLINE_SURFACE ( (
 ( 1.000000000000000000, 0.8660254037844387076, 1.000000000000000000, 0.8660254037844387076, 1.000000000000000000, 0.8660254037844387076, 1.000000000000000000, 0.8660254037844387076, 1.000000000000000000, 0.8660254037844387076, 1.000000000000000000, 0.8660254037844387076, 1.000000000000000000, 0.8660254037844387076, 1.000000000000000000, 0.8660254037844387076, 1.000000000000000000, 0.8660254037844387076, 1.000000000000000000, 0.8660254037844387076, 1.000000000000000000, 0.8660254037844387076, 1.000000000000000000, 0.8660254037844387076, 1.000000000000000000, 0.8660254037844387076, 1.000000000000000000, 0.8660254037844387076, 1.000000000000000000, 0.8660254037844387076, 1.000000000000000000, 0.8660254037844387076, 1.000000000000000000, 0.8660254037844387076, 1.000000000000000000, 0.8660254037844387076, 1.000000000000000000, 0.8660254037844387076, 1.000000000000000000, 0.8660254037844387076, 1.000000000000000000, 0.8660254037844387076, 1.000000000000000000, 0.8660254037844387076, 1.000000000000000000, 0.8660254037844387076, 1.000000000000000000, 0.8660254037844387076, 1.000000000000000000, 0.8660254037844387076, 1.000000000000000000, 0.8660254037844387076, 1.000000000000000000, 0.8660254037844387076, 1.000000000000000000, 0.8660254037844387076, 1.000000000000000000, 0.8660254037844387076, 1.000000000000000000, 0.8660254037844387076, 1.000000000000000000, 0.8660254037844387076, 1.000000000000000000, 0.8660254037844387076, 1.000000000000000000, 0.8660254037844387076, 1.000000000000000000, 0.8660254037844387076, 1.000000000000000000, 0.8660254037844387076, 1.000000000000000000, 0.8660254037844387076, 1.000000000000000000, 0.8660254037844387076, 1.000000000000000000, 0.8660254037844387076, 1.000000000000000000, 0.8660254037844387076, 1.000000000000000000, 0.8660254037844387076, 1.000000000000000000, 0.8660254037844387076, 1.000000000000000000, 0.8660254037844387076, 1.000000000000000000, 0.8660254037844387076, 1.000000000000000000, 0.8660254037844387076, 1.000000000000000000, 0.8660254037844387076, 1.000000000000000000, 0.8660254037844387076, 1.000000000000000000, 0.8660254037844387076, 1.000000000000000000, 0.8660254037844387076, 1.000000000000000000, 0.8660254037844387076, 1.000000000000000000, 0.8660254037844387076, 1.000000000000000000, 0.8660254037844387076, 1.000000000000000000, 0.8660254037844387076, 1.000000000000000000, 0.8660254037844387076, 1.000000000000000000, 0.8660254037844387076, 1.000000000000000000, 0.8660254037844387076, 1.000000000000000000, 0.8660254037844387076, 1.000000000000000000, 0.8660254037844387076, 1.000000000000000000, 0.8660254037844387076, 1.000000000000000000, 0.8660254037844387076, 1.000000000000000000, 0.8660254037844387076, 1.000000000000000000, 0.8660254037844387076, 1.000000000000000000, 0.8660254037844387076, 1.000000000000000000, 0.8660254037844387076, 1.000000000000000000, 0.8660254037844387076, 1.000000000000000000, 0.8660254037844387076, 1.000000000000000000, 0.8660254037844387076, 1.000000000000000000, 0.8660254037844387076, 1.000000000000000000, 0.8660254037844387076, 1.000000000000000000, 0.8660254037844387076, 1.000000000000000000, 0.8660254037844387076, 1.000000000000000000, 0.8660254037844387076, 1.000000000000000000, 0.8660254037844387076, 1.000000000000000000, 0.8660254037844387076, 1.000000000000000000, 0.8660254037844387076, 1.000000000000000000, 0.8660254037844387076, 1.000000000000000000, 0.8660254037844387076, 1.000000000000000000, 0.8660254037844387076, 1.000000000000000000, 0.8660254037844387076, 1.000000000000000000, 0.8660254037844387076, 1.000000000000000000, 0.8660254037844387076, 1.000000000000000000, 0.8660254037844387076, 1.000000000000000000, 0.8660254037844387076, 1.000000000000000000, 0.8660254037844387076, 1.000000000000000000, 0.8660254037844387076, 1.000000000000000000, 0.8660254037844387076, 1.000000000000000000, 0.8660254037844387076, 1.000000000000000000, 0.8660254037844387076, 1.000000000000000000, 0.8660254037844387076, 1.000000000000000000, 0.8660254037844387076, 1.000000000000000000, 0.8660254037844387076, 1.000000000000000000, 0.8660254037844387076, 1.000000000000000000, 0.8660254037844387076, 1.000000000000000000, 0.8660254037844387076, 1.000000000000000000, 0.8660254037844387076, 1.000000000000000000, 0.8660254037844387076, 1.000000000000000000, 0.8660254037844387076, 1.000000000000000000, 0.8660254037844387076, 1.000000000000000000, 0.8660254037844387076, 1.000000000000000000, 0.8660254037844387076, 1.000000000000000000, 0.8660254037844387076, 1.000000000000000000, 0.8660254037844387076, 1.000000000000000000, 0.8660254037844387076, 1.000000000000000000, 0.8660254037844387076, 1.000000000000000000, 0.8660254037844387076, 1.000000000000000000, 0.8660254037844387076, 1.000000000000000000, 0.8660254037844387076, 1.000000000000000000, 0.8660254037844387076, 1.000000000000000000, 0.8660254037844387076, 1.000000000000000000, 0.8660254037844387076, 1.000000000000000000, 0.8660254037844387076, 1.000000000000000000, 0.8660254037844387076, 1.000000000000000000, 0.8660254037844387076, 1.000000000000000000, 0.8660254037844387076, 1.000000000000000000, 0.8660254037844387076, 1.000000000000000000, 0.8660254037844387076, 1.000000000000000000, 0.8660254037844387076, 1.000000000000000000, 0.8660254037844387076, 1.000000000000000000, 0.8660254037844387076, 1.000000000000000000, 0.8660254037844387076, 1.000000000000000000, 0.8660254037844387076, 1.000000000000000000, 0.8660254037844387076, 1.000000000000000000, 0.8660254037844387076, 1.000000000000000000, 0.8660254037844387076, 1.000000000000000000, 0.8660254037844387076, 1.000000000000000000, 0.8660254037844387076, 1.000000000000000000, 0.8660254037844387076, 1.000000000000000000, 0.8660254037844387076, 1.000000000000000000, 0.8660254037844387076, 1.000000000000000000, 0.8660254037844387076, 1.000000000000000000, 0.8660254037844387076, 1.000000000000000000, 0.8660254037844387076, 1.000000000000000000, 0.8660254037844387076, 1.000000000000000000, 0.8660254037844387076, 1.000000000000000000, 0.8660254037844387076, 1.000000000000000000, 0.8660254037844387076, 1.000000000000000000, 0.8660254037844387076, 1.000000000000000000, 0.8660254037844387076, 1.000000000000000000, 0.8660254037844387076, 1.000000000000000000, 0.8660254037844387076, 1.000000000000000000, 0.8660254037844387076, 1.000000000000000000, 0.8660254037844387076, 1.000000000000000000, 0.8660254037844387076, 1.000000000000000000, 0.8660254037844387076, 1.000000000000000000, 0.8660254037844387076, 1.000000000000000000, 0.8660254037844387076, 1.000000000000000000, 0.8660254037844387076, 1.000000000000000000, 0.8660254037844387076, 1.000000000000000000, 0.8660254037844387076, 1.000000000000000000, 0.8660254037844387076, 1.000000000000000000, 0.8660254037844387076, 1.000000000000000000, 0.8660254037844387076, 1.000000000000000000, 0.8660254037844387076, 1.000000000000000000, 0.8660254037844387076, 1.000000000000000000, 0.8660254037844387076, 1.000000000000000000, 0.8660254037844387076, 1.000000000000000000, 0.8660254037844387076, 1.000000000000000000, 0.8660254037844387076, 1.000000000000000000, 0.8660254037844387076, 1.000000000000000000, 0.8660254037844387076, 1.000000000000000000, 0.8660254037844387076, 1.000000000000000000, 0.8660254037844387076, 1.000000000000000000, 0.8660254037844387076, 1.000000000000000000, 0.8660254037844387076, 1.000000000000000000, 0.8660254037844387076, 1.000000000000000000, 0.8660254037844387076, 1.000000000000000000, 0.8660254037844387076, 1.000000000000000000, 0.8660254037844387076, 1.000000000000000000, 0.8660254037844387076, 1.000000000000000000),
 ( 1.000000000000000000, 0.8660254037844387076, 1.000000000000000000, 0.8660254037844387076, 1.000000000000000000, 0.8660254037844387076, 1.000000000000000000, 0.8660254037844387076, 1.000000000000000000, 0.8660254037844387076, 1.000000000000000000, 0.8660254037844387076, 1.000000000000000000, 0.8660254037844387076, 1.000000000000000000, 0.8660254037844387076, 1.000000000000000000, 0.8660254037844387076, 1.000000000000000000, 0.8660254037844387076, 1.000000000000000000, 0.8660254037844387076, 1.000000000000000000, 0.8660254037844387076, 1.000000000000000000, 0.8660254037844387076, 1.000000000000000000, 0.8660254037844387076, 1.000000000000000000, 0.8660254037844387076, 1.000000000000000000, 0.8660254037844387076, 1.000000000000000000, 0.8660254037844387076, 1.000000000000000000, 0.8660254037844387076, 1.000000000000000000, 0.8660254037844387076, 1.000000000000000000, 0.8660254037844387076, 1.000000000000000000, 0.8660254037844387076, 1.000000000000000000, 0.8660254037844387076, 1.000000000000000000, 0.8660254037844387076, 1.000000000000000000, 0.8660254037844387076, 1.000000000000000000, 0.8660254037844387076, 1.000000000000000000, 0.8660254037844387076, 1.000000000000000000, 0.8660254037844387076, 1.000000000000000000, 0.8660254037844387076, 1.000000000000000000, 0.8660254037844387076, 1.000000000000000000, 0.8660254037844387076, 1.000000000000000000, 0.8660254037844387076, 1.000000000000000000, 0.8660254037844387076, 1.000000000000000000, 0.8660254037844387076, 1.000000000000000000, 0.8660254037844387076, 1.000000000000000000, 0.8660254037844387076, 1.000000000000000000, 0.8660254037844387076, 1.000000000000000000, 0.8660254037844387076, 1.000000000000000000, 0.8660254037844387076, 1.000000000000000000, 0.8660254037844387076, 1.000000000000000000, 0.8660254037844387076, 1.000000000000000000, 0.8660254037844387076, 1.000000000000000000, 0.8660254037844387076, 1.000000000000000000, 0.8660254037844387076, 1.000000000000000000, 0.8660254037844387076, 1.000000000000000000, 0.8660254037844387076, 1.000000000000000000, 0.8660254037844387076, 1.000000000000000000, 0.8660254037844387076, 1.000000000000000000, 0.8660254037844387076, 1.000000000000000000, 0.8660254037844387076, 1.000000000000000000, 0.8660254037844387076, 1.000000000000000000, 0.8660254037844387076, 1.000000000000000000, 0.8660254037844387076, 1.000000000000000000, 0.8660254037844387076, 1.000000000000000000, 0.8660254037844387076, 1.000000000000000000, 0.8660254037844387076, 1.000000000000000000, 0.8660254037844387076, 1.000000000000000000, 0.8660254037844387076, 1.000000000000000000, 0.8660254037844387076, 1.000000000000000000, 0.8660254037844387076, 1.000000000000000000, 0.8660254037844387076, 1.000000000000000000, 0.8660254037844387076, 1.000000000000000000, 0.8660254037844387076, 1.000000000000000000, 0.8660254037844387076, 1.000000000000000000, 0.8660254037844387076, 1.000000000000000000, 0.8660254037844387076, 1.000000000000000000, 0.8660254037844387076, 1.000000000000000000, 0.8660254037844387076, 1.000000000000000000, 0.8660254037844387076, 1.000000000000000000, 0.8660254037844387076, 1.000000000000000000, 0.8660254037844387076, 1.000000000000000000, 0.8660254037844387076, 1.000000000000000000, 0.8660254037844387076, 1.000000000000000000, 0.8660254037844387076, 1.000000000000000000, 0.8660254037844387076, 1.000000000000000000, 0.8660254037844387076, 1.000000000000000000, 0.8660254037844387076, 1.000000000000000000, 0.8660254037844387076, 1.000000000000000000, 0.8660254037844387076, 1.000000000000000000, 0.8660254037844387076, 1.000000000000000000, 0.8660254037844387076, 1.000000000000000000, 0.8660254037844387076, 1.000000000000000000, 0.8660254037844387076, 1.000000000000000000, 0.8660254037844387076, 1.000000000000000000, 0.8660254037844387076, 1.000000000000000000, 0.8660254037844387076, 1.000000000000000000, 0.8660254037844387076, 1.000000000000000000, 0.8660254037844387076, 1.000000000000000000, 0.8660254037844387076, 1.000000000000000000, 0.8660254037844387076, 1.000000000000000000, 0.8660254037844387076, 1.000000000000000000, 0.8660254037844387076, 1.000000000000000000, 0.8660254037844387076, 1.000000000000000000, 0.8660254037844387076, 1.000000000000000000, 0.8660254037844387076, 1.000000000000000000, 0.8660254037844387076, 1.000000000000000000, 0.8660254037844387076, 1.000000000000000000, 0.8660254037844387076, 1.000000000000000000, 0.8660254037844387076, 1.000000000000000000, 0.8660254037844387076, 1.000000000000000000, 0.8660254037844387076, 1.000000000000000000, 0.8660254037844387076, 1.000000000000000000, 0.8660254037844387076, 1.000000000000000000, 0.8660254037844387076, 1.000000000000000000, 0.8660254037844387076, 1.000000000000000000, 0.8660254037844387076, 1.000000000000000000, 0.8660254037844387076, 1.000000000000000000, 0.8660254037844387076, 1.000000000000000000, 0.8660254037844387076, 1.000000000000000000, 0.8660254037844387076, 1.000000000000000000, 0.8660254037844387076, 1.000000000000000000, 0.8660254037844387076, 1.000000000000000000, 0.8660254037844387076, 1.000000000000000000, 0.8660254037844387076, 1.000000000000000000, 0.8660254037844387076, 1.000000000000000000, 0.8660254037844387076, 1.000000000000000000, 0.8660254037844387076, 1.000000000000000000, 0.8660254037844387076, 1.000000000000000000, 0.8660254037844387076, 1.000000000000000000, 0.8660254037844387076, 1.000000000000000000, 0.8660254037844387076, 1.000000000000000000, 0.8660254037844387076, 1.000000000000000000, 0.8660254037844387076, 1.000000000000000000, 0.8660254037844387076, 1.000000000000000000, 0.8660254037844387076, 1.000000000000000000, 0.8660254037844387076, 1.000000000000000000, 0.8660254037844387076, 1.000000000000000000, 0.8660254037844387076, 1.000000000000000000, 0.8660254037844387076, 1.000000000000000000, 0.8660254037844387076, 1.000000000000000000, 0.8660254037844387076, 1.000000000000000000, 0.8660254037844387076, 1.000000000000000000, 0.8660254037844387076, 1.000000000000000000, 0.8660254037844387076, 1.000000000000000000, 0.8660254037844387076, 1.000000000000000000, 0.8660254037844387076, 1.000000000000000000, 0.8660254037844387076, 1.000000000000000000, 0.8660254037844387076, 1.000000000000000000, 0.8660254037844387076, 1.000000000000000000, 0.8660254037844387076, 1.000000000000000000, 0.8660254037844387076, 1.000000000000000000, 0.8660254037844387076, 1.000000000000000000, 0.8660254037844387076, 1.000000000000000000, 0.8660254037844387076, 1.000000000000000000, 0.8660254037844387076, 1.000000000000000000, 0.8660254037844387076, 1.000000000000000000, 0.8660254037844387076, 1.000000000000000000, 0.8660254037844387076, 1.000000000000000000, 0.8660254037844387076, 1.000000000000000000, 0.8660254037844387076, 1.000000000000000000, 0.8660254037844387076, 1.000000000000000000, 0.8660254037844387076, 1.000000000000000000, 0.8660254037844387076, 1.000000000000000000, 0.8660254037844387076, 1.000000000000000000, 0.8660254037844387076, 1.000000000000000000, 0.8660254037844387076, 1.000000000000000000, 0.8660254037844387076, 1.000000000000000000, 0.8660254037844387076, 1.000000000000000000, 0.8660254037844387076, 1.000000000000000000, 0.8660254037844387076, 1.000000000000000000, 0.8660254037844387076, 1.000000000000000000, 0.8660254037844387076, 1.000000000000000000, 0.8660254037844387076, 1.000000000000000000, 0.8660254037844387076, 1.000000000000000000, 0.8660254037844387076, 1.000000000000000000, 0.8660254037844387076, 1.000000000000000000, 0.8660254037844387076, 1.000000000000000000, 0.8660254037844387076, 1.000000000000000000, 0.8660254037844387076, 1.000000000000000000) ) ) 
 REPRESENTATION_ITEM ( '' )  SURFACE ( )  );
#148068=CARTESIAN_POINT ( 'NONE',  ( 1.499999999999996891, 11.92708333401613174, -0.8660254037844378194 ) ) ;
#148091=CARTESIAN_POINT ( 'NONE',  ( -0.7500000000000006661, 11.20833333333333393, -1.299038105676657340 ) ) ;
#148097=CARTESIAN_POINT ( 'NONE',  ( -1.364683531250000748, 8.859375000341396245, 0.000000000000000000 ) ) ;
#148103=ADVANCED_FACE ( 'NONE', ( #209793 ), #42009, .T. ) ;
#148108=CARTESIAN_POINT ( 'NONE',  ( -0.5727794709109862437, 3.454100923638389720, 0.3117576387476111432 ) ) ;
#148137=CARTESIAN_POINT ( 'NONE',  ( -0.6823417656250003738, 10.71354166700806765, 1.181850606188754593 ) ) ;
#148209=CARTESIAN_POINT ( 'NONE',  ( 1.500000000000001332, 11.90625000068279427, 0.000000000000000000 ) ) ;
#148288=CARTESIAN_POINT ( 'NONE',  ( -2.788906526875773208E-15, 8.968750000682797818, -1.499999999999998446 ) ) ;
#148352=B_SPLINE_CURVE_WITH_KNOTS ( 'NONE', 3,
 ( #127678, #129802, #161153, #163286, #195782, #179540, #80958, #147051, #193638, #32212, #15934, #82017, #148108, #214111, #65738, #143881, #181640, #49523 ),
 .UNSPECIFIED., .F., .F.,
 ( 4, 2, 2, 2, 2, 2, 2, 2, 4 ),
 ( 2.649649035303588278E-18, 0.0002050783776814521433, 0.0004101567553629016302, 0.0006152351330443510359, 0.0008203135107258005499, 0.001025391888407249956, 0.001230470266088699470, 0.001435548643770148984, 0.001640627021451598498 ),
 .UNSPECIFIED. ) ;
#148389=CARTESIAN_POINT ( 'NONE',  ( -1.242799958986342546, 13.28403883893647119, -0.7783234177255069497 ) ) ;
#148461=VECTOR ( 'NONE', #167275, 1000.000000000000000 ) ;
#148498=CARTESIAN_POINT ( 'NONE',  ( 0.6823417656249934904, 11.44270833367473728, 1.181850606188764807 ) ) ;
#148528=CARTESIAN_POINT ( 'NONE',  ( 1.233697830709073795, 13.31203353598178829, 0.7436150061141216794 ) ) ;
#148552=ORIENTED_EDGE ( 'NONE', *, *, #170324, .T. ) ;
#148562=CARTESIAN_POINT ( 'NONE',  ( -0.6224592253956000576, -4.250299932362466393, -0.9218689959748761487 ) ) ;
#148646=CARTESIAN_POINT ( 'NONE',  ( -0.6823417656250039265, 12.88020833367473017, -1.181850606188755259 ) ) ;
#148669=CARTESIAN_POINT ( 'NONE',  ( -1.364683531250000748, 15.35937500034140157, 0.000000000000000000 ) ) ;
#148672=ADVANCED_FACE ( 'NONE', ( #7355 ), #1221, .T. ) ;
#148673=CARTESIAN_POINT ( 'NONE',  ( -1.500000000000008216, 11.99999999999999645, 3.469446951953614189E-15 ) ) ;
#148708=CARTESIAN_POINT ( 'NONE',  ( 1.364683531249997417, 10.54687500034139802, 2.602085213965210642E-15 ) ) ;
#148750=CARTESIAN_POINT ( 'NONE',  ( -1.500000000000015099, 9.760416667349467446, -0.8660254037844309360 ) ) ;
#148812=CARTESIAN_POINT ( 'NONE',  ( 0.000000000000000000, 13.49999999999999822, 0.000000000000000000 ) ) ;
#148886=CARTESIAN_POINT ( 'NONE',  ( 1.836970198721030181E-16, 13.49999999999999822, 1.500000000000000222 ) ) ;
#148955=CARTESIAN_POINT ( 'NONE',  ( 1.364683531249997417, 14.04687500034140157, 2.602085213965210642E-15 ) ) ;
#149137=CARTESIAN_POINT ( 'NONE',  ( -6.009258394948636914E-15, 11.43749999999999822, -1.732050807568875195 ) ) ;
#149143=CARTESIAN_POINT ( 'NONE',  ( 1.364683531250000303, 14.56770833367473372, -0.7879004041258355073 ) ) ;
#149177=ORIENTED_EDGE ( 'NONE', *, *, #56964, .T. ) ;
#149187=CARTESIAN_POINT ( 'NONE',  ( -0.6823417656250039265, 10.38020833367472839, -1.181850606188755259 ) ) ;
#149261=CARTESIAN_POINT ( 'NONE',  ( -0.7500000000000006661, 12.73958333401613352, -1.299038105676657340 ) ) ;
#149354=CARTESIAN_POINT ( 'NONE',  ( -1.364683531250014514, 13.08854166700806410, -0.7879004041258335089 ) ) ;
#149407=CARTESIAN_POINT ( 'NONE',  ( -0.6823417656250039265, 12.31770833367473017, -1.181850606188755259 ) ) ;
#149442=CARTESIAN_POINT ( 'NONE',  ( -1.416502993825243362, 13.32998166073656066, -0.1108442676237804125 ) ) ;
#149462=CARTESIAN_POINT ( 'NONE',  ( 1.499999999999993117, 9.104166666666666075, 0.8660254037844408170 ) ) ;
#149555=CARTESIAN_POINT ( 'NONE',  ( 1.364683531250000303, 12.00520833367473195, -0.7879004041258355073 ) ) ;
#149575=ORIENTED_EDGE ( 'NONE', *, *, #179256, .F. ) ;
#149605=EDGE_LOOP ( 'NONE', ( #193715, #7601, #138857, #70561 ) ) ;
#149661=AXIS2_PLACEMENT_3D ( 'NONE', #44816, #43747, #127199 ) ;
#149709=CARTESIAN_POINT ( 'NONE',  ( -0.6823417656250039265, 11.88020833367473017, -1.181850606188755259 ) ) ;
#149777=CARTESIAN_POINT ( 'NONE',  ( -1.364683531250014514, 9.901041667008064096, -0.7879004041258335089 ) ) ;
#149808=CARTESIAN_POINT ( 'NONE',  ( 1.500000000000001332, 12.12499999999999645, 0.000000000000000000 ) ) ;
#149824=CARTESIAN_POINT ( 'NONE',  ( 1.499999999999993117, 8.385416667349465669, 0.8660254037844409281 ) ) ;
#150018=LINE ( 'NONE', #1588, #66189 ) ;
#150030=CARTESIAN_POINT ( 'NONE',  ( -8.012344526598182026E-15, 14.85937500034139980, -1.575800808251669460 ) ) ;
#150219=CARTESIAN_POINT ( 'NONE',  ( -1.364683531250014514, 12.33854166700805877, -0.7879004041258335089 ) ) ;
#150226=CARTESIAN_POINT ( 'NONE',  ( 0.7500000000000006661, 10.91666666666666430, -1.299038105676657340 ) ) ;
#150240=CARTESIAN_POINT ( 'NONE',  ( 1.500000000000001332, 9.625000000000001776, 0.000000000000000000 ) ) ;
#150273=CARTESIAN_POINT ( 'NONE',  ( -1.364683531250000748, 8.921875000341403350, 0.000000000000000000 ) ) ;
#150343=DIRECTION ( 'NONE',  ( 0.000000000000000000, 0.000000000000000000, -1.000000000000000000 ) ) ;
#150344=CARTESIAN_POINT ( 'NONE',  ( -1.500000000000008216, 12.53125000068279427, 3.469446951953614189E-15 ) ) ;
#150354=CARTESIAN_POINT ( 'NONE',  ( -0.4019237886466871523, 12.69866454968462754, -1.499999999999998668 ) ) ;
#150422=CARTESIAN_POINT ( 'NONE',  ( -1.432341765625004593, 8.460937500170699010, 8.673617379884035472E-16 ) ) ;
#150436=CARTESIAN_POINT ( 'NONE',  ( -0.6823417656250039265, 13.56770833367473195, -1.181850606188755259 ) ) ;
#150490=CARTESIAN_POINT ( 'NONE',  ( 0.6823417656249934904, 12.19270833367473017, 1.181850606188764807 ) ) ;
#150535=CARTESIAN_POINT ( 'NONE',  ( -1.500000000000015099, 9.479166666666669627, -0.8660254037844309360 ) ) ;
#150542=CARTESIAN_POINT ( 'NONE',  ( 3.834746474454188013E-15, 9.062500000000001776, 1.500000000000001554 ) ) ;
#150636=CARTESIAN_POINT ( 'NONE',  ( -8.012344526598182026E-15, 12.04687500034140335, -1.575800808251669460 ) ) ;
#150692=ORIENTED_EDGE ( 'NONE', *, *, #125292, .F. ) ;
#150787=CARTESIAN_POINT ( 'NONE',  ( -1.364683531250014514, 10.40104166700806765, -0.7879004041258335089 ) ) ;
#150838=CARTESIAN_POINT ( 'NONE',  ( -1.402160292154681736E-14, 12.92187500034139980, 1.575800808251682339 ) ) ;
#150852=CARTESIAN_POINT ( 'NONE',  ( 0.6823417656249969321, 9.338541667008065872, -1.181850606188757036 ) ) ;
#150895=CARTESIAN_POINT ( 'NONE',  ( -8.012344526598182026E-15, 15.04687500034140157, -1.575800808251669460 ) ) ;
#150996=CARTESIAN_POINT ( 'NONE',  ( 1.220146605508150803E-14, 9.468750000682799595, -1.499999999999998446 ) ) ;
#151085=VERTEX_POINT ( 'NONE', #18806 ) ;
#151103=CARTESIAN_POINT ( 'NONE',  ( 1.364683531249997417, 13.79687500034139980, 2.602085213965210642E-15 ) ) ;
#151273=CARTESIAN_POINT ( 'NONE',  ( -2.788906526875773208E-15, 13.21875000068279427, -1.499999999999998446 ) ) ;
#151274=CARTESIAN_POINT ( 'NONE',  ( -0.5773502691896261751, -2.500000000000002220, -0.9999999999999991118 ) ) ;
#151283=CARTESIAN_POINT ( 'NONE',  ( -1.364683531250010740, 11.63020833367472839, 0.7879004041258445001 ) ) ;
#151288=CARTESIAN_POINT ( 'NONE',  ( -0.7500000000000179856, 9.541666666666671404, 1.299038105676658228 ) ) ;
#151327=VERTEX_POINT ( 'NONE', #59864 ) ;
#151337=CARTESIAN_POINT ( 'NONE',  ( -1.364683531250014514, 8.901041667008069425, -0.7879004041258335089 ) ) ;
#151343=CARTESIAN_POINT ( 'NONE',  ( 3.834746474454188013E-15, 10.34375000068279782, 1.500000000000001554 ) ) ;
#151389=CARTESIAN_POINT ( 'NONE',  ( -0.4019237886466802689, 11.47991455036742714, -1.500000000000002887 ) ) ;
#151409=CARTESIAN_POINT ( 'NONE',  ( -0.7500000000000179856, 12.07291666734946389, 1.299038105676658228 ) ) ;
#151458=CARTESIAN_POINT ( 'NONE',  ( -1.500000000000008216, 11.28125000068279427, 3.469446951953614189E-15 ) ) ;
#151484=CARTESIAN_POINT ( 'NONE',  ( 1.355131232792150309, 3.931394762486951411, -0.6431325189496895911 ) ) ;
#151485=CARTESIAN_POINT ( 'NONE',  ( -0.2024025116386971856, -4.140708350189164832, 1.000000000000004441 ) ) ;
#151486=CARTESIAN_POINT ( 'NONE',  ( 0.000000000000000000, 13.49999999999999822, 0.000000000000000000 ) ) ;
#151498=CARTESIAN_POINT ( 'NONE',  ( -8.012344526598182026E-15, 12.79687500034139802, -1.575800808251669460 ) ) ;
#151521=CARTESIAN_POINT ( 'NONE',  ( 1.346800533732417149, 3.461515298693836229, 0.3345042947240741693 ) ) ;
#151544=CARTESIAN_POINT ( 'NONE',  ( 1.499999999999993117, 13.60416666666666607, 0.8660254037844409281 ) ) ;
#151550=CARTESIAN_POINT ( 'NONE',  ( 1.364683531249997417, 11.98437500034139980, 2.602085213965210642E-15 ) ) ;
#151598=CARTESIAN_POINT ( 'NONE',  ( -0.6823417656250003738, 12.96354166700806942, 1.181850606188754593 ) ) ;
#151657=LINE ( 'NONE', #28040, #206615 ) ;
#151675=DIRECTION ( 'NONE',  ( 0.000000000000000000, 0.000000000000000000, -1.000000000000000000 ) ) ;
#151689=CARTESIAN_POINT ( 'NONE',  ( 0.6386677588215936563, 4.335493988512285846, 0.1366812159789597692 ) ) ;
#151700=CARTESIAN_POINT ( 'NONE',  ( 0.6823417656249934904, 11.69270833367473017, 1.181850606188764807 ) ) ;
#151749=ORIENTED_EDGE ( 'NONE', *, *, #3077, .T. ) ;
#151846=CARTESIAN_POINT ( 'NONE',  ( -0.6823417656250039265, 11.13020833367473017, -1.181850606188755259 ) ) ;
#151847=AXIS2_PLACEMENT_3D ( 'NONE', #211414, #46821, #45752 ) ;
#151873=CARTESIAN_POINT ( 'NONE',  ( 1.364683531250000303, 15.25520833367473017, -0.7879004041258355073 ) ) ;
#151912=CARTESIAN_POINT ( 'NONE',  ( -0.6823417656250039265, 9.380208333674728394, -1.181850606188755259 ) ) ;
#151954=CARTESIAN_POINT ( 'NONE',  ( -1.500000000000015099, 8.760416667349462116, -0.8660254037844309360 ) ) ;
#152089=CARTESIAN_POINT ( 'NONE',  ( 1.364683531249997417, 8.484375000341396245, 2.602085213965210642E-15 ) ) ;
#152144=CARTESIAN_POINT ( 'NONE',  ( 0.000000000000000000, -4.500000000000003553, 2.000000000000000000 ) ) ;
#152158=CARTESIAN_POINT ( 'NONE',  ( -8.012344526598182026E-15, 13.35937500034140157, -1.575800808251669460 ) ) ;
#152322=FACE_BOUND ( 'NONE', #20709, .T. ) ;
#152327=ORIENTED_EDGE ( 'NONE', *, *, #175342, .F. ) ;
#152340=CARTESIAN_POINT ( 'NONE',  ( 1.364683531249996529, 11.46354166700806410, 0.7879004041258403923 ) ) ;
#152345=CARTESIAN_POINT ( 'NONE',  ( 0.7500000000000006661, 10.33333333333333393, 1.299038105676657340 ) ) ;
#152395=CARTESIAN_POINT ( 'NONE',  ( -1.402160292154681736E-14, 8.984375000341396245, 1.575800808251682339 ) ) ;
#152401=CARTESIAN_POINT ( 'NONE',  ( -1.500000000000015099, 10.26041666734946034, -0.8660254037844309360 ) ) ;
#152446=CARTESIAN_POINT ( 'NONE',  ( -0.7500000000000006661, 11.48958333401613174, -1.299038105676657340 ) ) ;
#152454=CARTESIAN_POINT ( 'NONE',  ( 0.4019237886466816012, 12.42633545031537068, -1.499999999999998668 ) ) ;
#152467=CARTESIAN_POINT ( 'NONE',  ( -0.7500000000000179856, 10.82291666734946212, 1.299038105676658228 ) ) ;
#152550=CARTESIAN_POINT ( 'NONE',  ( 0.6823417656249934904, 13.94270833367473195, 1.181850606188764807 ) ) ;
#152594=CARTESIAN_POINT ( 'NONE',  ( 1.500000000000001332, 13.37499999999999822, 0.000000000000000000 ) ) ;
#152601=CARTESIAN_POINT ( 'NONE',  ( -0.6823417656250039265, 11.31770833367473728, -1.181850606188755259 ) ) ;
#152648=CARTESIAN_POINT ( 'NONE',  ( -8.012344526598182026E-15, 12.85937500034139802, -1.575800808251669460 ) ) ;
#152671=CARTESIAN_POINT ( 'NONE',  ( -1.500000000000015099, 10.22916666666667318, -0.8660254037844309360 ) ) ;
#152695=ORIENTED_EDGE ( 'NONE', *, *, #208007, .F. ) ;
#152714=DIRECTION ( 'NONE',  ( 0.000000000000000000, 0.000000000000000000, -1.000000000000000000 ) ) ;
#152748=CARTESIAN_POINT ( 'NONE',  ( -1.364683531250014514, 12.08854166700806765, -0.7879004041258335089 ) ) ;
#152772=ORIENTED_EDGE ( 'NONE', *, *, #109845, .T. ) ;
#152866=CARTESIAN_POINT ( 'NONE',  ( -1.500000000000008216, 10.99999999999999645, 3.469446951953614189E-15 ) ) ;
#152898=CARTESIAN_POINT ( 'NONE',  ( 1.364683531249996529, 11.02604166700807120, 0.7879004041258405033 ) ) ;
#152917=VERTEX_POINT ( 'NONE', #160380 ) ;
#152925=CARTESIAN_POINT ( 'NONE',  ( -1.364683531250000748, 15.10937500034140157, 0.000000000000000000 ) ) ;
#152970=CARTESIAN_POINT ( 'NONE',  ( -1.364683531250010295, 9.692708333674737275, 0.7879004041258445001 ) ) ;
#152977=CARTESIAN_POINT ( 'NONE',  ( -1.364067407192364412, 3.688075514171739400, -0.6250643920678800036 ) ) ;
#153012=CARTESIAN_POINT ( 'NONE',  ( -1.500000000000008216, 8.781250000682797818, 3.469446951953614189E-15 ) ) ;
#153040=EDGE_CURVE ( 'NONE', #191004, #213528, #79764, .T. ) ;
#153050=ORIENTED_EDGE ( 'NONE', *, *, #160143, .F. ) ;
#153154=CARTESIAN_POINT ( 'NONE',  ( -1.364683531250014514, 14.90104166700806410, -0.7879004041258335089 ) ) ;
#153174=CIRCLE ( 'NONE', #163550, 1.249999999999999778 ) ;
#153176=CARTESIAN_POINT ( 'NONE',  ( 1.154700538379228147, -4.295408888568413630, -1.734723475976807094E-15 ) ) ;
#153206=CARTESIAN_POINT ( 'NONE',  ( -0.4019237886466871523, 8.698664549684629321, -1.499999999999998668 ) ) ;
#153214=CARTESIAN_POINT ( 'NONE',  ( -1.154700538379266339, -4.295408888568413630, 2.602085213965210642E-15 ) ) ;
#153217=CARTESIAN_POINT ( 'NONE',  ( -1.364683531250010295, 12.69270833367473550, 0.7879004041258445001 ) ) ;
#153335=EDGE_CURVE ( 'NONE', #70036, #137942, #210719, .T. ) ;
#153386=DIRECTION ( 'NONE',  ( 0.000000000000000000, 0.000000000000000000, -1.000000000000000000 ) ) ;
#153390=CARTESIAN_POINT ( 'NONE',  ( 7.960204194457795477E-17, -2.500000000000002220, 0.6500000000000000222 ) ) ;
#153409=CARTESIAN_POINT ( 'NONE',  ( -0.6823417656250003738, 12.40104166700806232, 1.181850606188754593 ) ) ;
#153414=CARTESIAN_POINT ( 'NONE',  ( 0.7500000000000006661, 9.583333333333332149, 1.299038105676657340 ) ) ;
#153435=CARTESIAN_POINT ( 'NONE',  ( 0.7500000000000006661, 9.666666666666671404, -1.299038105676657340 ) ) ;
#153465=CARTESIAN_POINT ( 'NONE',  ( 1.364683531249997417, 8.796875000341403350, 2.602085213965210642E-15 ) ) ;
#153524=CARTESIAN_POINT ( 'NONE',  ( -2.788906526875773208E-15, 8.687500000000000000, -1.499999999999998446 ) ) ;
#153588=CARTESIAN_POINT ( 'NONE',  ( 1.266901613973835827, 3.782120141946687664, 0.4965463943947275305 ) ) ;
#153627=CARTESIAN_POINT ( 'NONE',  ( -1.364683531250014514, 13.83854166700806765, -0.7879004041258335089 ) ) ;
#153629=( BOUNDED_CURVE ( )  B_SPLINE_CURVE ( 2, ( #198852, #2779, #82985, #137090, #38514, #50500, #202034, #101373, #118753 ),
 .UNSPECIFIED., .F., .T. ) 
 B_SPLINE_CURVE_WITH_KNOTS ( ( 3, 2, 2, 2, 3 ),
 ( 0.3303571428571428492, 0.3333333333333333148, 0.3392857142857143016, 0.3452380952380952328, 0.3482142857142856429 ),
 .UNSPECIFIED. ) 
 CURVE ( )  GEOMETRIC_REPRESENTATION_ITEM ( )  RATIONAL_B_SPLINE_CURVE ( ( 0.9330127018922194093, 0.9330127018922194093, 1.000000000000000000, 0.8660254037844387076, 1.000000000000000000, 0.8660254037844387076, 1.000000000000000000, 0.9330127018922206306, 0.9330127018922194093 ) ) 
 REPRESENTATION_ITEM ( '' )  );
#153672=CARTESIAN_POINT ( 'NONE',  ( -5.000000000000009770, 3.850000000000006306, 0.5000000000000064393 ) ) ;
#153674=CARTESIAN_POINT ( 'NONE',  ( 1.499999999999993117, 14.35416666666666785, 0.8660254037844409281 ) ) ;
#153679=CARTESIAN_POINT ( 'NONE',  ( -1.402160292154681736E-14, 11.92187500034140157, 1.575800808251682339 ) ) ;
#153724=CARTESIAN_POINT ( 'NONE',  ( -0.6823417656250003738, 13.21354166700806942, 1.181850606188754593 ) ) ;
#153729=FACE_OUTER_BOUND ( 'NONE', #1396, .T. ) ;
#153788=CARTESIAN_POINT ( 'NONE',  ( 1.500000000000001332, 14.65625000068279604, 0.000000000000000000 ) ) ;
#153798=FACE_OUTER_BOUND ( 'NONE', #11421, .T. ) ;
#153824=CARTESIAN_POINT ( 'NONE',  ( 1.364683531249996529, 10.46354166700806765, 0.7879004041258405033 ) ) ;
#153975=CARTESIAN_POINT ( 'NONE',  ( -0.6823417656250003738, 10.46354166700806587, 1.181850606188754593 ) ) ;
#154000=CARTESIAN_POINT ( 'NONE',  ( 1.364683531250000303, 14.50520833367473372, -0.7879004041258355073 ) ) ;
#154033=CYLINDRICAL_SURFACE ( 'NONE', #94076, 1.500000000000000222 ) ;
#154036=CARTESIAN_POINT ( 'NONE',  ( 2.449293598294706414E-16, -4.500000000000003553, -2.000000000000000000 ) ) ;
#154042=CARTESIAN_POINT ( 'NONE',  ( -0.6823417656250003738, 8.713541667008065872, 1.181850606188754593 ) ) ;
#154049=EDGE_CURVE ( 'NONE', #99270, #195556, #62679, .T. ) ;
#154085=CARTESIAN_POINT ( 'NONE',  ( -0.7500000000000179856, 8.822916667349467446, 1.299038105676658228 ) ) ;
#154226=CARTESIAN_POINT ( 'NONE',  ( -0.6823417656250039265, 14.88020833367473195, -1.181850606188755259 ) ) ;
#154233=( BOUNDED_CURVE ( )  B_SPLINE_CURVE ( 2, ( #136278, #137349, #50740, #33422, #151458, #202298, #37699, #201234, #3030 ),
 .UNSPECIFIED., .F., .T. ) 
 B_SPLINE_CURVE_WITH_KNOTS ( ( 3, 2, 2, 2, 3 ),
 ( 0.5625000000000000000, 0.5654761904761904656, 0.5714285714285713969, 0.5773809523809523281, 0.5803571428571429047 ),
 .UNSPECIFIED. ) 
 CURVE ( )  GEOMETRIC_REPRESENTATION_ITEM ( )  RATIONAL_B_SPLINE_CURVE ( ( 0.9330127018922194093, 0.9330127018922194093, 1.000000000000000000, 0.8660254037844387076, 1.000000000000000000, 0.8660254037844387076, 1.000000000000000000, 0.9330127018922180770, 0.9330127018922194093 ) ) 
 REPRESENTATION_ITEM ( '' )  );
#154270=ORIENTED_EDGE ( 'NONE', *, *, #153040, .T. ) ;
#154290=CARTESIAN_POINT ( 'NONE',  ( -1.364683531250014514, 12.90104166700806232, -0.7879004041258335089 ) ) ;
#154299=EDGE_CURVE ( 'NONE', #66068, #12932, #77541, .T. ) ;
#154460=PLANE ( 'NONE',  #198025 ) ;
#154462=CARTESIAN_POINT ( 'NONE',  ( 1.286813488861806354, 4.047007041464545374, -0.4595522011843541366 ) ) ;
#154480=DIRECTION ( 'NONE',  ( 0.1664974550714444224, 0.9062754367152173751, 0.3885143887443222588 ) ) ;
#154482=CARTESIAN_POINT ( 'NONE',  ( 1.364683531250000748, 12.00520833367472839, -0.7879004041258355073 ) ) ;
#154488=CARTESIAN_POINT ( 'NONE',  ( -1.500000000000015099, 9.729166666666669627, -0.8660254037844309360 ) ) ;
#154535=CARTESIAN_POINT ( 'NONE',  ( -8.012344526598182026E-15, 9.859375000341399797, -1.575800808251669460 ) ) ;
#154596=CARTESIAN_POINT ( 'NONE',  ( -2.788906526875773208E-15, 12.43750000000000000, -1.499999999999998446 ) ) ;
#154617=CARTESIAN_POINT ( 'NONE',  ( 0.000000000000000000, 13.49999999999999822, -1.500000000000000222 ) ) ;
#154706=EDGE_CURVE ( 'NONE', #84297, #96508, #206993, .T. ) ;
#154740=CARTESIAN_POINT ( 'NONE',  ( 0.7500000000000006661, 13.58333333333333570, 1.299038105676657340 ) ) ;
#154746=CARTESIAN_POINT ( 'NONE',  ( 0.6823417656249969321, 10.27604166700806587, -1.181850606188757036 ) ) ;
#154798=ORIENTED_EDGE ( 'NONE', *, *, #170324, .F. ) ;
#154800=DIRECTION ( 'NONE',  ( 0.000000000000000000, 0.000000000000000000, -1.000000000000000000 ) ) ;
#154803=( BOUNDED_CURVE ( )  B_SPLINE_CURVE ( 2, ( #165732, #163615, #96501, #31482, #16251, #132203, #210202, #179858, #62893 ),
 .UNSPECIFIED., .F., .T. ) 
 B_SPLINE_CURVE_WITH_KNOTS ( ( 3, 2, 2, 2, 3 ),
 ( 0.7410714285714286031, 0.7440476190476190688, 0.7500000000000000000, 0.7559523809523809312, 0.7589285714285713969 ),
 .UNSPECIFIED. ) 
 CURVE ( )  GEOMETRIC_REPRESENTATION_ITEM ( )  RATIONAL_B_SPLINE_CURVE ( ( 0.9330127018922194093, 0.9330127018922194093, 1.000000000000000000, 0.8660254037844387076, 1.000000000000000000, 0.8660254037844387076, 1.000000000000000000, 0.9330127018922194093, 0.9330127018922194093 ) ) 
 REPRESENTATION_ITEM ( '' )  );
#154818=CARTESIAN_POINT ( 'NONE',  ( -1.364683531250014514, 13.33854166700806587, -0.7879004041258335089 ) ) ;
#154858=CARTESIAN_POINT ( 'NONE',  ( 1.499999999999997113, 15.17708333401613352, -0.8660254037844378194 ) ) ;
#154885=DIRECTION ( 'NONE',  ( 0.000000000000000000, -1.000000000000000000, 0.000000000000000000 ) ) ;
#154894=CARTESIAN_POINT ( 'NONE',  ( 1.364683531249997417, 10.98437500034139802, 2.602085213965210642E-15 ) ) ;
#154900=CARTESIAN_POINT ( 'NONE',  ( -0.4019237886467001974, 9.082585450998170273, 1.500000000000001998 ) ) ;
#154961=EDGE_CURVE ( 'NONE', #80044, #1738, #198729, .T. ) ;
#154979=EDGE_CURVE ( 'NONE', #170262, #110148, #124059, .T. ) ;
#155039=CARTESIAN_POINT ( 'NONE',  ( 1.364683531249996529, 11.27604166700806410, 0.7879004041258405033 ) ) ;
#155049=FACE_OUTER_BOUND ( 'NONE', #100145, .T. ) ;
#155063=AXIS2_PLACEMENT_3D ( 'NONE', #36235, #183562, #35168 ) ;
#155065=CARTESIAN_POINT ( 'NONE',  ( -1.402160292154681736E-14, 14.92187500034139980, 1.575800808251682339 ) ) ;
#155096=CARTESIAN_POINT ( 'NONE',  ( 0.7500000000000006661, 11.61458333401613174, 1.299038105676657340 ) ) ;
#155100=CARTESIAN_POINT ( 'NONE',  ( 0.3985077402206628205, -4.205987624083942222, 1.000000000000004441 ) ) ;
#155112=CARTESIAN_POINT ( 'NONE',  ( 1.364683531249996529, 9.276041667008062319, 0.7879004041258405033 ) ) ;
#155156=CARTESIAN_POINT ( 'NONE',  ( 1.364683531249997417, 14.73437500034140157, 2.602085213965210642E-15 ) ) ;
#155193=LINE ( 'NONE', #71771, #12453 ) ;
#155293=CARTESIAN_POINT ( 'NONE',  ( -1.364683531250000748, 8.359375000341396245, 0.000000000000000000 ) ) ;
#155317=VERTEX_POINT ( 'NONE', #105545 ) ;
#155342=CARTESIAN_POINT ( 'NONE',  ( -1.500000000000001110, 8.770833333333337478, 0.8660254037844418162 ) ) ;
#155351=CARTESIAN_POINT ( 'NONE',  ( -8.012344526598182026E-15, 13.60937500034139447, -1.575800808251669460 ) ) ;
#155352=CARTESIAN_POINT ( 'NONE',  ( 0.000000000000000000, 13.49999999999999822, 0.000000000000000000 ) ) ;
#155387=CARTESIAN_POINT ( 'NONE',  ( -1.500000000000015099, 11.22916666666666785, -0.8660254037844309360 ) ) ;
#155394=AXIS2_PLACEMENT_3D ( 'NONE', #89987, #71561, #137668 ) ;
#155474=EDGE_CURVE ( 'NONE', #112831, #35502, #177841, .T. ) ;
#155528=CARTESIAN_POINT ( 'NONE',  ( 1.499999999999996891, 8.895833333333339255, -0.8660254037844378194 ) ) ;
#155549=CARTESIAN_POINT ( 'NONE',  ( -0.6823417656250039265, 10.56770833367473550, -1.181850606188755259 ) ) ;
#155555=CARTESIAN_POINT ( 'NONE',  ( 1.499999999999993117, 10.10416666666667140, 0.8660254037844409281 ) ) ;
#155597=ORIENTED_EDGE ( 'NONE', *, *, #98379, .F. ) ;
#155610=ORIENTED_EDGE ( 'NONE', *, *, #170196, .F. ) ;
#155722=CARTESIAN_POINT ( 'NONE',  ( 0.4019237886466778820, 11.82366454968463110, 1.500000000000001554 ) ) ;
#155807=LINE ( 'NONE', #153672, #87174 ) ;
#155809=CARTESIAN_POINT ( 'NONE',  ( 1.500000000000001332, 13.12499999999999822, 0.000000000000000000 ) ) ;
#155814=CARTESIAN_POINT ( 'NONE',  ( 1.364683531249997417, 10.73437500034139802, 2.602085213965210642E-15 ) ) ;
#155858=CARTESIAN_POINT ( 'NONE',  ( 0.6823417656249934904, 13.00520833367473017, 1.181850606188764807 ) ) ;
#155885=CARTESIAN_POINT ( 'NONE',  ( -1.364683531250004522, 13.36700584430852068, 0.2885925621847857947 ) ) ;
#155926=CARTESIAN_POINT ( 'NONE',  ( 0.7500000000000006661, 15.11458333401612819, 1.299038105676657340 ) ) ;
#155959=CARTESIAN_POINT ( 'NONE',  ( 0.6823417656249969321, 10.27604166700806587, -1.181850606188757036 ) ) ;
#155962=CARTESIAN_POINT ( 'NONE',  ( -0.7655046440382844430, 13.24001401857275440, -1.290086495267464883 ) ) ;
#156112=CARTESIAN_POINT ( 'NONE',  ( -1.364683531250010295, 9.442708333674733723, 0.7879004041258445001 ) ) ;
#156136=CARTESIAN_POINT ( 'NONE',  ( 0.4019237886466816012, 9.207585450998170273, -1.499999999999998668 ) ) ;
#156139=CARTESIAN_POINT ( 'NONE',  ( -0.6823417656250039265, 14.06770833367473195, -1.181850606188755259 ) ) ;
#156163=DIRECTION ( 'NONE',  ( 0.000000000000000000, -0.3940140829290779689, -0.9191044023687177100 ) ) ;
#156186=CARTESIAN_POINT ( 'NONE',  ( 0.7500000000000006661, 14.41666666666666785, -1.299038105676657340 ) ) ;
#156192=CARTESIAN_POINT ( 'NONE',  ( -1.355395447572484535, 3.935140844187386744, -0.6425755019599873608 ) ) ;
#156200=CARTESIAN_POINT ( 'NONE',  ( 1.836970198721030181E-16, 13.49999999999999822, 1.500000000000000222 ) ) ;
#156202=DIRECTION ( 'NONE',  ( -0.5000000000000001110, 0.000000000000000000, 0.8660254037844385966 ) ) ;
#156232=CARTESIAN_POINT ( 'NONE',  ( 1.364683531249997417, 13.73437500034139980, 2.602085213965210642E-15 ) ) ;
#156369=CARTESIAN_POINT ( 'NONE',  ( 0.6823417656249934904, 14.75520833367473195, 1.181850606188764807 ) ) ;
#156432=CARTESIAN_POINT ( 'NONE',  ( -0.6823417656250039265, 12.13020833367473017, -1.181850606188755259 ) ) ;
#156466=LINE ( 'NONE', #190011, #39220 ) ;
#156475=CARTESIAN_POINT ( 'NONE',  ( -1.500000000000001110, 11.05208333401613707, 0.8660254037844419273 ) ) ;
#156621=CARTESIAN_POINT ( 'NONE',  ( -1.364683531250014514, 10.58854166700806765, -0.7879004041258335089 ) ) ;
#156628=CARTESIAN_POINT ( 'NONE',  ( 0.7500000000000006661, 8.583333333333332149, 1.299038105676657340 ) ) ;
#156643=ORIENTED_EDGE ( 'NONE', *, *, #84877, .F. ) ;
#156647=CARTESIAN_POINT ( 'NONE',  ( -1.286956418854606543, 4.047654341997520611, 0.4592741676706140197 ) ) ;
#156677=CARTESIAN_POINT ( 'NONE',  ( -1.364683531250000748, 8.421875000341403350, 0.000000000000000000 ) ) ;
#156730=DIRECTION ( 'NONE',  ( 0.000000000000000000, -1.000000000000000000, 0.000000000000000000 ) ) ;
#156883=CARTESIAN_POINT ( 'NONE',  ( 1.499999999999997113, 12.39583333333333215, -0.8660254037844378194 ) ) ;
#156888=CARTESIAN_POINT ( 'NONE',  ( 1.364683531250000303, 11.00520833367473550, -0.7879004041258355073 ) ) ;
#156913=DIRECTION ( 'NONE',  ( 0.000000000000000000, -1.000000000000000000, 0.000000000000000000 ) ) ;
#156928=VERTEX_POINT ( 'NONE', #180355 ) ;
#156933=CARTESIAN_POINT ( 'NONE',  ( -1.364683531250000748, 12.42187500034139980, 0.000000000000000000 ) ) ;
#156959=CARTESIAN_POINT ( 'NONE',  ( 1.364683531249997417, 12.73437500034139980, 2.602085213965210642E-15 ) ) ;
#157002=CARTESIAN_POINT ( 'NONE',  ( -1.402160292154681736E-14, 14.84375000068279427, 1.732050807568881190 ) ) ;
#157011=DIRECTION ( 'NONE',  ( 0.000000000000000000, 0.000000000000000000, -1.000000000000000000 ) ) ;
#157034=CARTESIAN_POINT ( 'NONE',  ( -1.364683531250010295, 10.88020833367473372, 0.7879004041258445001 ) ) ;
#157049=CIRCLE ( 'NONE', #181304, 1.359291649810832503 ) ;
#157077=ORIENTED_EDGE ( 'NONE', *, *, #46969, .F. ) ;
#157080=CARTESIAN_POINT ( 'NONE',  ( -1.500000000000015099, 11.76041666734946922, -0.8660254037844309360 ) ) ;
#157180=CARTESIAN_POINT ( 'NONE',  ( -1.364683531250014514, 9.901041667008064096, -0.7879004041258335089 ) ) ;
#157203=CARTESIAN_POINT ( 'NONE',  ( 1.364683531249996529, 14.46354166700806410, 0.7879004041258405033 ) ) ;
#157250=CARTESIAN_POINT ( 'NONE',  ( 1.499999999999993117, 14.85416666666666252, 0.8660254037844409281 ) ) ;
#157267=CARTESIAN_POINT ( 'NONE',  ( 1.154700538379228147, -2.500000000000002220, -1.734723475976807094E-15 ) ) ;
#157296=CARTESIAN_POINT ( 'NONE',  ( 1.364683531249997417, 14.48437500034140157, 2.602085213965210642E-15 ) ) ;
#157442=CARTESIAN_POINT ( 'NONE',  ( -8.012344526598182026E-15, 13.10937500034140157, -1.575800808251669460 ) ) ;
#157504=CARTESIAN_POINT ( 'NONE',  ( -1.402160292154681736E-14, 11.98437500034140335, 1.575800808251682339 ) ) ;
#157546=CARTESIAN_POINT ( 'NONE',  ( -0.7500000000000006661, 11.48958333401613174, -1.299038105676657340 ) ) ;
#157657=EDGE_CURVE ( 'NONE', #147411, #191004, #23757, .T. ) ;
#157666=CARTESIAN_POINT ( 'NONE',  ( 3.834746474454188013E-15, 8.843750000682797818, 1.500000000000001554 ) ) ;
#157688=CARTESIAN_POINT ( 'NONE',  ( -1.402160292154681736E-14, 10.17187500034139447, 1.575800808251682339 ) ) ;
#157732=ORIENTED_EDGE ( 'NONE', *, *, #191014, .T. ) ;
#157759=CARTESIAN_POINT ( 'NONE',  ( 0.6823417656249934904, 15.25520833367473372, 1.181850606188764807 ) ) ;
#157896=CARTESIAN_POINT ( 'NONE',  ( 1.500000000000001332, 12.65625000068279427, 0.000000000000000000 ) ) ;
#157954=CARTESIAN_POINT ( 'NONE',  ( 0.7500000000000006661, 12.08333333333333570, 1.299038105676657340 ) ) ;
#157959=CARTESIAN_POINT ( 'NONE',  ( 1.364683531250000303, 10.50520833367473195, -0.7879004041258355073 ) ) ;
#157961=EDGE_CURVE ( 'NONE', #11879, #142064, #59463, .T. ) ;
#158002=CARTESIAN_POINT ( 'NONE',  ( 0.6823417656249934904, 11.75520833367473017, 1.181850606188764807 ) ) ;
#158069=CARTESIAN_POINT ( 'NONE',  ( 1.499999999999997113, 14.67708333401612997, -0.8660254037844378194 ) ) ;
#158096=CARTESIAN_POINT ( 'NONE',  ( 0.000000000000000000, 13.49999999999999822, 0.000000000000000000 ) ) ;
#158102=CARTESIAN_POINT ( 'NONE',  ( -1.364683531250014514, 10.08854166700806410, -0.7879004041258335089 ) ) ;
#158105=ORIENTED_EDGE ( 'NONE', *, *, #62155, .F. ) ;
#158219=EDGE_LOOP ( 'NONE', ( #90344, #1547, #85634, #157077 ) ) ;
#158253=CARTESIAN_POINT ( 'NONE',  ( -8.012344526598182026E-15, 10.35937500034139624, -1.575800808251669460 ) ) ;
#158293=CARTESIAN_POINT ( 'NONE',  ( 0.7500000000000006661, 10.33333333333333393, 1.299038105676657340 ) ) ;
#158310=CARTESIAN_POINT ( 'NONE',  ( -1.500000000000008216, 13.03125000068279604, 3.469446951953614189E-15 ) ) ;
#158319=CARTESIAN_POINT ( 'NONE',  ( 0.7500000000000006661, 15.16666666666666785, -1.299038105676657340 ) ) ;
#158325=CARTESIAN_POINT ( 'NONE',  ( 0.000000000000000000, -2.500000000000002220, -0.6500000000000000222 ) ) ;
#158360=CARTESIAN_POINT ( 'NONE',  ( -0.6823417656250003738, 14.90104166700806410, 1.181850606188754593 ) ) ;
#158415=CARTESIAN_POINT ( 'NONE',  ( 0.7500000000000006661, 11.36458333401613174, 1.299038105676657340 ) ) ;
#158451=EDGE_CURVE ( 'NONE', #110599, #202706, #197981, .T. ) ;
#158496=CARTESIAN_POINT ( 'NONE',  ( -1.402160292154681736E-14, 14.23437500034139624, 1.575800808251682339 ) ) ;
#158533=CARTESIAN_POINT ( 'NONE',  ( -0.5773502691896470473, -2.500000000000002220, 0.9999999999999991118 ) ) ;
#158535=ORIENTED_EDGE ( 'NONE', *, *, #31832, .F. ) ;
#158560=CARTESIAN_POINT ( 'NONE',  ( -1.364683531250010295, 12.19270833367473195, 0.7879004041258445001 ) ) ;
#158597=CARTESIAN_POINT ( 'NONE',  ( 0.000000000000000000, 13.49999999999999822, 0.000000000000000000 ) ) ;
#158602=CARTESIAN_POINT ( 'NONE',  ( 0.7500000000000006661, 11.19791666734946212, -1.299038105676657340 ) ) ;
#158660=CARTESIAN_POINT ( 'NONE',  ( 0.7641400526929170711, -4.157144623729202237, 0.6764706046374659998 ) ) ;
#158703=CARTESIAN_POINT ( 'NONE',  ( 1.446922511646519860, 4.325961798920477719, 0.4002501213623005927 ) ) ;
#158724=CARTESIAN_POINT ( 'NONE',  ( -1.424678450204426516, 3.742891979394406210, 0.4927150456334949413 ) ) ;
#158742=CARTESIAN_POINT ( 'NONE',  ( -1.364683531250014514, 10.33854166700806587, -0.7879004041258335089 ) ) ;
#158796=ORIENTED_EDGE ( 'NONE', *, *, #13528, .T. ) ;
#158849=CYLINDRICAL_SURFACE ( 'NONE', #16890, 1.500000000000000222 ) ;
#158884=EDGE_CURVE ( 'NONE', #91043, #151085, #14599, .T. ) ;
#158965=CARTESIAN_POINT ( 'NONE',  ( -1.500000000000015099, 10.47916666666666607, -0.8660254037844309360 ) ) ;
#158982=DIRECTION ( 'NONE',  ( 0.000000000000000000, -1.000000000000000000, 0.000000000000000000 ) ) ;
#158993=EDGE_CURVE ( 'NONE', #18633, #70036, #99082, .T. ) ;
#159006=CARTESIAN_POINT ( 'NONE',  ( -1.500000000000008216, 11.74999999999999645, 3.469446951953614189E-15 ) ) ;
#159011=CARTESIAN_POINT ( 'NONE',  ( -0.6823417656250039265, 10.06770833367473550, -1.181850606188755259 ) ) ;
#159049=CARTESIAN_POINT ( 'NONE',  ( -1.364683531250014514, 12.15104166700806765, -0.7879004041258335089 ) ) ;
#159054=CARTESIAN_POINT ( 'NONE',  ( 1.499999999999996891, 9.895833333333333925, -0.8660254037844378194 ) ) ;
#159110=DIRECTION ( 'NONE',  ( 0.000000000000000000, -1.000000000000000000, 0.000000000000000000 ) ) ;
#159115=CARTESIAN_POINT ( 'NONE',  ( -1.500000000000008216, 14.53125000068279604, 3.469446951953614189E-15 ) ) ;
#159282=CARTESIAN_POINT ( 'NONE',  ( -1.500000000000001110, 11.77083333333333570, 0.8660254037844418162 ) ) ;
#159295=CARTESIAN_POINT ( 'NONE',  ( 1.364683531250000303, 9.567708333674735499, -0.7879004041258355073 ) ) ;
#159324=CARTESIAN_POINT ( 'NONE',  ( 1.499902018610889343, 4.449786617651237286, -0.08390812002217802601 ) ) ;
#159356=CARTESIAN_POINT ( 'NONE',  ( 1.195384358724066508E-16, -4.140708350189171938, 1.000000000000004441 ) ) ;
#159365=CARTESIAN_POINT ( 'NONE',  ( -0.7500000000000006661, 14.70833333333333748, -1.299038105676657340 ) ) ;
#159409=CARTESIAN_POINT ( 'NONE',  ( 1.364683531249997417, 13.98437500034140157, 2.602085213965210642E-15 ) ) ;
#159440=( LENGTH_UNIT ( ) NAMED_UNIT ( * ) SI_UNIT ( .MILLI., .METRE. ) );
#159530=CARTESIAN_POINT ( 'NONE',  ( 1.445379498298573928, 3.562780597991719755, 0.4160626371120853539 ) ) ;
#159556=CARTESIAN_POINT ( 'NONE',  ( 1.364683531249997417, 13.04687500034139980, 2.602085213965210642E-15 ) ) ;
#159579=CYLINDRICAL_SURFACE ( 'NONE', #41988, 1.500000000000000222 ) ;
#159611=CARTESIAN_POINT ( 'NONE',  ( 0.000000000000000000, 13.49999999999999822, 0.000000000000000000 ) ) ;
#159625=CARTESIAN_POINT ( 'NONE',  ( 0.6823417656249934904, 11.25520833367473017, 1.181850606188764807 ) ) ;
#159664=CARTESIAN_POINT ( 'NONE',  ( 1.500000000000001332, 11.40625000068279427, 0.000000000000000000 ) ) ;
#159765=CARTESIAN_POINT ( 'NONE',  ( 1.443823057115801056, 4.128576303019145577, 0.4219843264276020856 ) ) ;
#159783=CARTESIAN_POINT ( 'NONE',  ( -1.367525579689991000, 3.416241981124319871, 0.2571629661623351382 ) ) ;
#159800=CARTESIAN_POINT ( 'NONE',  ( 1.364683531249997417, 10.73437500034139802, 2.602085213965210642E-15 ) ) ;
#159950=SURFACE_STYLE_FILL_AREA ( #31030 ) ;
#160011=CARTESIAN_POINT ( 'NONE',  ( 3.834746474454188013E-15, 9.062500000000001776, 1.500000000000001554 ) ) ;
#160066=CARTESIAN_POINT ( 'NONE',  ( -1.402160292154681736E-14, 12.56250000000000355, 1.732050807568881190 ) ) ;
#160073=CARTESIAN_POINT ( 'NONE',  ( -8.012344526598182026E-15, 9.796875000341399797, -1.575800808251669460 ) ) ;
#160106=ORIENTED_EDGE ( 'NONE', *, *, #68413, .T. ) ;
#160112=CARTESIAN_POINT ( 'NONE',  ( 1.364683531250000748, 12.56770833367473372, -0.7879004041258355073 ) ) ;
#160143=EDGE_CURVE ( 'NONE', #133382, #187426, #74629, .T. ) ;
#160182=CARTESIAN_POINT ( 'NONE',  ( -1.500000000000015099, 14.51041666734946567, -0.8660254037844309360 ) ) ;
#160184=ORIENTED_EDGE ( 'NONE', *, *, #66221, .F. ) ;
#160216=CARTESIAN_POINT ( 'NONE',  ( -0.6823417656250003738, 8.901041667008065872, 1.181850606188754593 ) ) ;
#160367=CARTESIAN_POINT ( 'NONE',  ( 0.6823417656249934904, 10.00520833367472839, 1.181850606188764807 ) ) ;
#160375=CARTESIAN_POINT ( 'NONE',  ( 1.264911064067348656, 3.849999999999994316, 0.5000000000000064393 ) ) ;
#160380=CARTESIAN_POINT ( 'NONE',  ( 0.5773502691896124084, -2.500000000000002220, -0.9999999999999991118 ) ) ;
#160438=AXIS2_PLACEMENT_3D ( 'NONE', #110951, #82638, #13376 ) ;
#160470=CARTESIAN_POINT ( 'NONE',  ( 0.000000000000000000, 0.000000000000000000, 0.000000000000000000 ) ) ;
#160479=CARTESIAN_POINT ( 'NONE',  ( 0.6823417656249969321, 12.77604166700806232, -1.181850606188757036 ) ) ;
#160583=CARTESIAN_POINT ( 'NONE',  ( 0.000000000000000000, -1.500000000000001332, 0.000000000000000000 ) ) ;
#160593=ADVANCED_FACE ( 'NONE', ( #13863 ), #65790, .T. ) ;
#160600=CARTESIAN_POINT ( 'NONE',  ( 1.369796495953883753, 3.411350084130203797, 0.2487645435796728144 ) ) ;
#160624=CARTESIAN_POINT ( 'NONE',  ( -1.364683531250014514, 13.90104166700806765, -0.7879004041258335089 ) ) ;
#160646=DIRECTION ( 'NONE',  ( 0.000000000000000000, 0.000000000000000000, -1.000000000000000000 ) ) ;
#160690=CARTESIAN_POINT ( 'NONE',  ( -1.364683531250010295, 11.69270833367473017, 0.7879004041258445001 ) ) ;
#160733=CARTESIAN_POINT ( 'NONE',  ( 0.7500000000000006661, 9.947916667349469222, -1.299038105676657340 ) ) ;
#160757=EDGE_CURVE ( 'NONE', #80954, #110599, #114196, .T. ) ;
#160838=CARTESIAN_POINT ( 'NONE',  ( 1.430949710260827068, 3.674736480791771509, 0.4689103363400765612 ) ) ;
#160858=CARTESIAN_POINT ( 'NONE',  ( -1.499630086250555605, 3.250805626717326202, 0.09116236908480998546 ) ) ;
#160877=CARTESIAN_POINT ( 'NONE',  ( 0.6823417656249934904, 8.942708333674733723, 1.181850606188764807 ) ) ;
#160936=DIRECTION ( 'NONE',  ( 0.000000000000000000, -1.000000000000000000, 0.000000000000000000 ) ) ;
#161029=DIRECTION ( 'NONE',  ( 0.000000000000000000, 1.000000000000000000, 0.000000000000000000 ) ) ;
#161117=CARTESIAN_POINT ( 'NONE',  ( -1.115562610750309283E-14, 8.562500000000000000, 1.500000000000001554 ) ) ;
#161139=CARTESIAN_POINT ( 'NONE',  ( 0.7500000000000006661, 12.58333333333333570, 1.299038105676657340 ) ) ;
#161145=CARTESIAN_POINT ( 'NONE',  ( -1.364683531250014514, 9.088541667008060543, -0.7879004041258335089 ) ) ;
#161153=CARTESIAN_POINT ( 'NONE',  ( -0.4339420102923736700, 3.713490786104575392, -0.4852232617283411265 ) ) ;
#161182=CARTESIAN_POINT ( 'NONE',  ( -8.012344526598182026E-15, 12.35937500034139624, -1.575800808251669460 ) ) ;
#161253=CARTESIAN_POINT ( 'NONE',  ( 0.7500000000000006661, 14.19791666734946567, -1.299038105676657340 ) ) ;
#161266=DIRECTION ( 'NONE',  ( 1.000000000000000000, 0.000000000000000000, 0.000000000000000000 ) ) ;
#161289=CARTESIAN_POINT ( 'NONE',  ( -1.364683531250010295, 8.630208333674731946, 0.7879004041258445001 ) ) ;
#161335=AXIS2_PLACEMENT_3D ( 'NONE', #14612, #93776, #193380 ) ;
#161341=CARTESIAN_POINT ( 'NONE',  ( -1.115562610750309283E-14, 10.84375000068279604, 1.500000000000001554 ) ) ;
#161423=DIRECTION ( 'NONE',  ( 0.000000000000000000, -1.000000000000000000, 0.000000000000000000 ) ) ;
#161431=CARTESIAN_POINT ( 'NONE',  ( -2.788906526875773208E-15, 10.46875000068279604, -1.499999999999998446 ) ) ;
#161478=CARTESIAN_POINT ( 'NONE',  ( 1.364643601765283432, 4.015812731716659201, 0.6238217115099053967 ) ) ;
#161530=ORIENTED_EDGE ( 'NONE', *, *, #121592, .T. ) ;
#161561=CARTESIAN_POINT ( 'NONE',  ( 1.364683531249997417, 12.98437500034139980, 2.602085213965210642E-15 ) ) ;
#161574=CARTESIAN_POINT ( 'NONE',  ( -1.318127287744123688, 4.161901352009867772, 0.3960634941688782606 ) ) ;
#161579=ORIENTED_EDGE ( 'NONE', *, *, #114249, .F. ) ;
#161629=CARTESIAN_POINT ( 'NONE',  ( -2.788906526875773208E-15, 9.187500000000001776, -1.499999999999998446 ) ) ;
#161649=ORIENTED_EDGE ( 'NONE', *, *, #17750, .T. ) ;
#161684=CARTESIAN_POINT ( 'NONE',  ( 1.352846302990980076, 3.447904424298776416, 0.3040853380226353764 ) ) ;
#161709=CARTESIAN_POINT ( 'NONE',  ( 0.6823417656249934904, 14.25520833367473195, 1.181850606188764807 ) ) ;
#161770=CARTESIAN_POINT ( 'NONE',  ( 1.364683531249997417, 10.79687500034139802, 2.602085213965210642E-15 ) ) ;
#161812=CARTESIAN_POINT ( 'NONE',  ( -0.7500000000000179856, 10.32291666734946922, 1.299038105676658228 ) ) ;
#161814=EDGE_LOOP ( 'NONE', ( #9694, #44240, #3624, #87917 ) ) ;
#161917=CARTESIAN_POINT ( 'NONE',  ( 1.465205965978033875, 4.370509616058218860, 0.3306380942217546082 ) ) ;
#161936=FACE_OUTER_BOUND ( 'NONE', #50614, .T. ) ;
#161954=CARTESIAN_POINT ( 'NONE',  ( 0.6823417656249934904, 8.692708333674733723, 1.181850606188764807 ) ) ;
#161998=VERTEX_POINT ( 'NONE', #153214 ) ;
#162002=VERTEX_POINT ( 'NONE', #70862 ) ;
#162093=( NAMED_UNIT ( * ) SI_UNIT ( $, .STERADIAN. ) SOLID_ANGLE_UNIT ( ) );
#162200=CARTESIAN_POINT ( 'NONE',  ( 1.220146605508150803E-14, 9.937500000000000000, -1.499999999999998446 ) ) ;
#162212=CARTESIAN_POINT ( 'NONE',  ( -1.500000000000015099, 10.72916666666666607, -0.8660254037844309360 ) ) ;
#162217=CARTESIAN_POINT ( 'NONE',  ( -1.364683531250010295, 9.130208333674731946, 0.7879004041258445001 ) ) ;
#162250=CARTESIAN_POINT ( 'NONE',  ( -0.6823417656250039265, 10.88020833367472839, -1.181850606188755259 ) ) ;
#162322=CARTESIAN_POINT ( 'NONE',  ( 0.7500000000000006661, 13.61458333401613352, 1.299038105676657340 ) ) ;
#162360=CARTESIAN_POINT ( 'NONE',  ( 1.364683531249997417, 9.234375000341396245, 2.602085213965210642E-15 ) ) ;
#162373=CARTESIAN_POINT ( 'NONE',  ( 0.000000000000000000, 6.161115872820241535, 1.249999999999999778 ) ) ;
#162376=VECTOR ( 'NONE', #147834, 1000.000000000000000 ) ;
#162489=FACE_OUTER_BOUND ( 'NONE', #94510, .T. ) ;
#162542=CARTESIAN_POINT ( 'NONE',  ( 1.493107181547908668, 4.435412813646488317, 0.1630395111544306885 ) ) ;
#162559=ORIENTED_EDGE ( 'NONE', *, *, #157961, .F. ) ;
#162621=CARTESIAN_POINT ( 'NONE',  ( 0.6823417656249969321, 13.27604166700806232, -1.181850606188757036 ) ) ;
#162651=EDGE_CURVE ( 'NONE', #143111, #187426, #45003, .T. ) ;
#162774=CARTESIAN_POINT ( 'NONE',  ( 0.6823417656249969321, 12.83854166700806942, -1.181850606188757036 ) ) ;
#162793=EDGE_CURVE ( 'NONE', #28009, #173308, #8919, .T. ) ;
#162837=CARTESIAN_POINT ( 'NONE',  ( 1.364683531249996529, 10.77604166700806765, 0.7879004041258405033 ) ) ;
#162876=CARTESIAN_POINT ( 'NONE',  ( -1.402160292154681736E-14, 9.593750000682801371, 1.732050807568881190 ) ) ;
#162878=VERTEX_POINT ( 'NONE', #63214 ) ;
#162981=CARTESIAN_POINT ( 'NONE',  ( 1.466385641617009128, 4.235413722433956529, -0.3259940066991331431 ) ) ;
#162998=CARTESIAN_POINT ( 'NONE',  ( -1.300073763039018004, 3.592844841581338322, -0.4337670944211725055 ) ) ;
#163016=CARTESIAN_POINT ( 'NONE',  ( 1.364683531249996529, 9.713541667008064096, 0.7879004041258403923 ) ) ;
#163091=CARTESIAN_POINT ( 'NONE',  ( 0.6823417656249934904, 13.75520833367473195, 1.181850606188764807 ) ) ;
#163274=CARTESIAN_POINT ( 'NONE',  ( -1.500000000000008216, 10.49999999999999467, 3.469446951953614189E-15 ) ) ;
#163278=CARTESIAN_POINT ( 'NONE',  ( 1.364683531249997417, 9.734375000341396245, 2.602085213965210642E-15 ) ) ;
#163286=CARTESIAN_POINT ( 'NONE',  ( -0.4839601414735590357, 3.595939936792758918, -0.4353502767700617171 ) ) ;
#163287=DIRECTION ( 'NONE',  ( 0.000000000000000000, 0.000000000000000000, -1.000000000000000000 ) ) ;
#163313=CARTESIAN_POINT ( 'NONE',  ( 0.6823417656249934904, 10.50520833367472839, 1.181850606188764807 ) ) ;
#163329=FACE_OUTER_BOUND ( 'NONE', #91487, .T. ) ;
#163330=DIRECTION ( 'NONE',  ( 0.000000000000000000, -1.000000000000000000, 0.000000000000000000 ) ) ;
#163339=DIRECTION ( 'NONE',  ( 0.000000000000000000, -1.000000000000000000, 0.000000000000000000 ) ) ;
#163391=CARTESIAN_POINT ( 'NONE',  ( 1.500000000000001332, 13.40625000068279604, 0.000000000000000000 ) ) ;
#163425=CARTESIAN_POINT ( 'NONE',  ( -0.6823417656250003738, 9.401041667008065872, 1.181850606188754593 ) ) ;
#163433=CYLINDRICAL_SURFACE ( 'NONE', #139208, 1.500000000000000222 ) ;
#163529=CARTESIAN_POINT ( 'NONE',  ( 0.6823417656249969321, 12.52604166700806232, -1.181850606188757036 ) ) ;
#163548=AXIS2_PLACEMENT_3D ( 'NONE', #184572, #59656, #142013 ) ;
#163550=AXIS2_PLACEMENT_3D ( 'NONE', #39613, #71016, #40700 ) ;
#163575=CARTESIAN_POINT ( 'NONE',  ( -1.380481604194455425, 13.35137502475254223, 0.2305342759981895417 ) ) ;
#163588=CARTESIAN_POINT ( 'NONE',  ( -0.4019237886466871523, 9.448664549684627545, -1.499999999999998668 ) ) ;
#163595=CARTESIAN_POINT ( 'NONE',  ( 1.500000000000001332, 9.125000000000001776, 0.000000000000000000 ) ) ;
#163615=CARTESIAN_POINT ( 'NONE',  ( -0.4019237886467001974, 10.08258545099816850, 1.500000000000001998 ) ) ;
#163670=CARTESIAN_POINT ( 'NONE',  ( 0.7500000000000006661, 11.08333333333333393, 1.299038105676657340 ) ) ;
#163687=CARTESIAN_POINT ( 'NONE',  ( -1.364683531250014514, 12.58854166700806054, -0.7879004041258335089 ) ) ;
#163699=CARTESIAN_POINT ( 'NONE',  ( -1.367350270964193371, 4.283378765250654752, -0.2578043790911884736 ) ) ;
#163741=( BOUNDED_CURVE ( )  B_SPLINE_CURVE ( 2, ( #20981, #166193, #36184, #168334, #86015, #185630, #37263, #103333, #87078 ),
 .UNSPECIFIED., .F., .T. ) 
 B_SPLINE_CURVE_WITH_KNOTS ( ( 3, 2, 2, 2, 3 ),
 ( 0.4017857142857143016, 0.4047619047619047672, 0.4107142857142856984, 0.4166666666666666852, 0.4196428571428570953 ),
 .UNSPECIFIED. ) 
 CURVE ( )  GEOMETRIC_REPRESENTATION_ITEM ( )  RATIONAL_B_SPLINE_CURVE ( ( 0.9330127018922194093, 0.9330127018922194093, 1.000000000000000000, 0.8660254037844387076, 1.000000000000000000, 0.8660254037844387076, 1.000000000000000000, 0.9330127018922206306, 0.9330127018922194093 ) ) 
 REPRESENTATION_ITEM ( '' )  );
#163838=CARTESIAN_POINT ( 'NONE',  ( 0.6823417656249969321, 11.83854166700806765, -1.181850606188757036 ) ) ;
#163864=CARTESIAN_POINT ( 'NONE',  ( -0.7500000000000006661, 11.95833333333333393, -1.299038105676657340 ) ) ;
#163904=CARTESIAN_POINT ( 'NONE',  ( -1.364683531250000748, 10.17187500034139802, 0.000000000000000000 ) ) ;
#163947=CARTESIAN_POINT ( 'NONE',  ( -0.7500000000000006661, 9.489583334016129967, -1.299038105676657340 ) ) ;
#163955=CARTESIAN_POINT ( 'NONE',  ( 0.7500000000000006661, 10.11458333401612997, 1.299038105676657340 ) ) ;
#163996=FACE_OUTER_BOUND ( 'NONE', #164448, .T. ) ;
#164048=CARTESIAN_POINT ( 'NONE',  ( -0.7500000000000179856, 9.291666666666669627, 1.299038105676658228 ) ) ;
#164083=CARTESIAN_POINT ( 'NONE',  ( 1.364683531250000748, 9.505208333674735499, -0.7879004041258355073 ) ) ;
#164149=CARTESIAN_POINT ( 'NONE',  ( 0.6823417656249969321, 14.33854166700806232, -1.181850606188757036 ) ) ;
#164330=CARTESIAN_POINT ( 'NONE',  ( 0.7500000000000006661, 11.41666666666666607, -1.299038105676657340 ) ) ;
#164336=CARTESIAN_POINT ( 'NONE',  ( 0.6823417656249934904, 9.442708333674735499, 1.181850606188764807 ) ) ;
#164345=B_SPLINE_CURVE_WITH_KNOTS ( 'NONE', 3,
 ( #86909, #152977, #4552, #156192, #108558, #172435, #89061, #205978, #187597, #22946, #39224, #137809, #104235, #138877 ),
 .UNSPECIFIED., .F., .F.,
 ( 4, 2, 2, 2, 2, 2, 4 ),
 ( 0.003709280639842195849, 0.003956362438780343382, 0.004203444237718490482, 0.004697607835594785550, 0.004944689634532933517, 0.005191771433471080617, 0.005685935031347376552 ),
 .UNSPECIFIED. ) ;
#164358=CARTESIAN_POINT ( 'NONE',  ( -1.279995097189637887, 3.683921063351213387, -0.4728108786798664309 ) ) ;
#164371=ORIENTED_EDGE ( 'NONE', *, *, #142087, .T. ) ;
#164375=CARTESIAN_POINT ( 'NONE',  ( -1.402160292154681736E-14, 10.98437500034139802, 1.575800808251682339 ) ) ;
#164403=CARTESIAN_POINT ( 'NONE',  ( -2.788906526875773208E-15, 10.21875000068279782, -1.499999999999998446 ) ) ;
#164445=CARTESIAN_POINT ( 'NONE',  ( -1.500000000000001110, 12.80208333401612997, 0.8660254037844419273 ) ) ;
#164448=EDGE_LOOP ( 'NONE', ( #197088, #27123, #58168, #126520, #211098 ) ) ;
#164489=CARTESIAN_POINT ( 'NONE',  ( -0.4019237886466802689, 9.479914550367428916, -1.500000000000002887 ) ) ;
#164627=CARTESIAN_POINT ( 'NONE',  ( 1.364683531249997417, 8.796875000341403350, 2.602085213965210642E-15 ) ) ;
#164649=CARTESIAN_POINT ( 'NONE',  ( 1.836970198721030181E-16, 13.49999999999999822, 1.500000000000000222 ) ) ;
#164726=CARTESIAN_POINT ( 'NONE',  ( 0.5723599497803509850, 4.245284329187786199, -0.3124809264750579851 ) ) ;
#164727=PLANE ( 'NONE',  #142093 ) ;
#164735=CARTESIAN_POINT ( 'NONE',  ( -1.364683531250010295, 12.38020833367473372, 0.7879004041258445001 ) ) ;
#164885=CARTESIAN_POINT ( 'NONE',  ( -1.364683531250014514, 12.65104166700806232, -0.7879004041258335089 ) ) ;
#164949=CARTESIAN_POINT ( 'NONE',  ( 0.6823417656249934904, 11.00520833367472839, 1.181850606188764807 ) ) ;
#164993=CARTESIAN_POINT ( 'NONE',  ( -1.500000000000008216, 9.781250000682799595, 3.469446951953614189E-15 ) ) ;
#165073=CARTESIAN_POINT ( 'NONE',  ( -0.7500000000000179856, 12.82291666734946389, 1.299038105676658228 ) ) ;
#165176=ORIENTED_EDGE ( 'NONE', *, *, #80209, .T. ) ;
#165202=CARTESIAN_POINT ( 'NONE',  ( -0.6823417656250039265, 14.63020833367473195, -1.181850606188755259 ) ) ;
#165305=AXIS2_PLACEMENT_3D ( 'NONE', #211439, #194131, #78250 ) ;
#165357=EDGE_CURVE ( 'NONE', #173308, #193052, #53209, .T. ) ;
#165365=CARTESIAN_POINT ( 'NONE',  ( 0.4019237886466814902, 11.85491455036742892, 1.499999999999999334 ) ) ;
#165387=CARTESIAN_POINT ( 'NONE',  ( -6.009258394948636914E-15, 10.93750000000000355, -1.732050807568875195 ) ) ;
#165391=CARTESIAN_POINT ( 'NONE',  ( 1.364683531249996529, 14.52604166700806232, 0.7879004041258405033 ) ) ;
#165404=CARTESIAN_POINT ( 'NONE',  ( -0.2024025116420367920, -4.140708350189159503, -0.9999999999999991118 ) ) ;
#165433=CARTESIAN_POINT ( 'NONE',  ( 1.364683531249997417, 11.04687500034139802, 2.602085213965210642E-15 ) ) ;
#165443=CIRCLE ( 'NONE', #68640, 1.240450515248286534 ) ;
#165447=CARTESIAN_POINT ( 'NONE',  ( -2.788906526875773208E-15, 10.93750000000000178, -1.499999999999998446 ) ) ;
#165508=CARTESIAN_POINT ( 'NONE',  ( 1.499999999999993117, 12.63541666734946389, 0.8660254037844409281 ) ) ;
#165591=ORIENTED_EDGE ( 'NONE', *, *, #46016, .T. ) ;
#165616=EDGE_CURVE ( 'NONE', #42462, #103348, #209431, .T. ) ;
#165668=VECTOR ( 'NONE', #140188, 1000.000000000000000 ) ;
#165732=CARTESIAN_POINT ( 'NONE',  ( -1.115562610750309283E-14, 10.09375000068279782, 1.500000000000001554 ) ) ;
#165737=CARTESIAN_POINT ( 'NONE',  ( 0.000000000000000000, 13.49999999999999822, 0.000000000000000000 ) ) ;
#165739=CARTESIAN_POINT ( 'NONE',  ( 0.7500000000000006661, 10.61458333401613174, 1.299038105676657340 ) ) ;
#165775=FACE_OUTER_BOUND ( 'NONE', #45479, .T. ) ;
#165807=CARTESIAN_POINT ( 'NONE',  ( -0.6823417656250003738, 12.15104166700806054, 1.181850606188754593 ) ) ;
#165809=ORIENTED_EDGE ( 'NONE', *, *, #165616, .T. ) ;
#165836=CARTESIAN_POINT ( 'NONE',  ( 1.404687167041647866, 13.32212500979552594, 0.2168455861850217548 ) ) ;
#165953=CARTESIAN_POINT ( 'NONE',  ( -1.402160292154681736E-14, 11.98437500034140335, 1.575800808251682339 ) ) ;
#165975=EDGE_CURVE ( 'NONE', #78562, #112702, #1045, .T. ) ;
#165977=CARTESIAN_POINT ( 'NONE',  ( -0.6823417656250003738, 15.15104166700806410, 1.181850606188754593 ) ) ;
#166007=VECTOR ( 'NONE', #198633, 1000.000000000000000 ) ;
#166019=CARTESIAN_POINT ( 'NONE',  ( -8.012344526598182026E-15, 10.35937500034139624, -1.575800808251669460 ) ) ;
#166048=CARTESIAN_POINT ( 'NONE',  ( 1.499999999999993117, 12.10416666666666607, 0.8660254037844408170 ) ) ;
#166061=CARTESIAN_POINT ( 'NONE',  ( 0.7500000000000006661, 9.197916667349467446, -1.299038105676657340 ) ) ;
#166133=EDGE_LOOP ( 'NONE', ( #160184, #140753, #58473, #181568 ) ) ;
#166157=ORIENTED_EDGE ( 'NONE', *, *, #172733, .F. ) ;
#166159=CARTESIAN_POINT ( 'NONE',  ( -1.115562610750309283E-14, 9.343750000682801371, 1.500000000000001554 ) ) ;
#166193=CARTESIAN_POINT ( 'NONE',  ( 0.4019237886466816012, 12.67633545031536713, -1.499999999999998668 ) ) ;
#166204=DIRECTION ( 'NONE',  ( 0.000000000000000000, -1.000000000000000000, 0.000000000000000000 ) ) ;
#166249=VERTEX_POINT ( 'NONE', #121305 ) ;
#166265=CARTESIAN_POINT ( 'NONE',  ( -1.364683531250014514, 13.90104166700806765, -0.7879004041258335089 ) ) ;
#166284=ORIENTED_EDGE ( 'NONE', *, *, #49580, .T. ) ;
#166446=CARTESIAN_POINT ( 'NONE',  ( 0.4019237886466847653, 13.10491455036743247, 1.499999999999997113 ) ) ;
#166460=CARTESIAN_POINT ( 'NONE',  ( 1.499999999999993117, 10.85416666666666785, 0.8660254037844409281 ) ) ;
#166473=CARTESIAN_POINT ( 'NONE',  ( 0.4019237886466778820, 9.573664549684629321, 1.500000000000001554 ) ) ;
#166482=EDGE_CURVE ( 'NONE', #14542, #188147, #17117, .T. ) ;
#166506=CARTESIAN_POINT ( 'NONE',  ( 0.6823417656249969321, 9.088541667008065872, -1.181850606188757036 ) ) ;
#166583=CARTESIAN_POINT ( 'NONE',  ( -6.009258394948636914E-15, 12.96875000068280137, -1.732050807568875195 ) ) ;
#166674=CARTESIAN_POINT ( 'NONE',  ( -8.012344526598182026E-15, 13.54687500034139269, -1.575800808251669460 ) ) ;
#166728=CARTESIAN_POINT ( 'NONE',  ( -1.364683531250010295, 11.38020833367473728, 0.7879004041258445001 ) ) ;
#166798=DIRECTION ( 'NONE',  ( -0.5000000000000003331, 0.000000000000000000, -0.8660254037844383745 ) ) ;
#166877=CARTESIAN_POINT ( 'NONE',  ( -0.6823417656250003738, 11.65104166700806765, 1.181850606188754593 ) ) ;
#166998=ORIENTED_EDGE ( 'NONE', *, *, #109767, .F. ) ;
#167026=CARTESIAN_POINT ( 'NONE',  ( 0.6823417656249934904, 11.75520833367473017, 1.181850606188764807 ) ) ;
#167079=ORIENTED_EDGE ( 'NONE', *, *, #112471, .F. ) ;
#167080=CARTESIAN_POINT ( 'NONE',  ( -0.6823417656250039265, 13.06770833367473017, -1.181850606188755259 ) ) ;
#167095=CARTESIAN_POINT ( 'NONE',  ( -1.364683531250000748, 8.921875000341403350, 0.000000000000000000 ) ) ;
#167137=CARTESIAN_POINT ( 'NONE',  ( 0.6823417656249969321, 15.27604166700806410, -1.181850606188757036 ) ) ;
#167274=CARTESIAN_POINT ( 'NONE',  ( 0.6823417656249969321, 8.526041667008064096, -1.181850606188757036 ) ) ;
#167275=DIRECTION ( 'NONE',  ( 0.000000000000000000, -1.000000000000000000, 0.000000000000000000 ) ) ;
#167276=CARTESIAN_POINT ( 'NONE',  ( -2.788906526875773208E-15, 13.18750000000000000, -1.499999999999998446 ) ) ;
#167341=CARTESIAN_POINT ( 'NONE',  ( 0.6823417656249934904, 14.25520833367473195, 1.181850606188764807 ) ) ;
#167459=EDGE_CURVE ( 'NONE', #196686, #80044, #173514, .T. ) ;
#167500=EDGE_CURVE ( 'NONE', #190224, #109852, #59386, .T. ) ;
#167522=CARTESIAN_POINT ( 'NONE',  ( -8.012344526598182026E-15, 12.54687500034139980, -1.575800808251669460 ) ) ;
#167527=CARTESIAN_POINT ( 'NONE',  ( -0.7500000000000006661, 9.208333333333332149, -1.299038105676657340 ) ) ;
#167575=CARTESIAN_POINT ( 'NONE',  ( -0.6823417656250039265, 9.380208333674728394, -1.181850606188755259 ) ) ;
#167588=CARTESIAN_POINT ( 'NONE',  ( 1.500000000000001332, 10.87499999999999645, 0.000000000000000000 ) ) ;
#167645=CARTESIAN_POINT ( 'NONE',  ( -0.7500000000000179856, 12.82291666734946389, 1.299038105676658228 ) ) ;
#167693=CARTESIAN_POINT ( 'NONE',  ( 1.274579945453880647, 3.715243558054538653, 0.4827076737218298219 ) ) ;
#167736=CARTESIAN_POINT ( 'NONE',  ( -1.364683531250014514, 13.58854166700806587, -0.7879004041258335089 ) ) ;
#167782=CARTESIAN_POINT ( 'NONE',  ( 0.7500000000000006661, 13.91666666666666785, -1.299038105676657340 ) ) ;
#167790=CARTESIAN_POINT ( 'NONE',  ( 0.6823417656249969321, 12.52604166700806232, -1.181850606188757036 ) ) ;
#167828=ORIENTED_EDGE ( 'NONE', *, *, #93138, .F. ) ;
#167833=CARTESIAN_POINT ( 'NONE',  ( 0.6823417656249969321, 13.08854166700806942, -1.181850606188757036 ) ) ;
#167834=ADVANCED_FACE ( 'NONE', ( #172397 ), #70583, .T. ) ;
#167913=CYLINDRICAL_SURFACE ( 'NONE', #56318, 1.500000000000000222 ) ;
#167935=CARTESIAN_POINT ( 'NONE',  ( -1.364683531250014514, 11.58854166700806410, -0.7879004041258335089 ) ) ;
#167943=DIRECTION ( 'NONE',  ( 0.000000000000000000, 0.000000000000000000, -1.000000000000000000 ) ) ;
#168026=EDGE_LOOP ( 'NONE', ( #104175, #15315, #120778, #46804, #87692 ) ) ;
#168032=APPLICATION_CONTEXT ( 'automotive_design' ) ;
#168055=EDGE_LOOP ( 'NONE', ( #149575, #187344, #185400, #130084 ) ) ;
#168067=ORIENTED_EDGE ( 'NONE', *, *, #157657, .F. ) ;
#168088=CARTESIAN_POINT ( 'NONE',  ( -0.6823417656250039265, 11.38020833367473017, -1.181850606188755259 ) ) ;
#168137=CARTESIAN_POINT ( 'NONE',  ( 0.7500000000000006661, 11.69791666734946389, -1.299038105676657340 ) ) ;
#168154=CARTESIAN_POINT ( 'NONE',  ( -1.364683531250010295, 9.442708333674733723, 0.7879004041258445001 ) ) ;
#168161=FACE_OUTER_BOUND ( 'NONE', #9633, .T. ) ;
#168182=CARTESIAN_POINT ( 'NONE',  ( -3.602337597214539753E-15, 12.06250000000000178, 1.500000000000001554 ) ) ;
#168195=CARTESIAN_POINT ( 'NONE',  ( -0.7500000000000179856, 8.572916667349467446, 1.299038105676658228 ) ) ;
#168311=VECTOR ( 'NONE', #195238, 1000.000000000000000 ) ;
#168334=CARTESIAN_POINT ( 'NONE',  ( 1.499999999999996891, 12.64583333333333215, -0.8660254037844378194 ) ) ;
#168343=FACE_OUTER_BOUND ( 'NONE', #32316, .T. ) ;
#168387=DIRECTION ( 'NONE',  ( 0.000000000000000000, 0.000000000000000000, -1.000000000000000000 ) ) ;
#168402=CARTESIAN_POINT ( 'NONE',  ( -0.6823417656250039265, 13.63020833367473195, -1.181850606188755259 ) ) ;
#168446=CARTESIAN_POINT ( 'NONE',  ( 0.5773502691896192918, -2.500000000000002220, 1.000000000000004441 ) ) ;
#168482=CARTESIAN_POINT ( 'NONE',  ( -0.4019237886466871523, 10.97991455036742359, -1.499999999999998668 ) ) ;
#168582=CARTESIAN_POINT ( 'NONE',  ( 0.6823417656249969321, 11.77604166700806054, -1.181850606188757036 ) ) ;
#168587=CARTESIAN_POINT ( 'NONE',  ( 1.500000000000001332, 9.875000000000001776, 0.000000000000000000 ) ) ;
#168604=CARTESIAN_POINT ( 'NONE',  ( 0.7500000000000006661, 9.583333333333332149, 1.299038105676657340 ) ) ;
#168635=CARTESIAN_POINT ( 'NONE',  ( -1.364683531250000748, 9.921875000341398021, 0.000000000000000000 ) ) ;
#168638=VECTOR ( 'NONE', #205853, 1000.000000000000000 ) ;
#168693=CARTESIAN_POINT ( 'NONE',  ( -1.115562610750309283E-14, 8.562500000000000000, 1.500000000000001554 ) ) ;
#168710=CARTESIAN_POINT ( 'NONE',  ( 1.499999999999993117, 11.38541666734946567, 0.8660254037844409281 ) ) ;
#168759=CARTESIAN_POINT ( 'NONE',  ( 1.286956418854607431, 3.652345658002486672, 0.4592741676706121323 ) ) ;
#168797=CARTESIAN_POINT ( 'NONE',  ( -1.364683531250010295, 12.88020833367473372, 0.7879004041258445001 ) ) ;
#168843=CARTESIAN_POINT ( 'NONE',  ( -1.500000000000015099, 13.47916666666667140, -0.8660254037844309360 ) ) ;
#168849=CARTESIAN_POINT ( 'NONE',  ( -1.364683531250000748, 11.35937500034139802, 0.000000000000000000 ) ) ;
#168917=CARTESIAN_POINT ( 'NONE',  ( -2.788906526875773208E-15, 10.18750000000000000, -1.499999999999998446 ) ) ;
#168928=ORIENTED_EDGE ( 'NONE', *, *, #71800, .F. ) ;
#168996=CARTESIAN_POINT ( 'NONE',  ( -8.012344526598182026E-15, 11.79687500034140157, -1.575800808251669460 ) ) ;
#169003=CARTESIAN_POINT ( 'NONE',  ( -1.500000000000001110, 9.052083334016126415, 0.8660254037844418162 ) ) ;
#169050=VERTEX_POINT ( 'NONE', #111193 ) ;
#169145=CARTESIAN_POINT ( 'NONE',  ( -1.364683531250014514, 11.40104166700806410, -0.7879004041258335089 ) ) ;
#169215=CARTESIAN_POINT ( 'NONE',  ( 0.6823417656249934904, 8.755208333674733723, 1.181850606188764807 ) ) ;
#169260=CARTESIAN_POINT ( 'NONE',  ( 1.500000000000001332, 8.406250000682797818, 0.000000000000000000 ) ) ;
#169325=DIRECTION ( 'NONE',  ( 0.000000000000000000, -1.000000000000000000, 0.000000000000000000 ) ) ;
#169328=B_SPLINE_CURVE_WITH_KNOTS ( 'NONE', 3,
 ( #52875, #103775, #153588, #167693, #36615, #168759 ),
 .UNSPECIFIED., .F., .F.,
 ( 4, 2, 4 ),
 ( 0.001616326159039268694, 0.001719602896561273769, 0.001822879634083278844 ),
 .UNSPECIFIED. ) ;
#169343=ORIENTED_EDGE ( 'NONE', *, *, #91968, .T. ) ;
#169359=ORIENTED_EDGE ( 'NONE', *, *, #68413, .F. ) ;
#169396=CARTESIAN_POINT ( 'NONE',  ( -0.6823417656250003738, 8.651041667008065872, 1.181850606188754593 ) ) ;
#169401=CARTESIAN_POINT ( 'NONE',  ( 0.6823417656249969321, 15.08854166700806410, -1.181850606188757036 ) ) ;
#169409=( BOUNDED_CURVE ( )  B_SPLINE_CURVE ( 2, ( #105013, #155885, #205677, #154818, #6403, #198482, #138575, #71400, #199550, #117315, #23731, #183311, #189441, #100990, #107191, #57314, #167080, #172136, #18671, #188365, #40005, #106115, #173216, #150838, #89836, #182237, #7473, #116249, #5318, #137512, #73554, #90898, #156959, #8551, #50127, #87341, #137172, #84133, #201057, #179779, #170717, #167522, #163529, #71056, #169651, #54842, #31398, #118829, #153409, #35375, #200001, #150219, #21236, #97472, #18046, #196031, #38592, #53775, #52698, #6060, #101449, #4978, #22303, #104669, #183765, #88414, #19119, #154482, #47666, #130039, #102519, #113777, #136099, #186960, #1791, #185883, #67848, #135044, #168582, #133995, #51651, #120993, #117774, #85198, #203196, #151283, #103594, #2854, #184815, #36445, #68923, #20182, #86269, #152340, #3918, #69987, #202115, #119908, #37518, #26595, #107930, #10336, #72131, #93761, #92696, #76410, #23383, #140392, #122061, #110056, #41817, #74296, #206411, #59098, #123148, #189105, #89495, #40738, #55904, #139307, #205336, #108990, #39654, #188025, #138238, #192280, #207478, #58035, #159800, #106844, #56974, #172875, #24446, #90559, #105763, #156621, #155549, #25528, #43940, #124199, #204252, #75359, #126319, #171788, #125258, #7128, #191218, #158742, #173954, #190163, #91636, #73201, #42881, #8211, #141471, #157688, #175009, #142520, #9286, #208529, #60165, #176068, #27666, #64439, #111121, #197620, #65470, #112195, #13545, #130583, #194433, #212801, #46074, #195509, #181379, #77481, #177124, #163016, #79616, #129529, #30890, #143600, #114327, #33003, #12471, #196573, #80695, #164083, #147833, #131621, #180323, #49264, #28741, #11403, #47146, #31945, #15664, #179267, #113262, #209592, #145735, #193366, #94826, #115385, #78546, #45011, #61238, #96968, #14598, #211735, #146786, #127394, #99081, #63373, #160877, #62306, #48215, #144664, #98029, #210678, #178200, #81751, #213851, #128465, #29817, #95901, #161954, #119647, #169396, #116438, #18859, #458, #202938, #134793, #167274, #84943, #152089, #1531, #67594, #182432, #133739, #199746, #17783 ),
 .UNSPECIFIED., .F., .T. ) 
 B_SPLINE_CURVE_WITH_KNOTS ( ( 3, 2, 2, 2, 2, 2, 2, 2, 2, 2, 2, 2, 2, 2, 2, 2, 2, 2, 2, 2, 2, 2, 2, 2, 2, 2, 2, 2, 2, 2, 2, 2, 2, 2, 2, 2, 2, 2, 2, 2, 2, 2, 2, 2, 2, 2, 2, 2, 2, 2, 2, 2, 2, 2, 2, 2, 2, 2, 2, 2, 2, 2, 2, 2, 2, 2, 2, 2, 2, 2, 2, 2, 2, 2, 2, 2, 2, 2, 2, 2, 2, 2, 2, 2, 2, 2, 2, 2, 2, 2, 2, 2, 2, 2, 2, 2, 2, 2, 2, 2, 2, 2, 2, 2, 2, 2, 2, 2, 2, 2, 2, 2, 2, 2, 2, 2, 2, 2, 2, 2, 2, 3 ),
 ( 0.2833317628822501488, 0.2857142857142856984, 0.2916666666666666852, 0.2976190476190476164, 0.3035714285714285476, 0.3095238095238095344, 0.3154761904761904656, 0.3214285714285714524, 0.3273809523809523836, 0.3333333333333333148, 0.3392857142857143016, 0.3452380952380952328, 0.3511904761904761640, 0.3571428571428571508, 0.3630952380952380820, 0.3690476190476190688, 0.3750000000000000000, 0.3809523809523809312, 0.3869047619047619180, 0.3928571428571428492, 0.3988095238095238360, 0.4047619047619047672, 0.4107142857142856984, 0.4166666666666666852, 0.4226190476190476164, 0.4285714285714285476, 0.4345238095238095344, 0.4404761904761904656, 0.4464285714285714524, 0.4523809523809523836, 0.4583333333333333148, 0.4642857142857143016, 0.4702380952380952328, 0.4761904761904761640, 0.4821428571428571508, 0.4880952380952380820, 0.4940476190476190688, 0.5000000000000000000, 0.5059523809523809312, 0.5119047619047618625, 0.5178571428571429047, 0.5238095238095238360, 0.5297619047619047672, 0.5357142857142856984, 0.5416666666666666297, 0.5476190476190476719, 0.5535714285714286031, 0.5595238095238095344, 0.5654761904761904656, 0.5714285714285713969, 0.5773809523809523281, 0.5833333333333333703, 0.5892857142857143016, 0.5952380952380952328, 0.6011904761904761640, 0.6071428571428570953, 0.6130952380952381375, 0.6190476190476190688, 0.6250000000000000000, 0.6309523809523809312, 0.6369047619047618625, 0.6428571428571430157, 0.6488095238095238360, 0.6547619047619047672, 0.6607142857142856984, 0.6666666666666665186, 0.6726190476190476719, 0.6785714285714286031, 0.6845238095238095344, 0.6904761904761904656, 0.6964285714285713969, 0.7023809523809523281, 0.7083333333333333703, 0.7142857142857143016, 0.7202380952380952328, 0.7261904761904760530, 0.7321428571428570953, 0.7380952380952381375, 0.7440476190476190688, 0.7500000000000000000, 0.7559523809523809312, 0.7619047619047618625, 0.7678571428571429047, 0.7738095238095238360, 0.7797619047619047672, 0.7857142857142856984, 0.7916666666666666297, 0.7976190476190476719, 0.8035714285714286031, 0.8095238095238095344, 0.8154761904761904656, 0.8214285714285713969, 0.8273809523809523281, 0.8333333333333333703, 0.8392857142857143016, 0.8452380952380952328, 0.8511904761904761640, 0.8571428571428570953, 0.8630952380952381375, 0.8690476190476190688, 0.8750000000000000000, 0.8809523809523809312, 0.8869047619047618625, 0.8928571428571429047, 0.8988095238095238360, 0.9047619047619047672, 0.9107142857142856984, 0.9166666666666666297, 0.9226190476190476719, 0.9285714285714286031, 0.9345238095238095344, 0.9404761904761904656, 0.9464285714285713969, 0.9523809523809523281, 0.9583333333333333703, 0.9642857142857143016, 0.9702380952380952328, 0.9761904761904761640, 0.9821428571428570953, 0.9880952380952381375, 0.9940476190476190688, 1.000000000000000000 ),
 .UNSPECIFIED. ) 
 CURVE ( )  GEOMETRIC_REPRESENTATION_ITEM ( )  RATIONAL_B_SPLINE_CURVE ( ( 0.9356780735513487990, 0.9463748142214183368, 1.000000000000000000, 0.8660254037844387076, 1.000000000000000000, 0.8660254037844387076, 1.000000000000000000, 0.8660254037844387076, 1.000000000000000000, 0.8660254037844387076, 1.000000000000000000, 0.8660254037844387076, 1.000000000000000000, 0.8660254037844387076, 1.000000000000000000, 0.8660254037844387076, 1.000000000000000000, 0.8660254037844387076, 1.000000000000000000, 0.8660254037844387076, 1.000000000000000000, 0.8660254037844387076, 1.000000000000000000, 0.8660254037844387076, 1.000000000000000000, 0.8660254037844387076, 1.000000000000000000, 0.8660254037844387076, 1.000000000000000000, 0.8660254037844387076, 1.000000000000000000, 0.8660254037844387076, 1.000000000000000000, 0.8660254037844387076, 1.000000000000000000, 0.8660254037844387076, 1.000000000000000000, 0.8660254037844387076, 1.000000000000000000, 0.8660254037844387076, 1.000000000000000000, 0.8660254037844387076, 1.000000000000000000, 0.8660254037844387076, 1.000000000000000000, 0.8660254037844387076, 1.000000000000000000, 0.8660254037844387076, 1.000000000000000000, 0.8660254037844387076, 1.000000000000000000, 0.8660254037844387076, 1.000000000000000000, 0.8660254037844387076, 1.000000000000000000, 0.8660254037844387076, 1.000000000000000000, 0.8660254037844387076, 1.000000000000000000, 0.8660254037844387076, 1.000000000000000000, 0.8660254037844387076, 1.000000000000000000, 0.8660254037844387076, 1.000000000000000000, 0.8660254037844387076, 1.000000000000000000, 0.8660254037844387076, 1.000000000000000000, 0.8660254037844387076, 1.000000000000000000, 0.8660254037844387076, 1.000000000000000000, 0.8660254037844387076, 1.000000000000000000, 0.8660254037844387076, 1.000000000000000000, 0.8660254037844387076, 1.000000000000000000, 0.8660254037844387076, 1.000000000000000000, 0.8660254037844387076, 1.000000000000000000, 0.8660254037844387076, 1.000000000000000000, 0.8660254037844387076, 1.000000000000000000, 0.8660254037844387076, 1.000000000000000000, 0.8660254037844387076, 1.000000000000000000, 0.8660254037844387076, 1.000000000000000000, 0.8660254037844387076, 1.000000000000000000, 0.8660254037844387076, 1.000000000000000000, 0.8660254037844387076, 1.000000000000000000, 0.8660254037844387076, 1.000000000000000000, 0.8660254037844387076, 1.000000000000000000, 0.8660254037844387076, 1.000000000000000000, 0.8660254037844387076, 1.000000000000000000, 0.8660254037844387076, 1.000000000000000000, 0.8660254037844387076, 1.000000000000000000, 0.8660254037844387076, 1.000000000000000000, 0.8660254037844387076, 1.000000000000000000, 0.8660254037844387076, 1.000000000000000000, 0.8660254037844387076, 1.000000000000000000, 0.8660254037844387076, 1.000000000000000000, 0.8660254037844387076, 1.000000000000000000, 0.8660254037844387076, 1.000000000000000000, 0.8660254037844387076, 1.000000000000000000, 0.8660254037844387076, 1.000000000000000000, 0.8660254037844387076, 1.000000000000000000, 0.8660254037844387076, 1.000000000000000000, 0.8660254037844387076, 1.000000000000000000, 0.8660254037844387076, 1.000000000000000000, 0.8660254037844387076, 1.000000000000000000, 0.8660254037844387076, 1.000000000000000000, 0.8660254037844387076, 1.000000000000000000, 0.8660254037844387076, 1.000000000000000000, 0.8660254037844387076, 1.000000000000000000, 0.8660254037844387076, 1.000000000000000000, 0.8660254037844387076, 1.000000000000000000, 0.8660254037844387076, 1.000000000000000000, 0.8660254037844387076, 1.000000000000000000, 0.8660254037844387076, 1.000000000000000000, 0.8660254037844387076, 1.000000000000000000, 0.8660254037844387076, 1.000000000000000000, 0.8660254037844387076, 1.000000000000000000, 0.8660254037844387076, 1.000000000000000000, 0.8660254037844387076, 1.000000000000000000, 0.8660254037844387076, 1.000000000000000000, 0.8660254037844387076, 1.000000000000000000, 0.8660254037844387076, 1.000000000000000000, 0.8660254037844387076, 1.000000000000000000, 0.8660254037844387076, 1.000000000000000000, 0.8660254037844387076, 1.000000000000000000, 0.8660254037844387076, 1.000000000000000000, 0.8660254037844387076, 1.000000000000000000, 0.8660254037844387076, 1.000000000000000000, 0.8660254037844387076, 1.000000000000000000, 0.8660254037844387076, 1.000000000000000000, 0.8660254037844387076, 1.000000000000000000, 0.8660254037844387076, 1.000000000000000000, 0.8660254037844387076, 1.000000000000000000, 0.8660254037844387076, 1.000000000000000000, 0.8660254037844387076, 1.000000000000000000, 0.8660254037844387076, 1.000000000000000000, 0.8660254037844387076, 1.000000000000000000, 0.8660254037844387076, 1.000000000000000000, 0.8660254037844387076, 1.000000000000000000, 0.8660254037844387076, 1.000000000000000000, 0.8660254037844387076, 1.000000000000000000, 0.8660254037844387076, 1.000000000000000000, 0.8660254037844387076, 1.000000000000000000, 0.8660254037844387076, 1.000000000000000000, 0.8660254037844387076, 1.000000000000000000, 0.8660254037844387076, 1.000000000000000000, 0.8660254037844387076, 1.000000000000000000, 0.8660254037844387076, 1.000000000000000000, 0.8660254037844387076, 1.000000000000000000, 0.8660254037844387076, 1.000000000000000000, 0.8660254037844387076, 1.000000000000000000, 0.8660254037844387076, 1.000000000000000000, 0.8660254037844387076, 1.000000000000000000, 0.8660254037844387076, 1.000000000000000000, 0.8660254037844387076, 1.000000000000000000, 0.8660254037844387076, 1.000000000000000000, 0.8660254037844387076, 1.000000000000000000 ) ) 
 REPRESENTATION_ITEM ( '' )  );
#169413=EDGE_LOOP ( 'NONE', ( #153050, #47562, #13220, #105015 ) ) ;
#169463=CARTESIAN_POINT ( 'NONE',  ( 1.364683531250000303, 13.56770833367473017, -0.7879004041258355073 ) ) ;
#169550=CARTESIAN_POINT ( 'NONE',  ( -0.7500000000000179856, 11.07291666734946212, 1.299038105676658228 ) ) ;
#169651=CARTESIAN_POINT ( 'NONE',  ( 1.364683531249997417, 12.48437500034139980, 2.602085213965210642E-15 ) ) ;
#169655=CARTESIAN_POINT ( 'NONE',  ( 0.7500000000000006661, 9.333333333333332149, 1.299038105676657340 ) ) ;
#169656=CARTESIAN_POINT ( 'NONE',  ( 1.499999999999993117, 9.854166666666671404, 0.8660254037844409281 ) ) ;
#169704=CARTESIAN_POINT ( 'NONE',  ( 0.6823417656249969321, 9.838541667008065872, -1.181850606188757036 ) ) ;
#169776=CARTESIAN_POINT ( 'NONE',  ( 0.7500000000000006661, 11.61458333401613174, 1.299038105676657340 ) ) ;
#169861=CARTESIAN_POINT ( 'NONE',  ( -1.500000000000015099, 12.47916666666666785, -0.8660254037844309360 ) ) ;
#169862=CARTESIAN_POINT ( 'NONE',  ( -0.6823417656250003738, 13.90104166700806232, 1.181850606188754593 ) ) ;
#169906=CARTESIAN_POINT ( 'NONE',  ( -1.402160292154681736E-14, 13.06249999999999822, 1.732050807568881190 ) ) ;
#169912=CARTESIAN_POINT ( 'NONE',  ( -1.402160292154681736E-14, 12.42187500034139802, 1.575800808251682339 ) ) ;
#169938=CARTESIAN_POINT ( 'NONE',  ( 1.836970198721030181E-16, 13.49999999999999822, 1.500000000000000222 ) ) ;
#169951=ORIENTED_EDGE ( 'NONE', *, *, #212216, .F. ) ;
#170001=DIRECTION ( 'NONE',  ( -0.4999999999999997224, 0.000000000000000000, -0.8660254037844387076 ) ) ;
#170022=CARTESIAN_POINT ( 'NONE',  ( 0.7500000000000006661, 14.86458333401613530, 1.299038105676657340 ) ) ;
#170056=CARTESIAN_POINT ( 'NONE',  ( 1.364683531249997417, 11.23437500034139802, 2.602085213965210642E-15 ) ) ;
#170172=CARTESIAN_POINT ( 'NONE',  ( -0.4019237886466871523, 10.94866454968463110, -1.499999999999998668 ) ) ;
#170196=EDGE_CURVE ( 'NONE', #131458, #113572, #114029, .T. ) ;
#170209=CARTESIAN_POINT ( 'NONE',  ( -1.402160292154681736E-14, 11.23437500034139980, 1.575800808251682339 ) ) ;
#170236=CARTESIAN_POINT ( 'NONE',  ( 0.6823417656249934904, 14.44270833367473195, 1.181850606188764807 ) ) ;
#170253=VERTEX_POINT ( 'NONE', #139335 ) ;
#170262=VERTEX_POINT ( 'NONE', #109021 ) ;
#170266=FACE_OUTER_BOUND ( 'NONE', #131292, .T. ) ;
#170275=CARTESIAN_POINT ( 'NONE',  ( -1.402160292154681736E-14, 8.984375000341396245, 1.575800808251682339 ) ) ;
#170316=CARTESIAN_POINT ( 'NONE',  ( -1.500000000000008216, 8.281250000682797818, 3.469446951953614189E-15 ) ) ;
#170324=EDGE_CURVE ( 'NONE', #127955, #91043, #127963, .T. ) ;
#170329=CARTESIAN_POINT ( 'NONE',  ( -1.272148008267886654, 3.977632425219428391, -0.4878157535072980000 ) ) ;
#170333=CONICAL_SURFACE ( 'NONE', #184554, 1.376945625684933061, 0.7853981633974491672 ) ;
#170413=CARTESIAN_POINT ( 'NONE',  ( 1.500000000000001332, 8.406250000682797818, 0.000000000000000000 ) ) ;
#170462=CARTESIAN_POINT ( 'NONE',  ( 1.364683531249996529, 8.463541667008065872, 0.7879004041258405033 ) ) ;
#170525=CARTESIAN_POINT ( 'NONE',  ( 1.364683531249996529, 12.52604166700806054, 0.7879004041258405033 ) ) ;
#170651=CARTESIAN_POINT ( 'NONE',  ( -1.291015824433223491, 4.080642823807198560, -0.4575187270168924458 ) ) ;
#170694=DIRECTION ( 'NONE',  ( -1.000000000000000000, 0.000000000000000000, 0.000000000000000000 ) ) ;
#170717=CARTESIAN_POINT ( 'NONE',  ( -0.6823417656250039265, 12.56770833367473017, -1.181850606188755259 ) ) ;
#170723=CARTESIAN_POINT ( 'NONE',  ( 0.7500000000000006661, 9.916666666666671404, -1.299038105676657340 ) ) ;
#170765=VERTEX_POINT ( 'NONE', #113291 ) ;
#170775=CARTESIAN_POINT ( 'NONE',  ( 1.364683531249996529, 8.776041667008067648, 0.7879004041258403923 ) ) ;
#170920=VERTEX_POINT ( 'NONE', #153176 ) ;
#170928=CARTESIAN_POINT ( 'NONE',  ( -1.500000000000008216, 12.49999999999999645, 3.469446951953614189E-15 ) ) ;
#170929=CARTESIAN_POINT ( 'NONE',  ( -1.364683531250010295, 13.38020833367473017, 0.7879004041258445001 ) ) ;
#170976=CARTESIAN_POINT ( 'NONE',  ( 1.499999999999997113, 14.14583333333333037, -0.8660254037844378194 ) ) ;
#170981=CARTESIAN_POINT ( 'NONE',  ( 1.364683531249996529, 11.46354166700806410, 0.7879004041258405033 ) ) ;
#171028=CARTESIAN_POINT ( 'NONE',  ( 0.6823417656249969321, 13.33854166700806942, -1.181850606188757036 ) ) ;
#171094=VERTEX_POINT ( 'NONE', #133765 ) ;
#171104=ORIENTED_EDGE ( 'NONE', *, *, #9331, .F. ) ;
#171128=CARTESIAN_POINT ( 'NONE',  ( 0.6823417656249934904, 9.692708333674735499, 1.181850606188764807 ) ) ;
#171173=ORIENTED_EDGE ( 'NONE', *, *, #41132, .F. ) ;
#171176=CARTESIAN_POINT ( 'NONE',  ( -2.788906526875773208E-15, 11.71875000068279604, -1.499999999999998446 ) ) ;
#171278=CARTESIAN_POINT ( 'NONE',  ( 1.364683531249996529, 10.77604166700806765, 0.7879004041258405033 ) ) ;
#171289=CARTESIAN_POINT ( 'NONE',  ( 0.000000000000000000, 0.000000000000000000, 2.000000000000000000 ) ) ;
#171304=CARTESIAN_POINT ( 'NONE',  ( -1.364683531250014514, 14.08854166700806942, -0.7879004041258335089 ) ) ;
#171335=CARTESIAN_POINT ( 'NONE',  ( -0.4019237886466933696, 13.08258545099817027, 1.500000000000005995 ) ) ;
#171345=CARTESIAN_POINT ( 'NONE',  ( -1.364683531250010295, 8.442708333674730170, 0.7879004041258445001 ) ) ;
#171392=CARTESIAN_POINT ( 'NONE',  ( -0.6823417656250039265, 13.81770833367473195, -1.181850606188755259 ) ) ;
#171532=CARTESIAN_POINT ( 'NONE',  ( 1.364683531250000303, 8.505208333674730170, -0.7879004041258355073 ) ) ;
#171540=CARTESIAN_POINT ( 'NONE',  ( 3.834746474454188013E-15, 12.34375000068279959, 1.500000000000001554 ) ) ;
#171553=AXIS2_PLACEMENT_3D ( 'NONE', #9383, #57072, #108023 ) ;
#171565=EDGE_LOOP ( 'NONE', ( #81874, #45460 ) ) ;
#171593=CARTESIAN_POINT ( 'NONE',  ( 0.6823417656249934904, 12.50520833367473017, 1.181850606188764807 ) ) ;
#171680=CARTESIAN_POINT ( 'NONE',  ( -2.788906526875773208E-15, 10.96875000068279427, -1.499999999999998446 ) ) ;
#171719=CARTESIAN_POINT ( 'NONE',  ( -1.286956418854606543, 4.047654341997520611, 0.4592741676706140197 ) ) ;
#171764=CYLINDRICAL_SURFACE ( 'NONE', #193393, 1.500000000000000222 ) ;
#171788=CARTESIAN_POINT ( 'NONE',  ( -1.402160292154681736E-14, 10.42187500034139624, 1.575800808251682339 ) ) ;
#171795=CARTESIAN_POINT ( 'NONE',  ( 1.500000000000001332, 9.375000000000001776, 0.000000000000000000 ) ) ;
#171808=ORIENTED_EDGE ( 'NONE', *, *, #109767, .T. ) ;
#171817=CARTESIAN_POINT ( 'NONE',  ( -0.4019237886466933696, 8.582585450998170273, 1.500000000000005995 ) ) ;
#171847=CARTESIAN_POINT ( 'NONE',  ( -1.402160292154681736E-14, 8.484375000341403350, 1.575800808251682339 ) ) ;
#171859=CARTESIAN_POINT ( 'NONE',  ( -0.4019237886466871523, 12.47991455036742892, -1.499999999999998668 ) ) ;
#172058=CARTESIAN_POINT ( 'NONE',  ( -0.7500000000000006661, 13.70833333333333570, -1.299038105676657340 ) ) ;
#172064=CARTESIAN_POINT ( 'NONE',  ( -8.012344526598182026E-15, 10.79687500034139624, -1.575800808251669460 ) ) ;
#172136=CARTESIAN_POINT ( 'NONE',  ( -8.012344526598182026E-15, 13.04687500034139980, -1.575800808251669460 ) ) ;
#172165=DIRECTION ( 'NONE',  ( 1.000000000000000000, 0.000000000000000000, 0.000000000000000000 ) ) ;
#172179=CARTESIAN_POINT ( 'NONE',  ( -6.009258394948636914E-15, 14.96875000068279427, -1.732050807568875195 ) ) ;
#172188=FACE_OUTER_BOUND ( 'NONE', #197559, .T. ) ;
#172213=CARTESIAN_POINT ( 'NONE',  ( 0.6823417656249934904, 9.942708333674735499, 1.181850606188764807 ) ) ;
#172220=CARTESIAN_POINT ( 'NONE',  ( -1.500000000000015099, 9.010416667349462116, -0.8660254037844309360 ) ) ;
#172305=CARTESIAN_POINT ( 'NONE',  ( -1.154700538379266339, -2.500000000000002220, 2.602085213965210642E-15 ) ) ;
#172359=CARTESIAN_POINT ( 'NONE',  ( 1.364683531249997417, 11.29687500034139802, 2.602085213965210642E-15 ) ) ;
#172363=ORIENTED_EDGE ( 'NONE', *, *, #108076, .F. ) ;
#172371=CARTESIAN_POINT ( 'NONE',  ( -1.500000000000015099, 10.72916666666666607, -0.8660254037844309360 ) ) ;
#172382=CARTESIAN_POINT ( 'NONE',  ( -2.788906526875773208E-15, 9.218750000682799595, -1.499999999999998446 ) ) ;
#172386=CARTESIAN_POINT ( 'NONE',  ( -0.6823417656250003738, 14.65104166700806410, 1.181850606188754593 ) ) ;
#172397=FACE_OUTER_BOUND ( 'NONE', #66269, .T. ) ;
#172429=CARTESIAN_POINT ( 'NONE',  ( -1.500000000000015099, 14.47916666666666785, -0.8660254037844309360 ) ) ;
#172435=CARTESIAN_POINT ( 'NONE',  ( -1.408744241983817425, 4.236591513440624013, -0.5205678189275618761 ) ) ;
#172476=CARTESIAN_POINT ( 'NONE',  ( -8.012344526598182026E-15, 13.79687500034139624, -1.575800808251669460 ) ) ;
#172479=LINE ( 'NONE', #209206, #74016 ) ;
#172525=ORIENTED_EDGE ( 'NONE', *, *, #42099, .F. ) ;
#172574=( BOUNDED_SURFACE ( )  B_SPLINE_SURFACE ( 1, 2, ( 
 ( #88799, #56288, #21608, #139695, #205717, #154858, #72518, #40044, #155926, #190534, #173256, #123516, #106153, #9657, #103979, #172179, #73593, #189480, #41123, #87716, #170022, #157002, #74670, #54155, #140773, #42190, #174325, #120294, #92011, #158069, #153788, #5358, #71440, #55221, #121367, #94143, #159115, #160182, #143980, #47521, #12840, #76785, #29117, #95203, #141846, #26967, #179639, #142907, #78914, #127782, #110436, #125634, #161253, #178574, #191595, #208907, #46442, #44314, #113634, #207851, #126699, #61612, #212103, #60540, #11783, #63740, #75733, #211039, #31259, #146092, #77856, #30181, #192660, #145036, #62665, #128824, #194806, #112561, #96272, #43256, #162322, #13906, #176438, #195883, #79988, #129898, #28050, #59477, #109375, #97333, #163391, #175382, #93073, #45383, #209971, #193737, #10716, #111499, #177505, #1913, #99451, #34435, #2984, #135171, #98382, #134116, #133045, #101577, #64802, #49624, #114695, #166583, #83178, #199046, #100508, #214211, #130948, #65840, #167645, #164445, #201186, #181739, #149261, #180689, #18172, #84259, #33370, #165508, #17100, #116817, #85326, #51778, #150344, #50693, #102653, #196939, #839, #182819, #115749, #66905, #32314, #48579, #67972, #131989, #14965, #197998, #200125, #117895, #213173, #69051, #183888, #52825, #35500, #19245, #151409, #118962, #184940, #16032, #36567, #81062, #147147, #82116, #148209, #125117, #191075, #20314, #120037, #61097, #21365, #174873, #9142, #206265, #4047, #42742, #60027, #70117, #169776, #142384, #140244, #143455, #86400, #8064, #157546, #93622, #90405, #41671, #159664, #168710, #92562, #127256, #27523, #173807, #126178, #74150, #108847, #26453, #158602, #10201, #76276, #208393, #136228, #192142, #43806, #156475, #77343, #109919, #57890, #53901, #44874, #193227, #37647, #202250, #175930, #11265, #152467, #209453, #186011, #75216, #124053, #103725, #190019, #107782, #25386, #91485, #141327, #207340, #58962, #115245, #110979, #29675, #98939, #79478, #81608, #94692, #31810, #114189, #180188, #62171, #161812, #194293, #210537, #176985, #144528, #211592, #181235, #14456, #196434, #130446, #113118, #212659, #147692, #95759, #179124, #198536, #28603, #213710, #160733, #65333, #145596, #13402, #78407, #129391, #96827, #30746, #164993, #148750, #16584, #80547, #48078, #63228, #97886, #128330, #12327, #162876, #195370, #112057, #64301, #146644, #163947, #47002, #131480, #45938, #15522, #197484, #49127, #32863, #82666, #320, #66390, #132538, #178057, #34976, #166061, #67455, #83732, #102126, #101047, #4588, #85877, #54450, #53373, #133601, #202801, #199606, #120593, #1394, #118442, #99995, #117374, #37119, #154085, #70662, #153012, #151954, #88014, #103198, #200663, #3524, #136772, #69598, #38198, #68532, #168195, #119508, #186570, #134660, #19794, #185494, #135706, #201732, #169260, #149824, #33920, #51249, #104271, #116303, #170316 ),
 ( #183371, #20846, #86945, #52312, #167137, #21904, #182293, #5653, #71733, #137847, #84806, #50182, #184429, #17648, #18722, #150895, #2456, #36046, #6737, #22983, #41423, #188710, #158360, #25134, #208146, #207083, #72816, #142132, #138918, #59776, #155156, #57652, #39261, #56588, #190829, #93373, #9953, #92319, #91236, #27266, #42488, #139995, #157296, #76029, #8886, #191892, #7809, #107531, #58714, #125934, #73902, #173562, #124863, #74965, #141075, #108597, #89102, #187634, #204937, #43554, #55512, #109675, #122748, #174625, #40346, #175677, #159409, #121667, #26201, #11009, #77086, #106452, #203868, #105355, #171392, #172476, #24063, #90166, #156232, #206016, #123811, #189772, #61917, #131240, #111800, #113935, #127005, #64044, #146388, #212402, #94440, #194033, #12086, #28345, #209203, #176731, #29422, #147436, #46751, #14197, #162621, #145343, #30490, #179931, #128077, #211344, #16326, #60843, #31555, #192963, #97630, #177806, #45684, #110731, #161561, #129138, #62969, #197227, #180983, #48867, #112863, #80290, #95513, #130189, #160479, #143213, #195114, #13149, #144284, #96574, #178878, #196182, #79226, #163687, #44616, #47824, #15269, #81356, #213460, #65084, #114983, #32604, #98679, #164735, #78153, #210277, #99735, #116044, #134406, #67202, #36852, #118183, #86681, #85612, #165807, #20595, #17391, #152748, #33661, #150636, #132274, #149555, #69336, #186301, #102936, #185229, #184171, #120325, #135447, #18468, #35791, #168996, #101867, #70399, #100792, #200410, #151700, #4330, #166877, #52056, #3269, #167935, #19535, #201469, #182032, #66130, #83474, #136517, #148498, #202536, #1140, #53112, #133339, #54185, #37937, #66, #119245, #104011, #170056, #199343, #82409, #198282, #49923, #50990, #117111, #183113, #34721, #84546, #2197, #68274, #154894, #9691, #204672, #206819, #5395, #157034, #24868, #90972, #187375, #72552, #105090, #121403, #87748, #55256, #122481, #25937, #139729, #107266, #41157, #23802, #123547, #58453, #6475, #89907, #109411, #153824, #124608, #71474, #190566, #56321, #138650, #203603, #40076, #7545, #155959, #75768, #59508, #141876, #205752, #173286, #188442, #88836, #106188, #158102, #21641, #8621, #125665, #92045, #73630, #42222, #172213, #74703, #140807, #108339, #174359, #189512, #207885, #137586, #191627, #43290, #57383, #39006, #171128, #22722, #60575, #48612, #64836, #44348, #208940, #146125, #13939, #61649, #175416, #93106, #128860, #31292, #163425, #142940, #145073, #144014, #45417, #47558, #80022, #196973, #162360, #111533, #194842, #15002, #81093, #110470, #212138, #78951, #113668, #10749, #210007, #126734, #112598, #29151, #211076, #46475, #160216, #76820, #11817, #179672, #176471, #147181, #127816, #95240, #192694, #178610, #30220, #193771, #177540, #161289, #62699, #97367, #63774, #96304, #129932, #27000, #28081, #12875, #195921, #213207, #130982, #94177, #77893 ) ),
 .UNSPECIFIED., .F., .F., .F. ) 
 B_SPLINE_SURFACE_WITH_KNOTS ( ( 2, 2 ),
 ( 3, 2, 2, 2, 2, 2, 2, 2, 2, 2, 2, 2, 2, 2, 2, 2, 2, 2, 2, 2, 2, 2, 2, 2, 2, 2, 2, 2, 2, 2, 2, 2, 2, 2, 2, 2, 2, 2, 2, 2, 2, 2, 2, 2, 2, 2, 2, 2, 2, 2, 2, 2, 2, 2, 2, 2, 2, 2, 2, 2, 2, 2, 2, 2, 2, 2, 2, 2, 2, 2, 2, 2, 2, 2, 2, 2, 2, 2, 2, 2, 2, 2, 2, 2, 2, 2, 2, 2, 2, 2, 2, 2, 2, 2, 2, 2, 2, 2, 2, 2, 2, 2, 2, 2, 2, 2, 2, 2, 2, 2, 2, 2, 2, 2, 2, 2, 2, 2, 2, 2, 2, 2, 2, 2, 2, 2, 2, 2, 2, 2, 2, 2, 2, 2, 2, 2, 2, 2, 2, 2, 2, 2, 2, 2, 2, 2, 2, 2, 2, 2, 2, 2, 2, 2, 2, 2, 2, 2, 2, 2, 2, 2, 2, 2, 2, 2, 2, 2, 3 ),
 ( 0.000000000000000000, 1.000000000000000000 ),
 ( 0.000000000000000000, 0.005952380952380952051, 0.01190476190476190410, 0.01785714285714285615, 0.02380952380952380820, 0.02976190476190476025, 0.03571428571428571230, 0.04166666666666666435, 0.04761904761904761640, 0.05357142857142856845, 0.05952380952380952051, 0.06547619047619047949, 0.07142857142857142461, 0.07738095238095238360, 0.08333333333333332871, 0.08928571428571428770, 0.09523809523809523281, 0.1011904761904761918, 0.1071428571428571369, 0.1130952380952380959, 0.1190476190476190410, 0.1250000000000000000, 0.1309523809523809590, 0.1369047619047619180, 0.1428571428571428492, 0.1488095238095238082, 0.1547619047619047672, 0.1607142857142857262, 0.1666666666666666574, 0.1726190476190476164, 0.1785714285714285754, 0.1845238095238095344, 0.1904761904761904656, 0.1964285714285714246, 0.2023809523809523836, 0.2083333333333333426, 0.2142857142857142738, 0.2202380952380952328, 0.2261904761904761918, 0.2321428571428571508, 0.2380952380952380820, 0.2440476190476190410, 0.2500000000000000000, 0.2559523809523809312, 0.2619047619047619180, 0.2678571428571428492, 0.2738095238095238360, 0.2797619047619047672, 0.2857142857142856984, 0.2916666666666666852, 0.2976190476190476164, 0.3035714285714285476, 0.3095238095238095344, 0.3154761904761904656, 0.3214285714285714524, 0.3273809523809523836, 0.3333333333333333148, 0.3392857142857143016, 0.3452380952380952328, 0.3511904761904761640, 0.3571428571428571508, 0.3630952380952380820, 0.3690476190476190688, 0.3750000000000000000, 0.3809523809523809312, 0.3869047619047619180, 0.3928571428571428492, 0.3988095238095238360, 0.4047619047619047672, 0.4107142857142856984, 0.4166666666666666852, 0.4226190476190476164, 0.4285714285714285476, 0.4345238095238095344, 0.4404761904761904656, 0.4464285714285714524, 0.4523809523809523836, 0.4583333333333333148, 0.4642857142857143016, 0.4702380952380952328, 0.4761904761904761640, 0.4821428571428571508, 0.4880952380952380820, 0.4940476190476190688, 0.5000000000000000000, 0.5059523809523809312, 0.5119047619047618625, 0.5178571428571429047, 0.5238095238095238360, 0.5297619047619047672, 0.5357142857142856984, 0.5416666666666666297, 0.5476190476190476719, 0.5535714285714286031, 0.5595238095238095344, 0.5654761904761904656, 0.5714285714285713969, 0.5773809523809523281, 0.5833333333333333703, 0.5892857142857143016, 0.5952380952380952328, 0.6011904761904761640, 0.6071428571428570953, 0.6130952380952381375, 0.6190476190476190688, 0.6250000000000000000, 0.6309523809523809312, 0.6369047619047618625, 0.6428571428571429047, 0.6488095238095238360, 0.6547619047619047672, 0.6607142857142856984, 0.6666666666666666297, 0.6726190476190476719, 0.6785714285714286031, 0.6845238095238095344, 0.6904761904761904656, 0.6964285714285713969, 0.7023809523809523281, 0.7083333333333333703, 0.7142857142857143016, 0.7202380952380952328, 0.7261904761904761640, 0.7321428571428570953, 0.7380952380952381375, 0.7440476190476190688, 0.7500000000000000000, 0.7559523809523809312, 0.7619047619047618625, 0.7678571428571429047, 0.7738095238095238360, 0.7797619047619047672, 0.7857142857142856984, 0.7916666666666666297, 0.7976190476190476719, 0.8035714285714286031, 0.8095238095238095344, 0.8154761904761904656, 0.8214285714285713969, 0.8273809523809523281, 0.8333333333333333703, 0.8392857142857143016, 0.8452380952380952328, 0.8511904761904761640, 0.8571428571428570953, 0.8630952380952381375, 0.8690476190476190688, 0.8750000000000000000, 0.8809523809523809312, 0.8869047619047618625, 0.8928571428571429047, 0.8988095238095238360, 0.9047619047619047672, 0.9107142857142856984, 0.9166666666666666297, 0.9226190476190476719, 0.9285714285714286031, 0.9345238095238095344, 0.9404761904761904656, 0.9464285714285713969, 0.9523809523809523281, 0.9583333333333333703, 0.9642857142857143016, 0.9702380952380952328, 0.9761904761904761640, 0.9821428571428570953, 0.9880952380952381375, 0.9940476190476190688, 1.000000000000000000 ),
 .UNSPECIFIED. ) 
 GEOMETRIC_REPRESENTATION_ITEM ( )  RATIONAL_B_SPLINE_SURFACE ( (
 ( 1.000000000000000000, 0.8660254037844387076, 1.000000000000000000, 0.8660254037844387076, 1.000000000000000000, 0.8660254037844387076, 1.000000000000000000, 0.8660254037844387076, 1.000000000000000000, 0.8660254037844387076, 1.000000000000000000, 0.8660254037844387076, 1.000000000000000000, 0.8660254037844387076, 1.000000000000000000, 0.8660254037844387076, 1.000000000000000000, 0.8660254037844387076, 1.000000000000000000, 0.8660254037844387076, 1.000000000000000000, 0.8660254037844387076, 1.000000000000000000, 0.8660254037844387076, 1.000000000000000000, 0.8660254037844387076, 1.000000000000000000, 0.8660254037844387076, 1.000000000000000000, 0.8660254037844387076, 1.000000000000000000, 0.8660254037844387076, 1.000000000000000000, 0.8660254037844387076, 1.000000000000000000, 0.8660254037844387076, 1.000000000000000000, 0.8660254037844387076, 1.000000000000000000, 0.8660254037844387076, 1.000000000000000000, 0.8660254037844387076, 1.000000000000000000, 0.8660254037844387076, 1.000000000000000000, 0.8660254037844387076, 1.000000000000000000, 0.8660254037844387076, 1.000000000000000000, 0.8660254037844387076, 1.000000000000000000, 0.8660254037844387076, 1.000000000000000000, 0.8660254037844387076, 1.000000000000000000, 0.8660254037844387076, 1.000000000000000000, 0.8660254037844387076, 1.000000000000000000, 0.8660254037844387076, 1.000000000000000000, 0.8660254037844387076, 1.000000000000000000, 0.8660254037844387076, 1.000000000000000000, 0.8660254037844387076, 1.000000000000000000, 0.8660254037844387076, 1.000000000000000000, 0.8660254037844387076, 1.000000000000000000, 0.8660254037844387076, 1.000000000000000000, 0.8660254037844387076, 1.000000000000000000, 0.8660254037844387076, 1.000000000000000000, 0.8660254037844387076, 1.000000000000000000, 0.8660254037844387076, 1.000000000000000000, 0.8660254037844387076, 1.000000000000000000, 0.8660254037844387076, 1.000000000000000000, 0.8660254037844387076, 1.000000000000000000, 0.8660254037844387076, 1.000000000000000000, 0.8660254037844387076, 1.000000000000000000, 0.8660254037844387076, 1.000000000000000000, 0.8660254037844387076, 1.000000000000000000, 0.8660254037844387076, 1.000000000000000000, 0.8660254037844387076, 1.000000000000000000, 0.8660254037844387076, 1.000000000000000000, 0.8660254037844387076, 1.000000000000000000, 0.8660254037844387076, 1.000000000000000000, 0.8660254037844387076, 1.000000000000000000, 0.8660254037844387076, 1.000000000000000000, 0.8660254037844387076, 1.000000000000000000, 0.8660254037844387076, 1.000000000000000000, 0.8660254037844387076, 1.000000000000000000, 0.8660254037844387076, 1.000000000000000000, 0.8660254037844387076, 1.000000000000000000, 0.8660254037844387076, 1.000000000000000000, 0.8660254037844387076, 1.000000000000000000, 0.8660254037844387076, 1.000000000000000000, 0.8660254037844387076, 1.000000000000000000, 0.8660254037844387076, 1.000000000000000000, 0.8660254037844387076, 1.000000000000000000, 0.8660254037844387076, 1.000000000000000000, 0.8660254037844387076, 1.000000000000000000, 0.8660254037844387076, 1.000000000000000000, 0.8660254037844387076, 1.000000000000000000, 0.8660254037844387076, 1.000000000000000000, 0.8660254037844387076, 1.000000000000000000, 0.8660254037844387076, 1.000000000000000000, 0.8660254037844387076, 1.000000000000000000, 0.8660254037844387076, 1.000000000000000000, 0.8660254037844387076, 1.000000000000000000, 0.8660254037844387076, 1.000000000000000000, 0.8660254037844387076, 1.000000000000000000, 0.8660254037844387076, 1.000000000000000000, 0.8660254037844387076, 1.000000000000000000, 0.8660254037844387076, 1.000000000000000000, 0.8660254037844387076, 1.000000000000000000, 0.8660254037844387076, 1.000000000000000000, 0.8660254037844387076, 1.000000000000000000, 0.8660254037844387076, 1.000000000000000000, 0.8660254037844387076, 1.000000000000000000, 0.8660254037844387076, 1.000000000000000000, 0.8660254037844387076, 1.000000000000000000, 0.8660254037844387076, 1.000000000000000000, 0.8660254037844387076, 1.000000000000000000, 0.8660254037844387076, 1.000000000000000000, 0.8660254037844387076, 1.000000000000000000, 0.8660254037844387076, 1.000000000000000000, 0.8660254037844387076, 1.000000000000000000, 0.8660254037844387076, 1.000000000000000000, 0.8660254037844387076, 1.000000000000000000, 0.8660254037844387076, 1.000000000000000000, 0.8660254037844387076, 1.000000000000000000, 0.8660254037844387076, 1.000000000000000000, 0.8660254037844387076, 1.000000000000000000, 0.8660254037844387076, 1.000000000000000000, 0.8660254037844387076, 1.000000000000000000, 0.8660254037844387076, 1.000000000000000000, 0.8660254037844387076, 1.000000000000000000, 0.8660254037844387076, 1.000000000000000000, 0.8660254037844387076, 1.000000000000000000, 0.8660254037844387076, 1.000000000000000000, 0.8660254037844387076, 1.000000000000000000, 0.8660254037844387076, 1.000000000000000000, 0.8660254037844387076, 1.000000000000000000, 0.8660254037844387076, 1.000000000000000000, 0.8660254037844387076, 1.000000000000000000, 0.8660254037844387076, 1.000000000000000000, 0.8660254037844387076, 1.000000000000000000, 0.8660254037844387076, 1.000000000000000000, 0.8660254037844387076, 1.000000000000000000, 0.8660254037844387076, 1.000000000000000000, 0.8660254037844387076, 1.000000000000000000, 0.8660254037844387076, 1.000000000000000000, 0.8660254037844387076, 1.000000000000000000, 0.8660254037844387076, 1.000000000000000000, 0.8660254037844387076, 1.000000000000000000, 0.8660254037844387076, 1.000000000000000000, 0.8660254037844387076, 1.000000000000000000, 0.8660254037844387076, 1.000000000000000000, 0.8660254037844387076, 1.000000000000000000, 0.8660254037844387076, 1.000000000000000000, 0.8660254037844387076, 1.000000000000000000, 0.8660254037844387076, 1.000000000000000000, 0.8660254037844387076, 1.000000000000000000, 0.8660254037844387076, 1.000000000000000000, 0.8660254037844387076, 1.000000000000000000, 0.8660254037844387076, 1.000000000000000000, 0.8660254037844387076, 1.000000000000000000, 0.8660254037844387076, 1.000000000000000000, 0.8660254037844387076, 1.000000000000000000, 0.8660254037844387076, 1.000000000000000000, 0.8660254037844387076, 1.000000000000000000, 0.8660254037844387076, 1.000000000000000000, 0.8660254037844387076, 1.000000000000000000, 0.8660254037844387076, 1.000000000000000000, 0.8660254037844387076, 1.000000000000000000, 0.8660254037844387076, 1.000000000000000000, 0.8660254037844387076, 1.000000000000000000, 0.8660254037844387076, 1.000000000000000000, 0.8660254037844387076, 1.000000000000000000, 0.8660254037844387076, 1.000000000000000000, 0.8660254037844387076, 1.000000000000000000, 0.8660254037844387076, 1.000000000000000000, 0.8660254037844387076, 1.000000000000000000, 0.8660254037844387076, 1.000000000000000000, 0.8660254037844387076, 1.000000000000000000, 0.8660254037844387076, 1.000000000000000000, 0.8660254037844387076, 1.000000000000000000, 0.8660254037844387076, 1.000000000000000000, 0.8660254037844387076, 1.000000000000000000, 0.8660254037844387076, 1.000000000000000000, 0.8660254037844387076, 1.000000000000000000, 0.8660254037844387076, 1.000000000000000000, 0.8660254037844387076, 1.000000000000000000, 0.8660254037844387076, 1.000000000000000000, 0.8660254037844387076, 1.000000000000000000, 0.8660254037844387076, 1.000000000000000000, 0.8660254037844387076, 1.000000000000000000, 0.8660254037844387076, 1.000000000000000000, 0.8660254037844387076, 1.000000000000000000, 0.8660254037844387076, 1.000000000000000000, 0.8660254037844387076, 1.000000000000000000, 0.8660254037844387076, 1.000000000000000000),
 ( 1.000000000000000000, 0.8660254037844387076, 1.000000000000000000, 0.8660254037844387076, 1.000000000000000000, 0.8660254037844387076, 1.000000000000000000, 0.8660254037844387076, 1.000000000000000000, 0.8660254037844387076, 1.000000000000000000, 0.8660254037844387076, 1.000000000000000000, 0.8660254037844387076, 1.000000000000000000, 0.8660254037844387076, 1.000000000000000000, 0.8660254037844387076, 1.000000000000000000, 0.8660254037844387076, 1.000000000000000000, 0.8660254037844387076, 1.000000000000000000, 0.8660254037844387076, 1.000000000000000000, 0.8660254037844387076, 1.000000000000000000, 0.8660254037844387076, 1.000000000000000000, 0.8660254037844387076, 1.000000000000000000, 0.8660254037844387076, 1.000000000000000000, 0.8660254037844387076, 1.000000000000000000, 0.8660254037844387076, 1.000000000000000000, 0.8660254037844387076, 1.000000000000000000, 0.8660254037844387076, 1.000000000000000000, 0.8660254037844387076, 1.000000000000000000, 0.8660254037844387076, 1.000000000000000000, 0.8660254037844387076, 1.000000000000000000, 0.8660254037844387076, 1.000000000000000000, 0.8660254037844387076, 1.000000000000000000, 0.8660254037844387076, 1.000000000000000000, 0.8660254037844387076, 1.000000000000000000, 0.8660254037844387076, 1.000000000000000000, 0.8660254037844387076, 1.000000000000000000, 0.8660254037844387076, 1.000000000000000000, 0.8660254037844387076, 1.000000000000000000, 0.8660254037844387076, 1.000000000000000000, 0.8660254037844387076, 1.000000000000000000, 0.8660254037844387076, 1.000000000000000000, 0.8660254037844387076, 1.000000000000000000, 0.8660254037844387076, 1.000000000000000000, 0.8660254037844387076, 1.000000000000000000, 0.8660254037844387076, 1.000000000000000000, 0.8660254037844387076, 1.000000000000000000, 0.8660254037844387076, 1.000000000000000000, 0.8660254037844387076, 1.000000000000000000, 0.8660254037844387076, 1.000000000000000000, 0.8660254037844387076, 1.000000000000000000, 0.8660254037844387076, 1.000000000000000000, 0.8660254037844387076, 1.000000000000000000, 0.8660254037844387076, 1.000000000000000000, 0.8660254037844387076, 1.000000000000000000, 0.8660254037844387076, 1.000000000000000000, 0.8660254037844387076, 1.000000000000000000, 0.8660254037844387076, 1.000000000000000000, 0.8660254037844387076, 1.000000000000000000, 0.8660254037844387076, 1.000000000000000000, 0.8660254037844387076, 1.000000000000000000, 0.8660254037844387076, 1.000000000000000000, 0.8660254037844387076, 1.000000000000000000, 0.8660254037844387076, 1.000000000000000000, 0.8660254037844387076, 1.000000000000000000, 0.8660254037844387076, 1.000000000000000000, 0.8660254037844387076, 1.000000000000000000, 0.8660254037844387076, 1.000000000000000000, 0.8660254037844387076, 1.000000000000000000, 0.8660254037844387076, 1.000000000000000000, 0.8660254037844387076, 1.000000000000000000, 0.8660254037844387076, 1.000000000000000000, 0.8660254037844387076, 1.000000000000000000, 0.8660254037844387076, 1.000000000000000000, 0.8660254037844387076, 1.000000000000000000, 0.8660254037844387076, 1.000000000000000000, 0.8660254037844387076, 1.000000000000000000, 0.8660254037844387076, 1.000000000000000000, 0.8660254037844387076, 1.000000000000000000, 0.8660254037844387076, 1.000000000000000000, 0.8660254037844387076, 1.000000000000000000, 0.8660254037844387076, 1.000000000000000000, 0.8660254037844387076, 1.000000000000000000, 0.8660254037844387076, 1.000000000000000000, 0.8660254037844387076, 1.000000000000000000, 0.8660254037844387076, 1.000000000000000000, 0.8660254037844387076, 1.000000000000000000, 0.8660254037844387076, 1.000000000000000000, 0.8660254037844387076, 1.000000000000000000, 0.8660254037844387076, 1.000000000000000000, 0.8660254037844387076, 1.000000000000000000, 0.8660254037844387076, 1.000000000000000000, 0.8660254037844387076, 1.000000000000000000, 0.8660254037844387076, 1.000000000000000000, 0.8660254037844387076, 1.000000000000000000, 0.8660254037844387076, 1.000000000000000000, 0.8660254037844387076, 1.000000000000000000, 0.8660254037844387076, 1.000000000000000000, 0.8660254037844387076, 1.000000000000000000, 0.8660254037844387076, 1.000000000000000000, 0.8660254037844387076, 1.000000000000000000, 0.8660254037844387076, 1.000000000000000000, 0.8660254037844387076, 1.000000000000000000, 0.8660254037844387076, 1.000000000000000000, 0.8660254037844387076, 1.000000000000000000, 0.8660254037844387076, 1.000000000000000000, 0.8660254037844387076, 1.000000000000000000, 0.8660254037844387076, 1.000000000000000000, 0.8660254037844387076, 1.000000000000000000, 0.8660254037844387076, 1.000000000000000000, 0.8660254037844387076, 1.000000000000000000, 0.8660254037844387076, 1.000000000000000000, 0.8660254037844387076, 1.000000000000000000, 0.8660254037844387076, 1.000000000000000000, 0.8660254037844387076, 1.000000000000000000, 0.8660254037844387076, 1.000000000000000000, 0.8660254037844387076, 1.000000000000000000, 0.8660254037844387076, 1.000000000000000000, 0.8660254037844387076, 1.000000000000000000, 0.8660254037844387076, 1.000000000000000000, 0.8660254037844387076, 1.000000000000000000, 0.8660254037844387076, 1.000000000000000000, 0.8660254037844387076, 1.000000000000000000, 0.8660254037844387076, 1.000000000000000000, 0.8660254037844387076, 1.000000000000000000, 0.8660254037844387076, 1.000000000000000000, 0.8660254037844387076, 1.000000000000000000, 0.8660254037844387076, 1.000000000000000000, 0.8660254037844387076, 1.000000000000000000, 0.8660254037844387076, 1.000000000000000000, 0.8660254037844387076, 1.000000000000000000, 0.8660254037844387076, 1.000000000000000000, 0.8660254037844387076, 1.000000000000000000, 0.8660254037844387076, 1.000000000000000000, 0.8660254037844387076, 1.000000000000000000, 0.8660254037844387076, 1.000000000000000000, 0.8660254037844387076, 1.000000000000000000, 0.8660254037844387076, 1.000000000000000000, 0.8660254037844387076, 1.000000000000000000, 0.8660254037844387076, 1.000000000000000000, 0.8660254037844387076, 1.000000000000000000, 0.8660254037844387076, 1.000000000000000000, 0.8660254037844387076, 1.000000000000000000, 0.8660254037844387076, 1.000000000000000000, 0.8660254037844387076, 1.000000000000000000, 0.8660254037844387076, 1.000000000000000000, 0.8660254037844387076, 1.000000000000000000, 0.8660254037844387076, 1.000000000000000000, 0.8660254037844387076, 1.000000000000000000, 0.8660254037844387076, 1.000000000000000000, 0.8660254037844387076, 1.000000000000000000, 0.8660254037844387076, 1.000000000000000000, 0.8660254037844387076, 1.000000000000000000, 0.8660254037844387076, 1.000000000000000000, 0.8660254037844387076, 1.000000000000000000, 0.8660254037844387076, 1.000000000000000000, 0.8660254037844387076, 1.000000000000000000, 0.8660254037844387076, 1.000000000000000000, 0.8660254037844387076, 1.000000000000000000, 0.8660254037844387076, 1.000000000000000000, 0.8660254037844387076, 1.000000000000000000, 0.8660254037844387076, 1.000000000000000000, 0.8660254037844387076, 1.000000000000000000, 0.8660254037844387076, 1.000000000000000000, 0.8660254037844387076, 1.000000000000000000, 0.8660254037844387076, 1.000000000000000000, 0.8660254037844387076, 1.000000000000000000, 0.8660254037844387076, 1.000000000000000000, 0.8660254037844387076, 1.000000000000000000, 0.8660254037844387076, 1.000000000000000000, 0.8660254037844387076, 1.000000000000000000, 0.8660254037844387076, 1.000000000000000000, 0.8660254037844387076, 1.000000000000000000, 0.8660254037844387076, 1.000000000000000000, 0.8660254037844387076, 1.000000000000000000, 0.8660254037844387076, 1.000000000000000000) ) ) 
 REPRESENTATION_ITEM ( '' )  SURFACE ( )  );
#172620=CARTESIAN_POINT ( 'NONE',  ( -0.6823417656250039265, 15.13020833367473372, -1.181850606188755259 ) ) ;
#172628=( BOUNDED_CURVE ( )  B_SPLINE_CURVE ( 2, ( #39166, #22882, #88998, #204831, #120493, #172371, #56483, #23961, #20751 ),
 .UNSPECIFIED., .F., .T. ) 
 B_SPLINE_CURVE_WITH_KNOTS ( ( 3, 2, 2, 2, 3 ),
 ( 0.6696428571428570953, 0.6726190476190476719, 0.6785714285714286031, 0.6845238095238095344, 0.6875000000000000000 ),
 .UNSPECIFIED. ) 
 CURVE ( )  GEOMETRIC_REPRESENTATION_ITEM ( )  RATIONAL_B_SPLINE_CURVE ( ( 0.9330127018922194093, 0.9330127018922180770, 1.000000000000000000, 0.8660254037844387076, 1.000000000000000000, 0.8660254037844387076, 1.000000000000000000, 0.9330127018922194093, 0.9330127018922194093 ) ) 
 REPRESENTATION_ITEM ( '' )  );
#172644=EDGE_CURVE ( 'NONE', #124391, #94456, #20130, .T. ) ;
#172682=CARTESIAN_POINT ( 'NONE',  ( 1.364683531250000303, 12.56770833367473372, -0.7879004041258355073 ) ) ;
#172712=CARTESIAN_POINT ( 'NONE',  ( 1.286813488861806354, 4.047007041464545374, -0.4595522011843541366 ) ) ;
#172733=EDGE_CURVE ( 'NONE', #188147, #151327, #94971, .T. ) ;
#172756=CARTESIAN_POINT ( 'NONE',  ( -1.115562610750309283E-14, 11.09375000068279427, 1.500000000000001554 ) ) ;
#172795=EDGE_CURVE ( 'NONE', #156928, #60352, #15533, .T. ) ;
#172875=CARTESIAN_POINT ( 'NONE',  ( -1.402160292154681736E-14, 10.67187500034139624, 1.575800808251682339 ) ) ;
#172901=CARTESIAN_POINT ( 'NONE',  ( -1.500000000000015099, 8.510416667349460340, -0.8660254037844309360 ) ) ;
#172951=( BOUNDED_CURVE ( )  B_SPLINE_CURVE ( 2, ( #25053, #59688, #42409, #125851, #72735 ),
 .UNSPECIFIED., .F., .T. ) 
 B_SPLINE_CURVE_WITH_KNOTS ( ( 3, 2, 3 ),
 ( 0.9910714285714286031, 0.9940476190476190688, 1.000000000000000000 ),
 .UNSPECIFIED. ) 
 CURVE ( )  GEOMETRIC_REPRESENTATION_ITEM ( )  RATIONAL_B_SPLINE_CURVE ( ( 0.9330127018922194093, 0.9330127018922194093, 1.000000000000000000, 0.8660254037844387076, 1.000000000000000000 ) ) 
 REPRESENTATION_ITEM ( '' )  );
#172954=CARTESIAN_POINT ( 'NONE',  ( 0.7500000000000006661, 13.08333333333333570, 1.299038105676657340 ) ) ;
#172970=FACE_OUTER_BOUND ( 'NONE', #25993, .T. ) ;
#172979=AXIS2_PLACEMENT_3D ( 'NONE', #151274, #1784, #136091 ) ;
#173052=EDGE_CURVE ( 'NONE', #35502, #210699, #54461, .T. ) ;
#173136=CARTESIAN_POINT ( 'NONE',  ( 1.499999999999993117, 12.60416666666666785, 0.8660254037844409281 ) ) ;
#173142=CARTESIAN_POINT ( 'NONE',  ( -1.364683531250014514, 10.08854166700806410, -0.7879004041258335089 ) ) ;
#173188=CARTESIAN_POINT ( 'NONE',  ( -1.364683531250010740, 12.44270833367473195, 0.7879004041258445001 ) ) ;
#173196=EDGE_CURVE ( 'NONE', #155317, #171094, #6749, .T. ) ;
#173201=CYLINDRICAL_SURFACE ( 'NONE', #126558, 1.500000000000000222 ) ;
#173216=CARTESIAN_POINT ( 'NONE',  ( 0.6823417656249934904, 12.94270833367473017, 1.181850606188764807 ) ) ;
#173242=ADVANCED_FACE ( 'NONE', ( #24074 ), #133970, .T. ) ;
#173256=CARTESIAN_POINT ( 'NONE',  ( -0.7500000000000179856, 15.07291666734946567, 1.299038105676658228 ) ) ;
#173264=CYLINDRICAL_SURFACE ( 'NONE', #92484, 1.500000000000000222 ) ;
#173286=CARTESIAN_POINT ( 'NONE',  ( -1.402160292154681736E-14, 10.17187500034139447, 1.575800808251682339 ) ) ;
#173308=VERTEX_POINT ( 'NONE', #43565 ) ;
#173366=LINE ( 'NONE', #5477, #185310 ) ;
#173428=EDGE_LOOP ( 'NONE', ( #72326, #129167 ) ) ;
#173442=CARTESIAN_POINT ( 'NONE',  ( -1.402160292154681736E-14, 9.984375000341401574, 1.575800808251682339 ) ) ;
#173450=PLANE ( 'NONE',  #86125 ) ;
#173462=CARTESIAN_POINT ( 'NONE',  ( 0.4841688312534724870, 3.595529751363280457, -0.4351271339793956749 ) ) ;
#173468=CARTESIAN_POINT ( 'NONE',  ( 0.6823417656249969321, 14.27604166700806232, -1.181850606188757036 ) ) ;
#173514=CIRCLE ( 'NONE', #14370, 2.000000000000000000 ) ;
#173515=CARTESIAN_POINT ( 'NONE',  ( 1.499999999999997113, 14.89583333333333570, -0.8660254037844378194 ) ) ;
#173562=CARTESIAN_POINT ( 'NONE',  ( -8.012344526598182026E-15, 14.29687500034139802, -1.575800808251669460 ) ) ;
#173576=CARTESIAN_POINT ( 'NONE',  ( -1.286813488861816790, 3.652992958535466794, -0.4595522011843584109 ) ) ;
#173596=SURFACE_STYLE_USAGE ( .BOTH. , #190860 ) ;
#173657=VECTOR ( 'NONE', #107542, 1000.000000000000000 ) ;
#173705=CARTESIAN_POINT ( 'NONE',  ( -1.364683531250014514, 13.15104166700806410, -0.7879004041258335089 ) ) ;
#173767=CARTESIAN_POINT ( 'NONE',  ( 1.364683531249996529, 12.02604166700806765, 0.7879004041258405033 ) ) ;
#173807=CARTESIAN_POINT ( 'NONE',  ( -1.500000000000001110, 11.30208333401612997, 0.8660254037844419273 ) ) ;
#173881=EDGE_CURVE ( 'NONE', #122713, #67094, #155807, .T. ) ;
#173889=CARTESIAN_POINT ( 'NONE',  ( -1.396038594575822467, 4.344678208267337638, 0.1345620919992577547 ) ) ;
#173911=VECTOR ( 'NONE', #70839, 1000.000000000000000 ) ;
#173935=CARTESIAN_POINT ( 'NONE',  ( 0.4019237886466816012, 8.957585450998170273, -1.499999999999998668 ) ) ;
#173954=CARTESIAN_POINT ( 'NONE',  ( -0.6823417656250039265, 10.31770833367473550, -1.181850606188755259 ) ) ;
#173961=CARTESIAN_POINT ( 'NONE',  ( 1.499999999999997113, 8.645833333333337478, -0.8660254037844378194 ) ) ;
#173984=CARTESIAN_POINT ( 'NONE',  ( -2.788906526875773208E-15, 8.468750000682796042, -1.499999999999998446 ) ) ;
#174001=ORIENTED_EDGE ( 'NONE', *, *, #207616, .T. ) ;
#174013=CARTESIAN_POINT ( 'NONE',  ( 0.5773502691896192918, -2.500000000000002220, 1.000000000000004441 ) ) ;
#174057=AXIS2_PLACEMENT_3D ( 'NONE', #49343, #197701, #79697 ) ;
#174144=EDGE_CURVE ( 'NONE', #75675, #170253, #184755, .T. ) ;
#174214=CARTESIAN_POINT ( 'NONE',  ( 1.500000000000001332, 12.12499999999999645, 0.000000000000000000 ) ) ;
#174219=CARTESIAN_POINT ( 'NONE',  ( 1.364683531250000303, 11.25520833367473550, -0.7879004041258355073 ) ) ;
#174237=CARTESIAN_POINT ( 'NONE',  ( 1.836970198721030181E-16, 13.49999999999999822, 1.500000000000000222 ) ) ;
#174260=CARTESIAN_POINT ( 'NONE',  ( 0.6823417656249934904, 12.25520833367473017, 1.181850606188764807 ) ) ;
#174325=CARTESIAN_POINT ( 'NONE',  ( -0.7500000000000006661, 14.73958333401613530, -1.299038105676657340 ) ) ;
#174359=CARTESIAN_POINT ( 'NONE',  ( -1.364683531250000748, 9.859375000341398021, 0.000000000000000000 ) ) ;
#174364=DIRECTION ( 'NONE',  ( -0.000000000000000000, 1.000000000000000000, -0.000000000000000000 ) ) ;
#174465=CARTESIAN_POINT ( 'NONE',  ( -1.396252044512855672, 3.354846891984019752, -0.1338139928737557549 ) ) ;
#174512=CARTESIAN_POINT ( 'NONE',  ( -0.6823417656250003738, 9.463541667008065872, 1.181850606188754593 ) ) ;
#174530=CARTESIAN_POINT ( 'NONE',  ( 0.6386894617478928726, 3.364476098278418092, -0.1366332986426504470 ) ) ;
#174582=CARTESIAN_POINT ( 'NONE',  ( -1.500000000000001110, 14.77083333333333570, 0.8660254037844419273 ) ) ;
#174586=CARTESIAN_POINT ( 'NONE',  ( 0.000000000000000000, 13.49999999999999822, 0.000000000000000000 ) ) ;
#174625=CARTESIAN_POINT ( 'NONE',  ( -8.012344526598182026E-15, 14.04687500034139624, -1.575800808251669460 ) ) ;
#174659=ADVANCED_FACE ( 'NONE', ( #32174 ), #154460, .F. ) ;
#174744=CARTESIAN_POINT ( 'NONE',  ( 1.443845971921564386, 3.571381292232905125, -0.4218533236949457144 ) ) ;
#174769=CARTESIAN_POINT ( 'NONE',  ( 0.6823417656249934904, 14.00520833367473195, 1.181850606188764807 ) ) ;
#174790=CYLINDRICAL_SURFACE ( 'NONE', #207998, 1.500000000000000222 ) ;
#174831=CARTESIAN_POINT ( 'NONE',  ( 0.6823417656249934904, 12.25520833367473017, 1.181850606188764807 ) ) ;
#174873=CARTESIAN_POINT ( 'NONE',  ( -1.500000000000015099, 11.76041666734946922, -0.8660254037844309360 ) ) ;
#174929=CARTESIAN_POINT ( 'NONE',  ( 0.5773502691896192918, -4.295408888568413630, 1.000000000000004441 ) ) ;
#175009=CARTESIAN_POINT ( 'NONE',  ( -0.6823417656250003738, 10.15104166700806587, 1.181850606188754593 ) ) ;
#175040=CARTESIAN_POINT ( 'NONE',  ( -1.500000000000015099, 8.760416667349462116, -0.8660254037844309360 ) ) ;
#175043=AXIS2_PLACEMENT_3D ( 'NONE', #106384, #90098, #156163 ) ;
#175211=CARTESIAN_POINT ( 'NONE',  ( -1.500000000000001110, 9.020833333333330373, 0.8660254037844418162 ) ) ;
#175270=CARTESIAN_POINT ( 'NONE',  ( -0.7500000000000006661, 11.95833333333333393, -1.299038105676657340 ) ) ;
#175275=CARTESIAN_POINT ( 'NONE',  ( -1.364683531250010295, 10.13020833367472839, 0.7879004041258445001 ) ) ;
#175287=CARTESIAN_POINT ( 'NONE',  ( -1.500000000000015099, 10.76041666734946212, -0.8660254037844309360 ) ) ;
#175313=CARTESIAN_POINT ( 'NONE',  ( 1.364683531249997417, 12.04687500034139980, 2.602085213965210642E-15 ) ) ;
#175320=EDGE_CURVE ( 'NONE', #193052, #102754, #74076, .T. ) ;
#175321=CARTESIAN_POINT ( 'NONE',  ( -1.115562610750309283E-14, 9.812500000000000000, 1.500000000000001554 ) ) ;
#175342=EDGE_CURVE ( 'NONE', #114519, #83117, #20602, .T. ) ;
#175382=CARTESIAN_POINT ( 'NONE',  ( 1.499999999999993117, 13.38541666734946745, 0.8660254037844409281 ) ) ;
#175390=LINE ( 'NONE', #78923, #64755 ) ;
#175416=CARTESIAN_POINT ( 'NONE',  ( 1.364683531249997417, 9.484375000341396245, 2.602085213965210642E-15 ) ) ;
#175461=CARTESIAN_POINT ( 'NONE',  ( -1.500000000000008216, 11.78125000068279427, 3.469446951953614189E-15 ) ) ;
#175566=CARTESIAN_POINT ( 'NONE',  ( 1.364683531249997417, 10.04687500034139802, 2.602085213965210642E-15 ) ) ;
#175573=CARTESIAN_POINT ( 'NONE',  ( -1.119339255005453736E-13, 13.28612805825129151, 1.454322456996997470 ) ) ;
#175592=CARTESIAN_POINT ( 'NONE',  ( 0.7500000000000006661, 11.58333333333333393, 1.299038105676657340 ) ) ;
#175638=CARTESIAN_POINT ( 'NONE',  ( -1.500000000000015099, 15.22916666666666607, -0.8660254037844309360 ) ) ;
#175677=CARTESIAN_POINT ( 'NONE',  ( 1.364683531250000303, 14.00520833367473195, -0.7879004041258355073 ) ) ;
#175679=VERTEX_POINT ( 'NONE', #43297 ) ;
#175709=CARTESIAN_POINT ( 'NONE',  ( -2.788906526875773208E-15, 8.937500000000001776, -1.499999999999998446 ) ) ;
#175778=CARTESIAN_POINT ( 'NONE',  ( -1.355148357678327198, 3.930362057294688682, 0.6430964159811503045 ) ) ;
#175799=CARTESIAN_POINT ( 'NONE',  ( 1.363015705810368239, 3.696841092726506517, -0.6271916676896889253 ) ) ;
#175823=CARTESIAN_POINT ( 'NONE',  ( 1.364683531250000303, 13.06770833367473728, -0.7879004041258355073 ) ) ;
#175832=ORIENTED_EDGE ( 'NONE', *, *, #90678, .F. ) ;
#175889=CARTESIAN_POINT ( 'NONE',  ( 0.6823417656249934904, 12.00520833367473017, 1.181850606188764807 ) ) ;
#175930=CARTESIAN_POINT ( 'NONE',  ( 0.7500000000000006661, 10.86458333401613174, 1.299038105676657340 ) ) ;
#175975=AXIS2_PLACEMENT_3D ( 'NONE', #148812, #169325, #101111 ) ;
#175983=CARTESIAN_POINT ( 'NONE',  ( -0.4153311931459208184, 3.850000000000006306, -0.4999999999999961142 ) ) ;
#176033=CARTESIAN_POINT ( 'NONE',  ( 1.354875605471919542, 3.923167251739089423, 0.6436714776511552882 ) ) ;
#176052=CARTESIAN_POINT ( 'NONE',  ( -1.446922511646519416, 3.374038201079560650, 0.4002501213623008702 ) ) ;
#176068=CARTESIAN_POINT ( 'NONE',  ( -8.012344526598182026E-15, 10.04687500034140335, -1.575800808251669460 ) ) ;
#176085=ORIENTED_EDGE ( 'NONE', *, *, #177186, .F. ) ;
#176140=CARTESIAN_POINT ( 'NONE',  ( 0.7500000000000006661, 12.91666666666666607, -1.299038105676657340 ) ) ;
#176272=CARTESIAN_POINT ( 'NONE',  ( 0.4019237886466850984, 12.70758545099816850, -1.499999999999996669 ) ) ;
#176327=CARTESIAN_POINT ( 'NONE',  ( -0.7500000000000179856, 12.79166666666666607, 1.299038105676658228 ) ) ;
#176332=CARTESIAN_POINT ( 'NONE',  ( 0.6823417656249934904, 8.692708333674733723, 1.181850606188764807 ) ) ;
#176347=CARTESIAN_POINT ( 'NONE',  ( 0.000000000000000000, -4.500000000000003553, 0.000000000000000000 ) ) ;
#176371=CARTESIAN_POINT ( 'NONE',  ( -0.6823417656250003738, 11.96354166700806765, 1.181850606188754593 ) ) ;
#176378=CARTESIAN_POINT ( 'NONE',  ( 1.500000000000001332, 9.875000000000001776, 0.000000000000000000 ) ) ;
#176380=ORIENTED_EDGE ( 'NONE', *, *, #199200, .F. ) ;
#176438=CARTESIAN_POINT ( 'NONE',  ( -0.7500000000000179856, 13.57291666734946389, 1.299038105676658228 ) ) ;
#176471=CARTESIAN_POINT ( 'NONE',  ( -0.6823417656250039265, 8.817708333674733723, -1.181850606188755259 ) ) ;
#176478=CARTESIAN_POINT ( 'NONE',  ( 0.4019237886466778820, 11.10491455036742536, 1.500000000000001554 ) ) ;
#176500=ADVANCED_FACE ( 'NONE', ( #61038 ), #28543, .T. ) ;
#176578=CARTESIAN_POINT ( 'NONE',  ( 0.000000000000000000, 13.49999999999999822, 0.000000000000000000 ) ) ;
#176621=CARTESIAN_POINT ( 'NONE',  ( 1.364683531249996529, 9.276041667008062319, 0.7879004041258405033 ) ) ;
#176710=CARTESIAN_POINT ( 'NONE',  ( -0.7500000000000006661, 9.708333333333332149, -1.299038105676657340 ) ) ;
#176731=CARTESIAN_POINT ( 'NONE',  ( -1.364683531250010295, 13.38020833367473017, 0.7879004041258445001 ) ) ;
#176742=CARTESIAN_POINT ( 'NONE',  ( -1.409302795777316097, 4.214550261772070705, -0.5172811130322977347 ) ) ;
#176823=ADVANCED_BREP_SHAPE_REPRESENTATION ( '', ( #12474, #200407 ), #197031 ) ;
#176824=CARTESIAN_POINT ( 'NONE',  ( -0.7500000000000006661, 12.20833333333333570, -1.299038105676657340 ) ) ;
#176852=CARTESIAN_POINT ( 'NONE',  ( 1.493145604987275998, 3.264456235588189426, 0.1636410324438895558 ) ) ;
#176878=CARTESIAN_POINT ( 'NONE',  ( 0.6823417656249969321, 13.33854166700806942, -1.181850606188757036 ) ) ;
#176896=ORIENTED_EDGE ( 'NONE', *, *, #173196, .F. ) ;
#176929=DIRECTION ( 'NONE',  ( 0.000000000000000000, -1.000000000000000000, 0.000000000000000000 ) ) ;
#176942=CARTESIAN_POINT ( 'NONE',  ( -8.012344526598182026E-15, 12.35937500034139624, -1.575800808251669460 ) ) ;
#176985=CARTESIAN_POINT ( 'NONE',  ( -1.500000000000015099, 10.26041666734946034, -0.8660254037844309360 ) ) ;
#177076=VERTEX_POINT ( 'NONE', #18669 ) ;
#177087=CARTESIAN_POINT ( 'NONE',  ( 1.264550565627409195, 3.910972709771358247, 0.5006333728358396407 ) ) ;
#177107=CARTESIAN_POINT ( 'NONE',  ( -1.392249819062528760, 3.364685323634090341, 0.1369250707803940370 ) ) ;
#177124=CARTESIAN_POINT ( 'NONE',  ( 1.364683531249997417, 9.734375000341396245, 2.602085213965210642E-15 ) ) ;
#177141=EDGE_LOOP ( 'NONE', ( #100690, #112756, #27456, #150692 ) ) ;
#177149=VERTEX_POINT ( 'NONE', #185438 ) ;
#177169=EDGE_LOOP ( 'NONE', ( #51444, #67401, #73406, #91704 ) ) ;
#177182=ORIENTED_EDGE ( 'NONE', *, *, #178292, .F. ) ;
#177186=EDGE_CURVE ( 'NONE', #33524, #78562, #206908, .T. ) ;
#177219=ORIENTED_EDGE ( 'NONE', *, *, #178292, .T. ) ;
#177314=VECTOR ( 'NONE', #37477, 1000.000000000000000 ) ;
#177351=ORIENTED_EDGE ( 'NONE', *, *, #103483, .F. ) ;
#177360=CARTESIAN_POINT ( 'NONE',  ( -0.7500000000000006661, 12.95833333333333570, -1.299038105676657340 ) ) ;
#177390=CARTESIAN_POINT ( 'NONE',  ( -1.500000000000008216, 12.24999999999999645, 3.469446951953614189E-15 ) ) ;
#177397=CARTESIAN_POINT ( 'NONE',  ( 1.364683531250000303, 9.505208333674735499, -0.7879004041258355073 ) ) ;
#177433=CARTESIAN_POINT ( 'NONE',  ( -0.6823417656250003738, 11.71354166700806765, 1.181850606188754593 ) ) ;
#177505=CARTESIAN_POINT ( 'NONE',  ( -0.7500000000000006661, 13.23958333401613352, -1.299038105676657340 ) ) ;
#177540=CARTESIAN_POINT ( 'NONE',  ( -0.6823417656250003738, 8.651041667008065872, 1.181850606188754593 ) ) ;
#177600=ORIENTED_EDGE ( 'NONE', *, *, #19150, .F. ) ;
#177692=CARTESIAN_POINT ( 'NONE',  ( -1.364683531250014514, 9.651041667008064096, -0.7879004041258335089 ) ) ;
#177716=CARTESIAN_POINT ( 'NONE',  ( 0.4019237886466778820, 9.104914550367427140, 1.500000000000001554 ) ) ;
#177722=CARTESIAN_POINT ( 'NONE',  ( 1.355377658251181394, 3.933662881449785598, 0.6426130056881899089 ) ) ;
#177806=CARTESIAN_POINT ( 'NONE',  ( -8.012344526598182026E-15, 13.04687500034139980, -1.575800808251669460 ) ) ;
#177817=CARTESIAN_POINT ( 'NONE',  ( -1.465018125636653901, 4.370054533944408348, -0.3314627765801590464 ) ) ;
#177841=( BOUNDED_CURVE ( )  B_SPLINE_CURVE ( 2, ( #16257, #198218, #99670, #113871, #2131, #67137, #165739, #17326, #68206 ),
 .UNSPECIFIED., .F., .T. ) 
 B_SPLINE_CURVE_WITH_KNOTS ( ( 3, 2, 2, 2, 3 ),
 ( 0.6517857142857143016, 0.6547619047619047672, 0.6607142857142856984, 0.6666666666666666297, 0.6696428571428570953 ),
 .UNSPECIFIED. ) 
 CURVE ( )  GEOMETRIC_REPRESENTATION_ITEM ( )  RATIONAL_B_SPLINE_CURVE ( ( 0.9330127018922194093, 0.9330127018922194093, 1.000000000000000000, 0.8660254037844387076, 1.000000000000000000, 0.8660254037844387076, 1.000000000000000000, 0.9330127018922206306, 0.9330127018922194093 ) ) 
 REPRESENTATION_ITEM ( '' )  );
#177895=ORIENTED_EDGE ( 'NONE', *, *, #158451, .F. ) ;
#177920=ORIENTED_EDGE ( 'NONE', *, *, #146436, .F. ) ;
#177928=CARTESIAN_POINT ( 'NONE',  ( 1.392969482149218452, 3.541472066643499783, 0.5575990067801355199 ) ) ;
#177952=CARTESIAN_POINT ( 'NONE',  ( 1.364683531249997417, 14.29687500034140157, 2.602085213965210642E-15 ) ) ;
#177972=ADVANCED_FACE ( 'NONE', ( #209165 ), #12044, .T. ) ;
#177977=CARTESIAN_POINT ( 'NONE',  ( -1.500000000000015099, 11.97916666666666785, -0.8660254037844309360 ) ) ;
#178014=CARTESIAN_POINT ( 'NONE',  ( 0.6823417656249969321, 11.08854166700806765, -1.181850606188757036 ) ) ;
#178030=CARTESIAN_POINT ( 'NONE',  ( -2.788906526875773208E-15, 8.468750000682796042, -1.499999999999998446 ) ) ;
#178057=CARTESIAN_POINT ( 'NONE',  ( -0.7500000000000006661, 9.239583334016129967, -1.299038105676657340 ) ) ;
#178139=EDGE_CURVE ( 'NONE', #111937, #155317, #140539, .T. ) ;
#178162=CARTESIAN_POINT ( 'NONE',  ( 1.272106862006046057, 3.977462442649445151, 0.4878970607599459886 ) ) ;
#178182=CARTESIAN_POINT ( 'NONE',  ( -1.392936117481092140, 3.541413949887021406, -0.5577005436123527726 ) ) ;
#178200=CARTESIAN_POINT ( 'NONE',  ( -0.6823417656250039265, 8.817708333674733723, -1.181850606188755259 ) ) ;
#178214=PLANE ( 'NONE',  #161335 ) ;
#178226=VERTEX_POINT ( 'NONE', #123256 ) ;
#178227=AXIS2_PLACEMENT_3D ( 'NONE', #75717, #58405, #124560 ) ;
#178248=DIRECTION ( 'NONE',  ( -1.000000000000000000, 0.000000000000000000, 1.665334536937734811E-16 ) ) ;
#178277=CARTESIAN_POINT ( 'NONE',  ( 1.364683531249996529, 15.27604166700806587, 0.7879004041258405033 ) ) ;
#178292=EDGE_CURVE ( 'NONE', #193052, #103348, #91752, .T. ) ;
#178346=( LENGTH_UNIT ( ) NAMED_UNIT ( * ) SI_UNIT ( .MILLI., .METRE. ) );
#178461=CARTESIAN_POINT ( 'NONE',  ( 1.500000000000001332, 11.12499999999999645, 0.000000000000000000 ) ) ;
#178466=CARTESIAN_POINT ( 'NONE',  ( -1.364683531250014514, 9.338541667008062319, -0.7879004041258335089 ) ) ;
#178500=CARTESIAN_POINT ( 'NONE',  ( 1.364683531249997417, 10.29687500034139802, 2.602085213965210642E-15 ) ) ;
#178574=CARTESIAN_POINT ( 'NONE',  ( 1.499999999999997113, 14.17708333401613352, -0.8660254037844378194 ) ) ;
#178583=DIRECTION ( 'NONE',  ( 0.000000000000000000, -0.7071067811865513475, -0.7071067811865435759 ) ) ;
#178610=CARTESIAN_POINT ( 'NONE',  ( 1.364683531249996529, 8.713541667008067648, 0.7879004041258405033 ) ) ;
#178739=VERTEX_POINT ( 'NONE', #191073 ) ;
#178792=CARTESIAN_POINT ( 'NONE',  ( 1.456203110946918677, 4.349935091901982354, 0.3915051095678068194 ) ) ;
#178818=CARTESIAN_POINT ( 'NONE',  ( -1.115562610750309283E-14, 11.31249999999999822, 1.500000000000001554 ) ) ;
#178860=CARTESIAN_POINT ( 'NONE',  ( -1.500000000000008216, 9.750000000000001776, 3.469446951953614189E-15 ) ) ;
#178878=CARTESIAN_POINT ( 'NONE',  ( -0.6823417656250003738, 12.65104166700806232, 1.181850606188754593 ) ) ;
#179000=CARTESIAN_POINT ( 'NONE',  ( 1.478151113144027251, 3.421726889910780667, 0.2686735943296981177 ) ) ;
#179023=CARTESIAN_POINT ( 'NONE',  ( -8.012344526598182026E-15, 12.60937500034139802, -1.575800808251669460 ) ) ;
#179060=VERTEX_POINT ( 'NONE', #119544 ) ;
#179082=CARTESIAN_POINT ( 'NONE',  ( 1.364683531249997417, 9.796875000341396245, 2.602085213965210642E-15 ) ) ;
#179124=CARTESIAN_POINT ( 'NONE',  ( -1.500000000000008216, 10.03125000068279959, 3.469446951953614189E-15 ) ) ;
#179176=CARTESIAN_POINT ( 'NONE',  ( -0.6384131795730932923, 4.335164563247821512, 0.1378994657016395786 ) ) ;
#179227=CARTESIAN_POINT ( 'NONE',  ( 1.369767765231834300, 4.288585766148679035, -0.2488260012212581695 ) ) ;
#179247=CARTESIAN_POINT ( 'NONE',  ( -1.436275828743291516, 3.619984746957625621, -0.4487520553618166153 ) ) ;
#179249=ADVANCED_FACE ( 'NONE', ( #26233 ), #137883, .T. ) ;
#179256=EDGE_CURVE ( 'NONE', #170920, #1432, #129059, .T. ) ;
#179267=CARTESIAN_POINT ( 'NONE',  ( -8.012344526598182026E-15, 9.296875000341398021, -1.575800808251669460 ) ) ;
#179281=LINE ( 'NONE', #211749, #67884 ) ;
#179342=CARTESIAN_POINT ( 'NONE',  ( 1.364683531249997417, 14.79687500034139447, 2.602085213965210642E-15 ) ) ;
#179375=CARTESIAN_POINT ( 'NONE',  ( 0.000000000000000000, 13.49999999999999822, 0.000000000000000000 ) ) ;
#179403=CARTESIAN_POINT ( 'NONE',  ( 1.499999999999996891, 8.677083334016133520, -0.8660254037844378194 ) ) ;
#179409=SURFACE_SIDE_STYLE ('',( #159950 ) ) ;
#179422=CARTESIAN_POINT ( 'NONE',  ( 1.686272053095002589E-16, -4.517653975874099892, 1.376945625684933061 ) ) ;
#179528=CARTESIAN_POINT ( 'NONE',  ( -0.7500000000000006661, 11.45833333333333393, -1.299038105676657340 ) ) ;
#179533=CARTESIAN_POINT ( 'NONE',  ( -1.364683531250014514, 8.838541667008069425, -0.7879004041258335089 ) ) ;
#179540=CARTESIAN_POINT ( 'NONE',  ( -0.5723599497803579794, 3.454715670812215311, -0.3124809264750456061 ) ) ;
#179565=CARTESIAN_POINT ( 'NONE',  ( -1.364683531250014514, 10.15104166700806587, -0.7879004041258335089 ) ) ;
#179569=( BOUNDED_CURVE ( )  B_SPLINE_CURVE ( 2, ( #141174, #22002, #186664, #203960, #170413, #71829, #56681, #42589, #121763 ),
 .UNSPECIFIED., .F., .T. ) 
 B_SPLINE_CURVE_WITH_KNOTS ( ( 3, 2, 2, 2, 3 ),
 ( 0.9732142857142856984, 0.9761904761904761640, 0.9821428571428570953, 0.9880952380952381375, 0.9910714285714286031 ),
 .UNSPECIFIED. ) 
 CURVE ( )  GEOMETRIC_REPRESENTATION_ITEM ( )  RATIONAL_B_SPLINE_CURVE ( ( 0.9330127018922194093, 0.9330127018922194093, 1.000000000000000000, 0.8660254037844387076, 1.000000000000000000, 0.8660254037844387076, 1.000000000000000000, 0.9330127018922194093, 0.9330127018922194093 ) ) 
 REPRESENTATION_ITEM ( '' )  );
#179573=CARTESIAN_POINT ( 'NONE',  ( 0.7500000000000006661, 9.916666666666671404, -1.299038105676657340 ) ) ;
#179639=CARTESIAN_POINT ( 'NONE',  ( -0.7500000000000179856, 14.32291666734946567, 1.299038105676658228 ) ) ;
#179672=CARTESIAN_POINT ( 'NONE',  ( -1.364683531250014514, 8.838541667008069425, -0.7879004041258335089 ) ) ;
#179676=ORIENTED_EDGE ( 'NONE', *, *, #146727, .F. ) ;
#179779=CARTESIAN_POINT ( 'NONE',  ( -1.364683531250014514, 12.58854166700806054, -0.7879004041258335089 ) ) ;
#179821=CARTESIAN_POINT ( 'NONE',  ( -0.6823417656250039265, 8.880208333674733723, -1.181850606188755259 ) ) ;
#179825=VERTEX_POINT ( 'NONE', #175709 ) ;
#179843=AXIS2_PLACEMENT_3D ( 'NONE', #185697, #196894, #132999 ) ;
#179858=CARTESIAN_POINT ( 'NONE',  ( -0.4019237886466871523, 9.979914550367427140, -1.499999999999998668 ) ) ;
#179874=CARTESIAN_POINT ( 'NONE',  ( 0.4019237886466884846, 11.42633545031536535, -1.499999999999994449 ) ) ;
#179899=ORIENTED_EDGE ( 'NONE', *, *, #117958, .F. ) ;
#179904=CARTESIAN_POINT ( 'NONE',  ( -0.7500000000000179856, 8.322916667349467446, 1.299038105676658228 ) ) ;
#179931=CARTESIAN_POINT ( 'NONE',  ( 1.364683531249996529, 13.21354166700806410, 0.7879004041258405033 ) ) ;
#179944=CARTESIAN_POINT ( 'NONE',  ( -1.500389033793473770, 4.450847250840007874, 0.07878897303668215557 ) ) ;
#180080=CARTESIAN_POINT ( 'NONE',  ( -1.364683531250010295, 12.19270833367473195, 0.7879004041258445001 ) ) ;
#180117=ORIENTED_EDGE ( 'NONE', *, *, #129667, .T. ) ;
#180121=VERTEX_POINT ( 'NONE', #181983 ) ;
#180143=CARTESIAN_POINT ( 'NONE',  ( 0.6823417656249969321, 10.08854166700806587, -1.181850606188757036 ) ) ;
#180171=CARTESIAN_POINT ( 'NONE',  ( 0.7500000000000006661, 12.08333333333333570, 1.299038105676657340 ) ) ;
#180188=CARTESIAN_POINT ( 'NONE',  ( 0.7500000000000006661, 10.36458333401613174, 1.299038105676657340 ) ) ;
#180239=CARTESIAN_POINT ( 'NONE',  ( -0.6500564563262781759, 4.350073393241474129, -0.06808518787147278817 ) ) ;
#180254=DIRECTION ( 'NONE',  ( 0.000000000000000000, 0.000000000000000000, -1.000000000000000000 ) ) ;
#180290=CARTESIAN_POINT ( 'NONE',  ( 1.392936117481126113, 4.158586050112920596, -0.5577005436122643989 ) ) ;
#180307=CARTESIAN_POINT ( 'NONE',  ( -1.350460993223241868, 3.453365176191621089, 0.3113056364347011606 ) ) ;
#180308=EDGE_CURVE ( 'NONE', #180412, #99270, #41131, .T. ) ;
#180323=CARTESIAN_POINT ( 'NONE',  ( 0.6823417656249934904, 9.442708333674735499, 1.181850606188764807 ) ) ;
#180355=CARTESIAN_POINT ( 'NONE',  ( 3.834746474454188013E-15, 12.84375000068279782, 1.500000000000001554 ) ) ;
#180392=CARTESIAN_POINT ( 'NONE',  ( -1.364683531250010295, 14.44270833367473550, 0.7879004041258445001 ) ) ;
#180412=VERTEX_POINT ( 'NONE', #131191 ) ;
#180574=CARTESIAN_POINT ( 'NONE',  ( -6.009258394948636914E-15, 10.43750000000000178, -1.732050807568875195 ) ) ;
#180580=CARTESIAN_POINT ( 'NONE',  ( -0.6823417656250003738, 9.651041667008065872, 1.181850606188754593 ) ) ;
#180615=CARTESIAN_POINT ( 'NONE',  ( -1.364683531250000748, 10.67187500034139802, 0.000000000000000000 ) ) ;
#180619=CIRCLE ( 'NONE', #139065, 1.359291649810832503 ) ;
#180647=ADVANCED_FACE ( 'NONE', ( #5336 ), #103958, .F. ) ;
#180656=CARTESIAN_POINT ( 'NONE',  ( -0.7500000000000006661, 9.958333333333332149, -1.299038105676657340 ) ) ;
#180686=VECTOR ( 'NONE', #35988, 1000.000000000000000 ) ;
#180689=CARTESIAN_POINT ( 'NONE',  ( -6.009258394948636914E-15, 12.71875000068280137, -1.732050807568875195 ) ) ;
#180764=CARTESIAN_POINT ( 'NONE',  ( -3.602337597214539753E-15, 12.81249999999999822, 1.500000000000001554 ) ) ;
#180856=VERTEX_POINT ( 'NONE', #58398 ) ;
#180871=CARTESIAN_POINT ( 'NONE',  ( -0.6823417656250039265, 8.630208333674733723, -1.181850606188755259 ) ) ;
#180890=CARTESIAN_POINT ( 'NONE',  ( 0.4019237886466816012, 9.176335450315372455, -1.499999999999998668 ) ) ;
#180893=ORIENTED_EDGE ( 'NONE', *, *, #37798, .T. ) ;
#180983=CARTESIAN_POINT ( 'NONE',  ( -0.6823417656250003738, 12.90104166700806232, 1.181850606188754593 ) ) ;
#181034=ORIENTED_EDGE ( 'NONE', *, *, #162651, .F. ) ;
#181048=CARTESIAN_POINT ( 'NONE',  ( -1.154700538379266339, -4.295408888568413630, 2.602085213965210642E-15 ) ) ;
#181109=EDGE_CURVE ( 'NONE', #98073, #60619, #101849, .T. ) ;
#181132=CARTESIAN_POINT ( 'NONE',  ( 1.364683531249996529, 12.27604166700806054, 0.7879004041258405033 ) ) ;
#181157=CARTESIAN_POINT ( 'NONE',  ( 2.449293598294706414E-16, -0.5000000000000004441, -2.000000000000000000 ) ) ;
#181194=CARTESIAN_POINT ( 'NONE',  ( 0.6823417656249934904, 10.00520833367472839, 1.181850606188764807 ) ) ;
#181235=CARTESIAN_POINT ( 'NONE',  ( 0.7500000000000006661, 10.19791666734946922, -1.299038105676657340 ) ) ;
#181244=CARTESIAN_POINT ( 'NONE',  ( 1.499999999999996891, 10.17708333401613174, -0.8660254037844378194 ) ) ;
#181304=AXIS2_PLACEMENT_3D ( 'NONE', #6481, #174364, #124614 ) ;
#181326=ORIENTED_EDGE ( 'NONE', *, *, #192671, .T. ) ;
#181379=CARTESIAN_POINT ( 'NONE',  ( 0.6823417656249969321, 9.776041667008065872, -1.181850606188757036 ) ) ;
#181443=CARTESIAN_POINT ( 'NONE',  ( 0.7500000000000006661, 12.83333333333333570, 1.299038105676657340 ) ) ;
#181444=CARTESIAN_POINT ( 'NONE',  ( -1.364683531250014514, 14.90104166700806410, -0.7879004041258335089 ) ) ;
#181568=ORIENTED_EDGE ( 'NONE', *, *, #37635, .T. ) ;
#181604=CARTESIAN_POINT ( 'NONE',  ( -2.788906526875773208E-15, 11.96875000068279604, -1.499999999999998446 ) ) ;
#181625=CARTESIAN_POINT ( 'NONE',  ( 1.500000000000001332, 11.62499999999999645, 0.000000000000000000 ) ) ;
#181630=CARTESIAN_POINT ( 'NONE',  ( -1.364683531250014514, 14.40104166700806410, -0.7879004041258335089 ) ) ;
#181640=CARTESIAN_POINT ( 'NONE',  ( -0.4153311931459131578, 3.780306491160339011, 0.5000000000000066613 ) ) ;
#181669=CARTESIAN_POINT ( 'NONE',  ( 0.6823417656249934904, 10.00520833367472839, 1.181850606188764807 ) ) ;
#181739=CARTESIAN_POINT ( 'NONE',  ( -1.500000000000015099, 12.76041666734946567, -0.8660254037844309360 ) ) ;
#181983=CARTESIAN_POINT ( 'NONE',  ( -2.788906526875773208E-15, 12.46875000068279782, -1.499999999999998446 ) ) ;
#182032=CARTESIAN_POINT ( 'NONE',  ( 0.6823417656249969321, 11.52604166700806765, -1.181850606188757036 ) ) ;
#182062=CARTESIAN_POINT ( 'NONE',  ( 0.1858884387159591145, 13.28951043065277737, 1.441950245016251575 ) ) ;
#182185=CARTESIAN_POINT ( 'NONE',  ( 1.364683531249996529, 12.02604166700806765, 0.7879004041258405033 ) ) ;
#182201=ORIENTED_EDGE ( 'NONE', *, *, #76416, .T. ) ;
#182208=ORIENTED_EDGE ( 'NONE', *, *, #120145, .T. ) ;
#182237=CARTESIAN_POINT ( 'NONE',  ( -1.364683531250010740, 12.88020833367473372, 0.7879004041258445001 ) ) ;
#182252=CARTESIAN_POINT ( 'NONE',  ( -8.012344526598182026E-15, 10.85937500034139624, -1.575800808251669460 ) ) ;
#182293=CARTESIAN_POINT ( 'NONE',  ( 1.364683531249997417, 15.23437500034140157, 2.602085213965210642E-15 ) ) ;
#182357=CYLINDRICAL_SURFACE ( 'NONE', #175975, 1.500000000000000222 ) ;
#182390=CARTESIAN_POINT ( 'NONE',  ( -1.500000000000008216, 9.250000000000001776, 3.469446951953614189E-15 ) ) ;
#182396=CARTESIAN_POINT ( 'NONE',  ( 0.7500000000000006661, 9.364583334016129967, 1.299038105676657340 ) ) ;
#182432=CARTESIAN_POINT ( 'NONE',  ( -1.402160292154681736E-14, 8.421875000341403350, 1.575800808251682339 ) ) ;
#182476=ORIENTED_EDGE ( 'NONE', *, *, #31832, .T. ) ;
#182498=CARTESIAN_POINT ( 'NONE',  ( 1.364683531249997417, 15.04687500034139447, 2.602085213965210642E-15 ) ) ;
#182500=PRODUCT_DEFINITION_CONTEXT ( 'detailed design', #198672, 'design' ) ;
#182695=CARTESIAN_POINT ( 'NONE',  ( -6.009258394948636914E-15, 11.18749999999999645, -1.732050807568875195 ) ) ;
#182701=CARTESIAN_POINT ( 'NONE',  ( -1.402160292154681736E-14, 14.98437500034140157, 1.575800808251682339 ) ) ;
#182744=CARTESIAN_POINT ( 'NONE',  ( -1.402160292154681736E-14, 10.23437500034139447, 1.575800808251682339 ) ) ;
#182819=CARTESIAN_POINT ( 'NONE',  ( 1.499999999999997113, 12.42708333401612819, -0.8660254037844378194 ) ) ;
#182910=CARTESIAN_POINT ( 'NONE',  ( 0.6823417656249934904, 12.94270833367473017, 1.181850606188764807 ) ) ;
#182963=CARTESIAN_POINT ( 'NONE',  ( 1.364683531249997417, 11.48437500034139802, 2.602085213965210642E-15 ) ) ;
#183052=CARTESIAN_POINT ( 'NONE',  ( -0.7500000000000179856, 11.54166666666666607, 1.299038105676658228 ) ) ;
#183069=AXIS2_PLACEMENT_3D ( 'NONE', #165737, #70331, #133269 ) ;
#183113=CARTESIAN_POINT ( 'NONE',  ( -1.364683531250014514, 11.08854166700806410, -0.7879004041258335089 ) ) ;
#183261=CARTESIAN_POINT ( 'NONE',  ( 1.364683531250000303, 12.06770833367473195, -0.7879004041258355073 ) ) ;
#183272=VERTEX_POINT ( 'NONE', #124704 ) ;
#183282=ORIENTED_EDGE ( 'NONE', *, *, #195251, .F. ) ;
#183311=CARTESIAN_POINT ( 'NONE',  ( -1.402160292154681736E-14, 13.17187500034139980, 1.575800808251682339 ) ) ;
#183328=CARTESIAN_POINT ( 'NONE',  ( 0.6823417656249969321, 9.838541667008065872, -1.181850606188757036 ) ) ;
#183331=COLOUR_RGB ( '', 0.66274510, 0.83137255, 0.94901961) ;
#183346=EDGE_LOOP ( 'NONE', ( #22251, #166284, #116239, #49982 ) ) ;
#183354=CARTESIAN_POINT ( 'NONE',  ( 1.154700538379228147, -2.500000000000002220, -1.734723475976807094E-15 ) ) ;
#183371=CARTESIAN_POINT ( 'NONE',  ( -1.364683531250000748, 15.35937500034140157, 0.000000000000000000 ) ) ;
#183562=DIRECTION ( 'NONE',  ( 0.000000000000000000, 1.000000000000000000, 0.000000000000000000 ) ) ;
#183575=CARTESIAN_POINT ( 'NONE',  ( -0.6823417656250039265, 13.88020833367473195, -1.181850606188755259 ) ) ;
#183713=VERTEX_POINT ( 'NONE', #976 ) ;
#183744=CARTESIAN_POINT ( 'NONE',  ( 0.7500000000000006661, 11.86458333401613174, 1.299038105676657340 ) ) ;
#183747=DIRECTION ( 'NONE',  ( 0.000000000000000000, -1.000000000000000000, 0.000000000000000000 ) ) ;
#183765=CARTESIAN_POINT ( 'NONE',  ( -0.6823417656250039265, 12.06770833367473017, -1.181850606188755259 ) ) ;
#183771=CARTESIAN_POINT ( 'NONE',  ( -1.500000000000008216, 9.250000000000001776, 3.469446951953614189E-15 ) ) ;
#183817=CARTESIAN_POINT ( 'NONE',  ( 0.6823417656249934904, 9.255208333674728394, 1.181850606188764807 ) ) ;
#183888=CARTESIAN_POINT ( 'NONE',  ( 1.500000000000001332, 12.15625000068279427, 0.000000000000000000 ) ) ;
#183963=CYLINDRICAL_SURFACE ( 'NONE', #134203, 1.500000000000000222 ) ;
#183977=CARTESIAN_POINT ( 'NONE',  ( -1.364683531250010295, 13.63020833367473017, 0.7879004041258445001 ) ) ;
#184023=VECTOR ( 'NONE', #33868, 1000.000000000000000 ) ;
#184024=CARTESIAN_POINT ( 'NONE',  ( -1.402160292154681736E-14, 11.42187500034140157, 1.575800808251682339 ) ) ;
#184161=CARTESIAN_POINT ( 'NONE',  ( 0.6499422464084809725, 4.349924920312916221, -0.06926476342541491860 ) ) ;
#184171=CARTESIAN_POINT ( 'NONE',  ( -0.6823417656250003738, 11.90104166700806054, 1.181850606188754593 ) ) ;
#184223=ORIENTED_EDGE ( 'NONE', *, *, #198065, .T. ) ;
#184316=CARTESIAN_POINT ( 'NONE',  ( -1.364683531250010295, 10.69270833367473372, 0.7879004041258445001 ) ) ;
#184385=CARTESIAN_POINT ( 'NONE',  ( -0.6823417656250003738, 9.713541667008065872, 1.181850606188754593 ) ) ;
#184429=CARTESIAN_POINT ( 'NONE',  ( -1.364683531250000748, 15.10937500034140157, 0.000000000000000000 ) ) ;
#184508=ORIENTED_EDGE ( 'NONE', *, *, #35190, .F. ) ;
#184537=EDGE_CURVE ( 'NONE', #213528, #31261, #91360, .T. ) ;
#184554=AXIS2_PLACEMENT_3D ( 'NONE', #146587, #130386, #81549 ) ;
#184572=CARTESIAN_POINT ( 'NONE',  ( 0.000000000000000000, 13.49999999999999822, 0.000000000000000000 ) ) ;
#184632=CARTESIAN_POINT ( 'NONE',  ( -1.402160292154681736E-14, 12.98437500034139980, 1.575800808251682339 ) ) ;
#184755=( BOUNDED_CURVE ( )  B_SPLINE_CURVE ( 2, ( #181604, #33232, #67827, #148068, #114560, #133974, #183744, #165365, #49488 ),
 .UNSPECIFIED., .F., .T. ) 
 B_SPLINE_CURVE_WITH_KNOTS ( ( 3, 2, 2, 2, 3 ),
 ( 0.4732142857142856984, 0.4761904761904761640, 0.4821428571428571508, 0.4880952380952380820, 0.4910714285714285476 ),
 .UNSPECIFIED. ) 
 CURVE ( )  GEOMETRIC_REPRESENTATION_ITEM ( )  RATIONAL_B_SPLINE_CURVE ( ( 0.9330127018922194093, 0.9330127018922194093, 1.000000000000000000, 0.8660254037844387076, 1.000000000000000000, 0.8660254037844387076, 1.000000000000000000, 0.9330127018922199644, 0.9330127018922194093 ) ) 
 REPRESENTATION_ITEM ( '' )  );
#184779=CARTESIAN_POINT ( 'NONE',  ( 0.000000000000000000, 13.49999999999999822, -1.500000000000000222 ) ) ;
#184797=FACE_OUTER_BOUND ( 'NONE', #111552, .T. ) ;
#184815=CARTESIAN_POINT ( 'NONE',  ( -0.6823417656250039265, 11.56770833367473017, -1.181850606188755259 ) ) ;
#184820=CARTESIAN_POINT ( 'NONE',  ( -1.500000000000015099, 9.479166666666669627, -0.8660254037844309360 ) ) ;
#184831=ORIENTED_EDGE ( 'NONE', *, *, #154049, .T. ) ;
#184871=CARTESIAN_POINT ( 'NONE',  ( -0.6823417656250039265, 9.630208333674728394, -1.181850606188755259 ) ) ;
#184926=CARTESIAN_POINT ( 'NONE',  ( 0.4019237886466778820, 8.573664549684629321, 1.500000000000001554 ) ) ;
#184940=CARTESIAN_POINT ( 'NONE',  ( -1.500000000000008216, 12.03125000068279427, 3.469446951953614189E-15 ) ) ;
#185015=CARTESIAN_POINT ( 'NONE',  ( 1.364853456228726225, 3.682974172409147595, -0.6233480900563427296 ) ) ;
#185031=CARTESIAN_POINT ( 'NONE',  ( -1.364683531250000748, 13.60937500034139980, 0.000000000000000000 ) ) ;
#185074=CARTESIAN_POINT ( 'NONE',  ( -0.7500000000000179856, 13.54166666666666785, 1.299038105676658228 ) ) ;
#185082=CARTESIAN_POINT ( 'NONE',  ( -1.364683531250010295, 11.63020833367472839, 0.7879004041258445001 ) ) ;
#185136=ORIENTED_EDGE ( 'NONE', *, *, #207358, .T. ) ;
#185229=CARTESIAN_POINT ( 'NONE',  ( -1.402160292154681736E-14, 11.92187500034140157, 1.575800808251682339 ) ) ;
#185232=VERTEX_POINT ( 'NONE', #41815 ) ;
#185237=CARTESIAN_POINT ( 'NONE',  ( 0.000000000000000000, 13.49999999999999822, -1.500000000000000222 ) ) ;
#185262=CARTESIAN_POINT ( 'NONE',  ( 4.344593448898664693E-13, 13.36537488277823371, -1.375075632470054154 ) ) ;
#185276=ORIENTED_EDGE ( 'NONE', *, *, #194138, .T. ) ;
#185310=VECTOR ( 'NONE', #56401, 1000.000000000000000 ) ;
#185387=CARTESIAN_POINT ( 'NONE',  ( 1.364683531250000303, 11.56770833367472839, -0.7879004041258355073 ) ) ;
#185400=ORIENTED_EDGE ( 'NONE', *, *, #38945, .F. ) ;
#185411=CARTESIAN_POINT ( 'NONE',  ( 1.364683531249997417, 15.23437500034140157, 2.602085213965210642E-15 ) ) ;
#185438=CARTESIAN_POINT ( 'NONE',  ( -2.926243505372967280E-18, -4.140708350189166609, -0.9999999999999991118 ) ) ;
#185447=LINE ( 'NONE', #154036, #139902 ) ;
#185453=CARTESIAN_POINT ( 'NONE',  ( 0.6823417656249969321, 9.088541667008065872, -1.181850606188757036 ) ) ;
#185461=DIRECTION ( 'NONE',  ( 0.000000000000000000, -1.000000000000000000, 0.000000000000000000 ) ) ;
#185494=CARTESIAN_POINT ( 'NONE',  ( -6.009258394948636914E-15, 8.468750000682796042, -1.732050807568875195 ) ) ;
#185630=CARTESIAN_POINT ( 'NONE',  ( 1.499999999999993117, 12.60416666666666785, 0.8660254037844408170 ) ) ;
#185646=CARTESIAN_POINT ( 'NONE',  ( 0.7500000000000006661, 12.36458333401613174, 1.299038105676657340 ) ) ;
#185696=CARTESIAN_POINT ( 'NONE',  ( -1.364683531250014514, 13.40104166700806587, -0.7879004041258335089 ) ) ;
#185697=CARTESIAN_POINT ( 'NONE',  ( 0.000000000000000000, 13.49999999999999822, 0.000000000000000000 ) ) ;
#185883=CARTESIAN_POINT ( 'NONE',  ( -1.364683531250014514, 11.83854166700806587, -0.7879004041258335089 ) ) ;
#185889=CARTESIAN_POINT ( 'NONE',  ( 1.500000000000001332, 10.12500000000000178, 0.000000000000000000 ) ) ;
#185938=CARTESIAN_POINT ( 'NONE',  ( -0.6823417656250003738, 9.463541667008065872, 1.181850606188754593 ) ) ;
#186000=EDGE_CURVE ( 'NONE', #178739, #175679, #193400, .T. ) ;
#186008=FACE_OUTER_BOUND ( 'NONE', #95555, .T. ) ;
#186011=CARTESIAN_POINT ( 'NONE',  ( -1.500000000000008216, 10.78125000068279249, 3.469446951953614189E-15 ) ) ;
#186012=EDGE_LOOP ( 'NONE', ( #101300, #119926, #144871, #96233 ) ) ;
#186096=EDGE_LOOP ( 'NONE', ( #192929, #79567, #176380, #10906 ) ) ;
#186105=CARTESIAN_POINT ( 'NONE',  ( 0.6823417656249969321, 13.52604166700806232, -1.181850606188757036 ) ) ;
#186126=CARTESIAN_POINT ( 'NONE',  ( 1.286956418854607431, 3.652345658002486672, 0.4592741676706121323 ) ) ;
#186148=CARTESIAN_POINT ( 'NONE',  ( -0.7500000000000006661, 13.20833333333333570, -1.299038105676657340 ) ) ;
#186155=CARTESIAN_POINT ( 'NONE',  ( 0.6823417656249934904, 12.44270833367473017, 1.181850606188764807 ) ) ;
#186180=DIRECTION ( 'NONE',  ( 0.000000000000000000, -1.000000000000000000, 0.000000000000000000 ) ) ;
#186182=CYLINDRICAL_SURFACE ( 'NONE', #87470, 1.500000000000000222 ) ;
#186234=ORIENTED_EDGE ( 'NONE', *, *, #180308, .T. ) ;
#186240=CARTESIAN_POINT ( 'NONE',  ( -1.115562610750309283E-14, 11.56249999999999822, 1.500000000000001554 ) ) ;
#186301=CARTESIAN_POINT ( 'NONE',  ( 1.364683531249996529, 11.96354166700806765, 0.7879004041258405033 ) ) ;
#186375=CARTESIAN_POINT ( 'NONE',  ( -0.4019237886466837106, 12.72991455036743069, -1.500000000000000666 ) ) ;
#186377=AXIS2_PLACEMENT_3D ( 'NONE', #201962, #5900, #120832 ) ;
#186409=CARTESIAN_POINT ( 'NONE',  ( -1.264911064067347324, 3.734364735516694012, 0.5000000000000092149 ) ) ;
#186453=CARTESIAN_POINT ( 'NONE',  ( -8.012344526598182026E-15, 10.60937500034139624, -1.575800808251669460 ) ) ;
#186462=CARTESIAN_POINT ( 'NONE',  ( -0.8537267228922215123, 13.37576698399828423, -1.079790317083570761 ) ) ;
#186482=CARTESIAN_POINT ( 'NONE',  ( -8.012344526598182026E-15, 15.04687500034140157, -1.575800808251669460 ) ) ;
#186485=CARTESIAN_POINT ( 'NONE',  ( -2.788906526875773208E-15, 10.68750000000000000, -1.499999999999998446 ) ) ;
#186503=ORIENTED_EDGE ( 'NONE', *, *, #54197, .F. ) ;
#186511=CARTESIAN_POINT ( 'NONE',  ( 1.499999999999993117, 11.63541666734946567, 0.8660254037844408170 ) ) ;
#186526=CARTESIAN_POINT ( 'NONE',  ( -1.364683531250010295, 8.692708333674730170, 0.7879004041258445001 ) ) ;
#186545=ORIENTED_EDGE ( 'NONE', *, *, #1351, .T. ) ;
#186570=CARTESIAN_POINT ( 'NONE',  ( -1.500000000000008216, 8.531250000682797818, 3.469446951953614189E-15 ) ) ;
#186664=CARTESIAN_POINT ( 'NONE',  ( 0.7500000000000006661, 8.447916667349467446, -1.299038105676657340 ) ) ;
#186708=CARTESIAN_POINT ( 'NONE',  ( -1.364683531250010295, 8.380208333674730170, 0.7879004041258445001 ) ) ;
#186773=CARTESIAN_POINT ( 'NONE',  ( 0.6823417656249934904, 13.00520833367473017, 1.181850606188764807 ) ) ;
#186937=CARTESIAN_POINT ( 'NONE',  ( 0.4019237886466847653, 8.854914550367425363, 1.499999999999997113 ) ) ;
#186941=CARTESIAN_POINT ( 'NONE',  ( 0.7500000000000006661, 8.916666666666669627, -1.299038105676657340 ) ) ;
#186960=CARTESIAN_POINT ( 'NONE',  ( -1.364683531250010740, 11.88020833367473017, 0.7879004041258445001 ) ) ;
#186965=CARTESIAN_POINT ( 'NONE',  ( -0.7500000000000179856, 10.29166666666667140, 1.299038105676658228 ) ) ;
#187016=CARTESIAN_POINT ( 'NONE',  ( -1.402160292154681736E-14, 9.734375000341399797, 1.575800808251682339 ) ) ;
#187020=CARTESIAN_POINT ( 'NONE',  ( -0.7500000000000179856, 10.32291666734946922, 1.299038105676658228 ) ) ;
#187067=DIRECTION ( 'NONE',  ( 0.000000000000000000, 1.000000000000000000, 0.000000000000000000 ) ) ;
#187074=CARTESIAN_POINT ( 'NONE',  ( -0.4019237886467001974, 9.332585450998170273, 1.500000000000001998 ) ) ;
#187087=ORIENTED_EDGE ( 'NONE', *, *, #71800, .T. ) ;
#187126=ORIENTED_EDGE ( 'NONE', *, *, #79219, .F. ) ;
#187177=CARTESIAN_POINT ( 'NONE',  ( 1.364683531249997417, 13.48437500034139980, 2.602085213965210642E-15 ) ) ;
#187188=CARTESIAN_POINT ( 'NONE',  ( 0.4019237886466847653, 12.10491455036742536, 1.499999999999997113 ) ) ;
#187223=CARTESIAN_POINT ( 'NONE',  ( 1.499999999999997113, 13.39583333333333570, -0.8660254037844378194 ) ) ;
#187228=CARTESIAN_POINT ( 'NONE',  ( -1.402160292154681736E-14, 11.67187500034140157, 1.575800808251682339 ) ) ;
#187241=ORIENTED_EDGE ( 'NONE', *, *, #165357, .T. ) ;
#187275=CARTESIAN_POINT ( 'NONE',  ( 0.6823417656249934904, 12.75520833367473017, 1.181850606188764807 ) ) ;
#187282=CARTESIAN_POINT ( 'NONE',  ( 0.4019237886466884846, 9.926335450315368902, -1.499999999999994449 ) ) ;
#187344=ORIENTED_EDGE ( 'NONE', *, *, #49372, .F. ) ;
#187375=CARTESIAN_POINT ( 'NONE',  ( -0.6823417656250039265, 10.81770833367473550, -1.181850606188755259 ) ) ;
#187413=CARTESIAN_POINT ( 'NONE',  ( 0.000000000000000000, 13.49999999999999822, -1.500000000000000222 ) ) ;
#187421=CARTESIAN_POINT ( 'NONE',  ( -0.7500000000000006661, 11.73958333401613174, -1.299038105676657340 ) ) ;
#187426=VERTEX_POINT ( 'NONE', #81479 ) ;
#187456=ORIENTED_EDGE ( 'NONE', *, *, #172795, .F. ) ;
#187457=CARTESIAN_POINT ( 'NONE',  ( -2.788906526875773208E-15, 10.18750000000000000, -1.499999999999998446 ) ) ;
#187490=CARTESIAN_POINT ( 'NONE',  ( -0.7500000000000179856, 11.04166666666666430, 1.299038105676658228 ) ) ;
#187524=CARTESIAN_POINT ( 'NONE',  ( 0.6823417656249934904, 11.00520833367472839, 1.181850606188764807 ) ) ;
#187549=CARTESIAN_POINT ( 'NONE',  ( -1.364683531250014514, 14.58854166700806232, -0.7879004041258335089 ) ) ;
#187591=CARTESIAN_POINT ( 'NONE',  ( -0.6823417656250003738, 8.463541667008064096, 1.181850606188754593 ) ) ;
#187597=CARTESIAN_POINT ( 'NONE',  ( -1.500085555261173376, 4.450186320795536332, -0.08157497973213596876 ) ) ;
#187634=CARTESIAN_POINT ( 'NONE',  ( -1.402160292154681736E-14, 14.17187500034139624, 1.575800808251682339 ) ) ;
#187644=CARTESIAN_POINT ( 'NONE',  ( -1.315349297999210076, 4.153791881628437821, -0.4023297572127273458 ) ) ;
#187667=CARTESIAN_POINT ( 'NONE',  ( 0.7662865668233912464, -4.140281660848650347, -0.6727527331043390291 ) ) ;
#187731=( BOUNDED_CURVE ( )  B_SPLINE_CURVE ( 2, ( #76617, #176272, #204460, #9489, #157896, #11612, #107051, #8413, #188229 ),
 .UNSPECIFIED., .F., .T. ) 
 B_SPLINE_CURVE_WITH_KNOTS ( ( 3, 2, 2, 2, 3 ),
 ( 0.3660714285714286031, 0.3690476190476190688, 0.3750000000000000000, 0.3809523809523809312, 0.3839285714285713969 ),
 .UNSPECIFIED. ) 
 CURVE ( )  GEOMETRIC_REPRESENTATION_ITEM ( )  RATIONAL_B_SPLINE_CURVE ( ( 0.9330127018922194093, 0.9330127018922199644, 1.000000000000000000, 0.8660254037844387076, 1.000000000000000000, 0.8660254037844387076, 1.000000000000000000, 0.9330127018922199644, 0.9330127018922194093 ) ) 
 REPRESENTATION_ITEM ( '' )  );
#187774=CARTESIAN_POINT ( 'NONE',  ( -1.364683531250000748, 14.67187500034139447, 0.000000000000000000 ) ) ;
#187777=AXIS2_PLACEMENT_3D ( 'NONE', #119473, #185461, #85841 ) ;
#187796=DIRECTION ( 'NONE',  ( 0.000000000000000000, 0.000000000000000000, -1.000000000000000000 ) ) ;
#187837=CARTESIAN_POINT ( 'NONE',  ( -8.012344526598182026E-15, 12.60937500034139802, -1.575800808251669460 ) ) ;
#187879=ORIENTED_EDGE ( 'NONE', *, *, #173196, .T. ) ;
#188025=CARTESIAN_POINT ( 'NONE',  ( -1.364683531250014514, 10.83854166700806942, -0.7879004041258335089 ) ) ;
#188031=CARTESIAN_POINT ( 'NONE',  ( 0.7500000000000006661, 9.416666666666669627, -1.299038105676657340 ) ) ;
#188083=CARTESIAN_POINT ( 'NONE',  ( -0.6823417656250003738, 9.963541667008065872, 1.181850606188754593 ) ) ;
#188146=CARTESIAN_POINT ( 'NONE',  ( 1.836970198721030181E-16, 13.49999999999999822, 1.500000000000000222 ) ) ;
#188147=VERTEX_POINT ( 'NONE', #164403 ) ;
#188229=CARTESIAN_POINT ( 'NONE',  ( -3.602337597214539753E-15, 12.59375000068279782, 1.500000000000001554 ) ) ;
#188239=CARTESIAN_POINT ( 'NONE',  ( -1.500000000000001110, 12.52083333333333215, 0.8660254037844418162 ) ) ;
#188287=CARTESIAN_POINT ( 'NONE',  ( -0.7500000000000006661, 13.95833333333333570, -1.299038105676657340 ) ) ;
#188293=CARTESIAN_POINT ( 'NONE',  ( 1.364683531249996529, 11.21354166700806232, 0.7879004041258405033 ) ) ;
#188345=CARTESIAN_POINT ( 'NONE',  ( -0.4019237886466871523, 12.22991455036742892, -1.499999999999998668 ) ) ;
#188358=CARTESIAN_POINT ( 'NONE',  ( -1.115562610750309283E-14, 10.31250000000000000, 1.500000000000001554 ) ) ;
#188365=CARTESIAN_POINT ( 'NONE',  ( 1.364683531250000748, 13.00520833367473550, -0.7879004041258355073 ) ) ;
#188442=CARTESIAN_POINT ( 'NONE',  ( -0.6823417656250003738, 10.15104166700806587, 1.181850606188754593 ) ) ;
#188446=CARTESIAN_POINT ( 'NONE',  ( -0.4019237886466871523, 13.22991455036742714, -1.499999999999998668 ) ) ;
#188550=CARTESIAN_POINT ( 'NONE',  ( -1.310129046446498746, 3.547233999020424466, -0.4142140226951010473 ) ) ;
#188570=CARTESIAN_POINT ( 'NONE',  ( 1.249999999999997558, -1.500000000000001332, 1.734723475976807094E-15 ) ) ;
#188594=CARTESIAN_POINT ( 'NONE',  ( -1.364683531250014514, 10.90104166700806942, -0.7879004041258335089 ) ) ;
#188608=ORIENTED_EDGE ( 'NONE', *, *, #9331, .T. ) ;
#188619=CARTESIAN_POINT ( 'NONE',  ( -1.364683531250010295, 14.38020833367473372, 0.7879004041258445001 ) ) ;
#188665=CARTESIAN_POINT ( 'NONE',  ( 1.500000000000001332, 14.62500000000000000, 0.000000000000000000 ) ) ;
#188668=EDGE_CURVE ( 'NONE', #151327, #81332, #154803, .T. ) ;
#188679=DIRECTION ( 'NONE',  ( 0.1669130127894903892, -0.9056625952363863696, -0.3897631457067597394 ) ) ;
#188710=CARTESIAN_POINT ( 'NONE',  ( -1.402160292154681736E-14, 14.92187500034139980, 1.575800808251682339 ) ) ;
#188720=CARTESIAN_POINT ( 'NONE',  ( -1.264548378739724699, 3.911400545389569050, -0.5006372017796719698 ) ) ;
#188852=CARTESIAN_POINT ( 'NONE',  ( -0.6823417656250003738, 14.46354166700806410, 1.181850606188754593 ) ) ;
#188912=CARTESIAN_POINT ( 'NONE',  ( 0.6823417656249969321, 12.83854166700806942, -1.181850606188757036 ) ) ;
#188997=CARTESIAN_POINT ( 'NONE',  ( -1.500000000000015099, 9.510416667349463893, -0.8660254037844309360 ) ) ;
#189063=CARTESIAN_POINT ( 'NONE',  ( 3.834746474454188013E-15, 13.06250000000000178, 1.500000000000001554 ) ) ;
#189087=CARTESIAN_POINT ( 'NONE',  ( 3.834746474454188013E-15, 8.812500000000000000, 1.500000000000001554 ) ) ;
#189088=CARTESIAN_POINT ( 'NONE',  ( 1.264911064067347324, 3.965635264483307054, 0.5000000000000092149 ) ) ;
#189105=CARTESIAN_POINT ( 'NONE',  ( 1.364683531250000748, 11.00520833367473550, -0.7879004041258355073 ) ) ;
#189111=CARTESIAN_POINT ( 'NONE',  ( -1.500000000000001110, 9.020833333333330373, 0.8660254037844419273 ) ) ;
#189132=CARTESIAN_POINT ( 'NONE',  ( -0.4019237886466871523, 8.729914550367427140, -1.499999999999998668 ) ) ;
#189329=CARTESIAN_POINT ( 'NONE',  ( 0.7500000000000006661, 12.11458333401613174, 1.299038105676657340 ) ) ;
#189362=CARTESIAN_POINT ( 'NONE',  ( 0.7500000000000006661, 14.16666666666666785, -1.299038105676657340 ) ) ;
#189367=CARTESIAN_POINT ( 'NONE',  ( 0.6823417656249934904, 10.19270833367473550, 1.181850606188764807 ) ) ;
#189412=CARTESIAN_POINT ( 'NONE',  ( -1.364683531250014514, 11.90104166700806587, -0.7879004041258335089 ) ) ;
#189418=CARTESIAN_POINT ( 'NONE',  ( -1.500000000000008216, 12.28125000068279427, 3.469446951953614189E-15 ) ) ;
#189435=FACE_OUTER_BOUND ( 'NONE', #183346, .T. ) ;
#189441=CARTESIAN_POINT ( 'NONE',  ( -0.6823417656250003738, 13.15104166700806232, 1.181850606188754593 ) ) ;
#189480=CARTESIAN_POINT ( 'NONE',  ( 1.499999999999997113, 14.92708333401612997, -0.8660254037844378194 ) ) ;
#189489=DIRECTION ( 'NONE',  ( 0.000000000000000000, 0.000000000000000000, -1.000000000000000000 ) ) ;
#189512=CARTESIAN_POINT ( 'NONE',  ( -1.364683531250014514, 9.838541667008064096, -0.7879004041258335089 ) ) ;
#189550=B_SPLINE_CURVE_WITH_KNOTS ( 'NONE', 3,
 ( #47421, #165404, #48481, #64703 ),
 .UNSPECIFIED., .F., .F.,
 ( 4, 4 ),
 ( 0.001203384219977627961, 0.001801384605269243855 ),
 .UNSPECIFIED. ) ;
#189579=AXIS2_PLACEMENT_3D ( 'NONE', #26033, #204767, #124702 ) ;
#189658=CARTESIAN_POINT ( 'NONE',  ( -0.6823417656250039265, 10.13020833367472839, -1.181850606188755259 ) ) ;
#189683=CARTESIAN_POINT ( 'NONE',  ( 1.364683531250000303, 14.25520833367473372, -0.7879004041258355073 ) ) ;
#189726=CARTESIAN_POINT ( 'NONE',  ( -0.7500000000000006661, 14.95833333333333748, -1.299038105676657340 ) ) ;
#189772=CARTESIAN_POINT ( 'NONE',  ( -1.402160292154681736E-14, 13.67187500034139447, 1.575800808251682339 ) ) ;
#189809=ADVANCED_FACE ( 'NONE', ( #189435 ), #190486, .T. ) ;
#189875=ORIENTED_EDGE ( 'NONE', *, *, #100966, .F. ) ;
#189918=CARTESIAN_POINT ( 'NONE',  ( -1.364683531250000748, 13.17187500034139980, 0.000000000000000000 ) ) ;
#189951=ORIENTED_EDGE ( 'NONE', *, *, #104977, .F. ) ;
#189977=CARTESIAN_POINT ( 'NONE',  ( 1.364683531250000303, 11.06770833367473550, -0.7879004041258355073 ) ) ;
#190011=CARTESIAN_POINT ( 'NONE',  ( 0.000000000000000000, 13.49999999999999822, -1.500000000000000222 ) ) ;
#190014=CARTESIAN_POINT ( 'NONE',  ( -2.788906526875773208E-15, 11.18749999999999822, -1.499999999999998446 ) ) ;
#190019=CARTESIAN_POINT ( 'NONE',  ( 0.7500000000000006661, 10.69791666734946212, -1.299038105676657340 ) ) ;
#190092=ORIENTED_EDGE ( 'NONE', *, *, #135275, .T. ) ;
#190163=CARTESIAN_POINT ( 'NONE',  ( -8.012344526598182026E-15, 10.29687500034139447, -1.575800808251669460 ) ) ;
#190169=CARTESIAN_POINT ( 'NONE',  ( -1.500000000000015099, 8.979166666666666075, -0.8660254037844309360 ) ) ;
#190212=CARTESIAN_POINT ( 'NONE',  ( 1.836970198721030181E-16, 13.49999999999999822, 1.500000000000000222 ) ) ;
#190224=VERTEX_POINT ( 'NONE', #70069 ) ;
#190228=CARTESIAN_POINT ( 'NONE',  ( -1.364683531250000748, 15.17187500034139447, 0.000000000000000000 ) ) ;
#190323=( BOUNDED_CURVE ( )  B_SPLINE_CURVE ( 2, ( #165447, #31201, #35440, #82059, #167588, #19189, #99394, #130888, #49564 ),
 .UNSPECIFIED., .F., .T. ) 
 B_SPLINE_CURVE_WITH_KNOTS ( ( 3, 2, 2, 2, 3 ),
 ( 0.6517857142857143016, 0.6547619047619047672, 0.6607142857142856984, 0.6666666666666666297, 0.6696428571428570953 ),
 .UNSPECIFIED. ) 
 CURVE ( )  GEOMETRIC_REPRESENTATION_ITEM ( )  RATIONAL_B_SPLINE_CURVE ( ( 0.9330127018922194093, 0.9330127018922194093, 1.000000000000000000, 0.8660254037844387076, 1.000000000000000000, 0.8660254037844387076, 1.000000000000000000, 0.9330127018922206306, 0.9330127018922194093 ) ) 
 REPRESENTATION_ITEM ( '' )  );
#190417=CARTESIAN_POINT ( 'NONE',  ( -0.7500000000000006661, 12.70833333333333570, -1.299038105676657340 ) ) ;
#190423=CARTESIAN_POINT ( 'NONE',  ( 0.6823417656249969321, 11.02604166700806765, -1.181850606188757036 ) ) ;
#190438=B_SPLINE_CURVE_WITH_KNOTS ( 'NONE', 3,
 ( #54695, #204109, #120847, #121917, #6982, #73063, #139162, #56833 ),
 .UNSPECIFIED., .F., .F.,
 ( 4, 2, 2, 4 ),
 ( 2.544396950753999607E-07, 0.0002984430161315527606, 0.0005966315925680303707, 0.001193008745440985808 ),
 .UNSPECIFIED. ) ;
#190464=CARTESIAN_POINT ( 'NONE',  ( -1.364683531250010740, 12.19270833367473195, 0.7879004041258445001 ) ) ;
#190486=CYLINDRICAL_SURFACE ( 'NONE', #199047, 1.500000000000000222 ) ;
#190534=CARTESIAN_POINT ( 'NONE',  ( -1.402160292154681736E-14, 15.09375000068279604, 1.732050807568881190 ) ) ;
#190566=CARTESIAN_POINT ( 'NONE',  ( -0.6823417656250003738, 10.40104166700806587, 1.181850606188754593 ) ) ;
#190691=PLANE ( 'NONE',  #102438 ) ;
#190716=CARTESIAN_POINT ( 'NONE',  ( -8.012344526598182026E-15, 9.359375000341399797, -1.575800808251669460 ) ) ;
#190738=CARTESIAN_POINT ( 'NONE',  ( 1.364683531250000303, 14.75520833367472839, -0.7879004041258355073 ) ) ;
#190758=CARTESIAN_POINT ( 'NONE',  ( -1.115562610750309283E-14, 10.06250000000000000, 1.500000000000001554 ) ) ;
#190784=CARTESIAN_POINT ( 'NONE',  ( 0.7500000000000006661, 15.33333333333333037, 1.299038105676657340 ) ) ;
#190789=DIRECTION ( 'NONE',  ( 0.000000000000000000, -1.000000000000000000, 0.000000000000000000 ) ) ;
#190829=CARTESIAN_POINT ( 'NONE',  ( -0.6823417656250003738, 14.65104166700806410, 1.181850606188754593 ) ) ;
#190860=SURFACE_SIDE_STYLE ('',( #124897 ) ) ;
#190927=ORIENTED_EDGE ( 'NONE', *, *, #60315, .T. ) ;
#190929=( BOUNDED_CURVE ( )  B_SPLINE_CURVE ( 2, ( #74897, #91167, #39191, #138843, #204860, #141006, #208076, #207013, #58644 ),
 .UNSPECIFIED., .F., .T. ) 
 B_SPLINE_CURVE_WITH_KNOTS ( ( 3, 2, 2, 2, 3 ),
 ( 0.7589285714285713969, 0.7619047619047618625, 0.7678571428571429047, 0.7738095238095238360, 0.7767857142857143016 ),
 .UNSPECIFIED. ) 
 CURVE ( )  GEOMETRIC_REPRESENTATION_ITEM ( )  RATIONAL_B_SPLINE_CURVE ( ( 0.9330127018922194093, 0.9330127018922194093, 1.000000000000000000, 0.8660254037844387076, 1.000000000000000000, 0.8660254037844387076, 1.000000000000000000, 0.9330127018922194093, 0.9330127018922194093 ) ) 
 REPRESENTATION_ITEM ( '' )  );
#190945=CARTESIAN_POINT ( 'NONE',  ( 1.315349297999212075, 3.546208118371547258, -0.4023297572127010335 ) ) ;
#190968=CARTESIAN_POINT ( 'NONE',  ( 1.364683531250000303, 13.56770833367473017, -0.7879004041258355073 ) ) ;
#190979=CIRCLE ( 'NONE', #97634, 1.249999999999999778 ) ;
#191004=VERTEX_POINT ( 'NONE', #6710 ) ;
#191014=EDGE_CURVE ( 'NONE', #195805, #66068, #90135, .T. ) ;
#191034=CARTESIAN_POINT ( 'NONE',  ( 0.6823417656249969321, 11.58854166700806765, -1.181850606188757036 ) ) ;
#191073=CARTESIAN_POINT ( 'NONE',  ( -3.602337597214539753E-15, 12.06250000000000178, 1.500000000000001554 ) ) ;
#191075=CARTESIAN_POINT ( 'NONE',  ( 0.7500000000000006661, 11.86458333401613174, 1.299038105676657340 ) ) ;
#191218=CARTESIAN_POINT ( 'NONE',  ( -1.364683531250000748, 10.35937500034139802, 0.000000000000000000 ) ) ;
#191319=EDGE_LOOP ( 'NONE', ( #182476, #149177 ) ) ;
#191341=EDGE_CURVE ( 'NONE', #177076, #139889, #212981, .T. ) ;
#191347=ORIENTED_EDGE ( 'NONE', *, *, #140315, .T. ) ;
#191408=LINE ( 'NONE', #187413, #56651 ) ;
#191419=CARTESIAN_POINT ( 'NONE',  ( -0.4019237886466933696, 9.051335450315374231, 1.500000000000005995 ) ) ;
#191481=CARTESIAN_POINT ( 'NONE',  ( 1.499999999999997113, 12.14583333333333748, -0.8660254037844378194 ) ) ;
#191486=CARTESIAN_POINT ( 'NONE',  ( 1.364683531250000303, 10.25520833367473017, -0.7879004041258355073 ) ) ;
#191499=CARTESIAN_POINT ( 'NONE',  ( -0.7500000000000179856, 10.82291666734946212, 1.299038105676658228 ) ) ;
#191526=CARTESIAN_POINT ( 'NONE',  ( 1.364683531249996529, 12.27604166700805877, 0.7879004041258403923 ) ) ;
#191573=DIRECTION ( 'NONE',  ( 0.000000000000000000, 1.000000000000000000, 0.000000000000000000 ) ) ;
#191595=CARTESIAN_POINT ( 'NONE',  ( 1.500000000000001332, 14.15625000068279604, 0.000000000000000000 ) ) ;
#191603=CARTESIAN_POINT ( 'NONE',  ( 0.000000000000000000, 13.49999999999999822, 0.000000000000000000 ) ) ;
#191627=CARTESIAN_POINT ( 'NONE',  ( 0.6823417656249969321, 9.776041667008065872, -1.181850606188757036 ) ) ;
#191632=CARTESIAN_POINT ( 'NONE',  ( 0.000000000000000000, 13.49999999999999822, -1.500000000000000222 ) ) ;
#191733=DIRECTION ( 'NONE',  ( -0.8660254037844384856, 0.000000000000000000, 0.5000000000000004441 ) ) ;
#191739=B_SPLINE_CURVE_WITH_KNOTS ( 'NONE', 3,
 ( #51944, #32486, #82289, #118067 ),
 .UNSPECIFIED., .F., .F.,
 ( 4, 4 ),
 ( 0.0006045091498275825597, 0.001203384219977627961 ),
 .UNSPECIFIED. ) ;
#191770=CARTESIAN_POINT ( 'NONE',  ( -0.7500000000000179856, 11.79166666666666607, 1.299038105676658228 ) ) ;
#191782=CARTESIAN_POINT ( 'NONE',  ( -1.402160292154681736E-14, 10.23437500034139447, 1.575800808251682339 ) ) ;
#191827=ORIENTED_EDGE ( 'NONE', *, *, #76416, .F. ) ;
#191841=CARTESIAN_POINT ( 'NONE',  ( -1.500000000000001110, 13.05208333401612997, 0.8660254037844418162 ) ) ;
#191849=CARTESIAN_POINT ( 'NONE',  ( -6.009258394948636914E-15, 14.93749999999999822, -1.732050807568875195 ) ) ;
#191892=CARTESIAN_POINT ( 'NONE',  ( -1.402160292154681736E-14, 14.42187500034139980, 1.575800808251682339 ) ) ;
#191903=CARTESIAN_POINT ( 'NONE',  ( -1.430889623655251075, 3.675352821211156140, -0.4691377289697510888 ) ) ;
#191975=CARTESIAN_POINT ( 'NONE',  ( 0.4019237886466816012, 10.17633545031537246, -1.499999999999998668 ) ) ;
#191977=CARTESIAN_POINT ( 'NONE',  ( 1.378881877344245277, 3.612814789602863730, 0.5904953584335879135 ) ) ;
#192008=CARTESIAN_POINT ( 'NONE',  ( 1.476450096886796626, 3.427809906544330598, -0.2781497094537699333 ) ) ;
#192034=CARTESIAN_POINT ( 'NONE',  ( 0.6823417656249969321, 13.08854166700806942, -1.181850606188757036 ) ) ;
#192098=CARTESIAN_POINT ( 'NONE',  ( -1.364683531250010295, 11.44270833367472662, 0.7879004041258445001 ) ) ;
#192142=CARTESIAN_POINT ( 'NONE',  ( -1.402160292154681736E-14, 11.09375000068279249, 1.732050807568881190 ) ) ;
#192144=ORIENTED_EDGE ( 'NONE', *, *, #160757, .F. ) ;
#192263=CARTESIAN_POINT ( 'NONE',  ( -1.425171720896323491, 3.966122586717212073, 0.4907744223921879922 ) ) ;
#192280=CARTESIAN_POINT ( 'NONE',  ( -8.012344526598182026E-15, 10.79687500034139802, -1.575800808251669460 ) ) ;
#192287=CARTESIAN_POINT ( 'NONE',  ( -0.7500000000000006661, 8.958333333333332149, -1.299038105676657340 ) ) ;
#192352=CARTESIAN_POINT ( 'NONE',  ( 0.4019237886466850984, 12.92633545031536713, -1.499999999999996669 ) ) ;
#192465=CARTESIAN_POINT ( 'NONE',  ( -1.115562610750309283E-14, 11.81249999999999822, 1.500000000000001554 ) ) ;
#192547=CARTESIAN_POINT ( 'NONE',  ( 1.500000000000001332, 11.87499999999999645, 0.000000000000000000 ) ) ;
#192552=CARTESIAN_POINT ( 'NONE',  ( 1.364683531250000303, 10.00520833367473017, -0.7879004041258355073 ) ) ;
#192590=CARTESIAN_POINT ( 'NONE',  ( 1.364683531249996529, 11.52604166700806410, 0.7879004041258403923 ) ) ;
#192616=DIRECTION ( 'NONE',  ( 0.000000000000000000, 0.000000000000000000, -1.000000000000000000 ) ) ;
#192660=CARTESIAN_POINT ( 'NONE',  ( -1.500000000000008216, 13.78125000068279604, 3.469446951953614189E-15 ) ) ;
#192671=EDGE_CURVE ( 'NONE', #195556, #166249, #155193, .T. ) ;
#192694=CARTESIAN_POINT ( 'NONE',  ( 1.364683531249997417, 8.734375000341396245, 2.602085213965210642E-15 ) ) ;
#192845=CARTESIAN_POINT ( 'NONE',  ( -1.364683531250014514, 9.401041667008062319, -0.7879004041258335089 ) ) ;
#192918=CARTESIAN_POINT ( 'NONE',  ( 1.500000000000001332, 15.12500000000000000, 0.000000000000000000 ) ) ;
#192929=ORIENTED_EDGE ( 'NONE', *, *, #104082, .T. ) ;
#192963=CARTESIAN_POINT ( 'NONE',  ( -1.364683531250014514, 13.08854166700806410, -0.7879004041258335089 ) ) ;
#192975=CARTESIAN_POINT ( 'NONE',  ( -1.369796495953883531, 4.288649915869804374, 0.2487645435796815019 ) ) ;
#193012=ORIENTED_EDGE ( 'NONE', *, *, #120622, .F. ) ;
#193016=EDGE_CURVE ( 'NONE', #48301, #210699, #197804, .T. ) ;
#193030=FACE_BOUND ( 'NONE', #69600, .T. ) ;
#193052=VERTEX_POINT ( 'NONE', #69673 ) ;
#193067=CARTESIAN_POINT ( 'NONE',  ( -1.492698588115513703, 3.265477196593705056, -0.1666886929329597367 ) ) ;
#193091=CARTESIAN_POINT ( 'NONE',  ( 1.378728738066228754, 4.086408449757453099, -0.5908528300941744416 ) ) ;
#193116=CARTESIAN_POINT ( 'NONE',  ( -0.6823417656250003738, 13.71354166700806942, 1.181850606188754593 ) ) ;
#193126=DIRECTION ( 'NONE',  ( 0.000000000000000000, 0.000000000000000000, -1.000000000000000000 ) ) ;
#193159=ORIENTED_EDGE ( 'NONE', *, *, #71115, .T. ) ;
#193181=CARTESIAN_POINT ( 'NONE',  ( 1.364683531250000303, 12.31770833367473195, -0.7879004041258355073 ) ) ;
#193209=CARTESIAN_POINT ( 'NONE',  ( -1.364683531250000748, 8.421875000341403350, 0.000000000000000000 ) ) ;
#193214=CARTESIAN_POINT ( 'NONE',  ( -2.788906526875773208E-15, 9.218750000682799595, -1.499999999999998446 ) ) ;
#193227=CARTESIAN_POINT ( 'NONE',  ( 1.499999999999997113, 10.92708333401613530, -0.8660254037844378194 ) ) ;
#193229=ORIENTED_EDGE ( 'NONE', *, *, #154961, .F. ) ;
#193236=CARTESIAN_POINT ( 'NONE',  ( 0.4019237886466816012, 10.20758545099816850, -1.499999999999998668 ) ) ;
#193279=PLANE ( 'NONE',  #140366 ) ;
#193348=CARTESIAN_POINT ( 'NONE',  ( -1.493068410184935635, 3.264629715075684668, -0.1642227666888320947 ) ) ;
#193366=CARTESIAN_POINT ( 'NONE',  ( 1.364683531249996529, 9.213541667008062319, 0.7879004041258403923 ) ) ;
#193380=DIRECTION ( 'NONE',  ( 0.000000000000000000, 0.000000000000000000, -1.000000000000000000 ) ) ;
#193393=AXIS2_PLACEMENT_3D ( 'NONE', #6035, #207459, #41795 ) ;
#193400=( BOUNDED_CURVE ( )  B_SPLINE_CURVE ( 2, ( #114113, #29592, #212584, #98859, #148673, #177977, #163864, #82586, #241 ),
 .UNSPECIFIED., .F., .T. ) 
 B_SPLINE_CURVE_WITH_KNOTS ( ( 3, 2, 2, 2, 3 ),
 ( 0.4910714285714285476, 0.4940476190476190688, 0.5000000000000000000, 0.5059523809523809312, 0.5089285714285713969 ),
 .UNSPECIFIED. ) 
 CURVE ( )  GEOMETRIC_REPRESENTATION_ITEM ( )  RATIONAL_B_SPLINE_CURVE ( ( 0.9330127018922194093, 0.9330127018922187432, 1.000000000000000000, 0.8660254037844387076, 1.000000000000000000, 0.8660254037844387076, 1.000000000000000000, 0.9330127018922194093, 0.9330127018922194093 ) ) 
 REPRESENTATION_ITEM ( '' )  );
#193568=CARTESIAN_POINT ( 'NONE',  ( -1.500000000000015099, 8.979166666666666075, -0.8660254037844309360 ) ) ;
#193586=CARTESIAN_POINT ( 'NONE',  ( -1.500000000000008216, 10.49999999999999467, 3.469446951953614189E-15 ) ) ;
#193625=CARTESIAN_POINT ( 'NONE',  ( 1.499999999999997113, 11.89583333333333570, -0.8660254037844378194 ) ) ;
#193630=CARTESIAN_POINT ( 'NONE',  ( -1.364683531250000748, 9.359375000341396245, 0.000000000000000000 ) ) ;
#193638=CARTESIAN_POINT ( 'NONE',  ( -0.6499422464084805284, 3.350075079687096391, -0.06926476342541870723 ) ) ;
#193667=CARTESIAN_POINT ( 'NONE',  ( -1.364683531250000748, 12.17187500034139980, 0.000000000000000000 ) ) ;
#193715=ORIENTED_EDGE ( 'NONE', *, *, #54197, .T. ) ;
#193737=CARTESIAN_POINT ( 'NONE',  ( -1.500000000000001110, 13.30208333401612997, 0.8660254037844419273 ) ) ;
#193771=CARTESIAN_POINT ( 'NONE',  ( -1.402160292154681736E-14, 8.671875000341403350, 1.575800808251682339 ) ) ;
#193782=DIRECTION ( 'NONE',  ( 0.000000000000000000, 1.000000000000000000, 0.000000000000000000 ) ) ;
#193908=CARTESIAN_POINT ( 'NONE',  ( 0.7500000000000006661, 10.44791666734946212, -1.299038105676657340 ) ) ;
#193922=CARTESIAN_POINT ( 'NONE',  ( -8.012344526598182026E-15, 9.109375000341398021, -1.575800808251669460 ) ) ;
#193950=CARTESIAN_POINT ( 'NONE',  ( 1.499999999999993117, 11.60416666666666607, 0.8660254037844408170 ) ) ;
#194013=CARTESIAN_POINT ( 'NONE',  ( 1.499999999999996891, 11.14583333333333215, -0.8660254037844378194 ) ) ;
#194033=CARTESIAN_POINT ( 'NONE',  ( 1.364683531249996529, 13.46354166700806765, 0.7879004041258405033 ) ) ;
#194131=DIRECTION ( 'NONE',  ( 0.000000000000000000, 1.000000000000000000, 0.000000000000000000 ) ) ;
#194138=EDGE_CURVE ( 'NONE', #102754, #179825, #173366, .T. ) ;
#194159=CARTESIAN_POINT ( 'NONE',  ( 1.355680771150860275, 3.935647470828122607, -0.6419739358886640268 ) ) ;
#194184=CARTESIAN_POINT ( 'NONE',  ( -1.364683531250010295, 13.19270833367472839, 0.7879004041258445001 ) ) ;
#194208=LINE ( 'NONE', #45853, #114686 ) ;
#194249=CARTESIAN_POINT ( 'NONE',  ( -0.6823417656250039265, 11.13020833367473017, -1.181850606188755259 ) ) ;
#194293=CARTESIAN_POINT ( 'NONE',  ( -1.500000000000001110, 10.30208333401613352, 0.8660254037844419273 ) ) ;
#194295=VERTEX_POINT ( 'NONE', #187457 ) ;
#194414=CARTESIAN_POINT ( 'NONE',  ( -1.286813488861816790, 3.652992958535466794, -0.4595522011843584109 ) ) ;
#194433=CARTESIAN_POINT ( 'NONE',  ( -1.364683531250000748, 9.859375000341398021, 0.000000000000000000 ) ) ;
#194456=ORIENTED_EDGE ( 'NONE', *, *, #105563, .T. ) ;
#194488=ORIENTED_EDGE ( 'NONE', *, *, #47895, .F. ) ;
#194489=ADVANCED_FACE ( 'NONE', ( #172970 ), #205435, .F. ) ;
#194691=CARTESIAN_POINT ( 'NONE',  ( -1.500000000000001110, 12.52083333333333037, 0.8660254037844419273 ) ) ;
#194697=CARTESIAN_POINT ( 'NONE',  ( -8.012344526598182026E-15, 9.546875000341399797, -1.575800808251669460 ) ) ;
#194733=CARTESIAN_POINT ( 'NONE',  ( -1.364683531250010740, 10.94270833367473372, 0.7879004041258445001 ) ) ;
#194736=( BOUNDED_CURVE ( )  B_SPLINE_CURVE ( 2, ( #77177, #110818, #145438, #211438, #63070, #129238, #176824, #142223, #112961 ),
 .UNSPECIFIED., .F., .T. ) 
 B_SPLINE_CURVE_WITH_KNOTS ( ( 3, 2, 2, 2, 3 ),
 ( 0.4553571428571427937, 0.4583333333333333148, 0.4642857142857143016, 0.4702380952380952328, 0.4732142857142856984 ),
 .UNSPECIFIED. ) 
 CURVE ( )  GEOMETRIC_REPRESENTATION_ITEM ( )  RATIONAL_B_SPLINE_CURVE ( ( 0.9330127018922194093, 0.9330127018922180770, 1.000000000000000000, 0.8660254037844387076, 1.000000000000000000, 0.8660254037844387076, 1.000000000000000000, 0.9330127018922194093, 0.9330127018922194093 ) ) 
 REPRESENTATION_ITEM ( '' )  );
#194806=CARTESIAN_POINT ( 'NONE',  ( 0.7500000000000006661, 13.69791666734946567, -1.299038105676657340 ) ) ;
#194837=CARTESIAN_POINT ( 'NONE',  ( 3.834746474454188013E-15, 8.593750000682796042, 1.500000000000001554 ) ) ;
#194839=VECTOR ( 'NONE', #193782, 1000.000000000000000 ) ;
#194842=CARTESIAN_POINT ( 'NONE',  ( 0.6823417656249934904, 9.192708333674733723, 1.181850606188764807 ) ) ;
#194995=CARTESIAN_POINT ( 'NONE',  ( -1.364683531250000748, 8.921875000341403350, 0.000000000000000000 ) ) ;
#195006=ORIENTED_EDGE ( 'NONE', *, *, #107076, .F. ) ;
#195007=CARTESIAN_POINT ( 'NONE',  ( -0.7500000000000006661, 9.458333333333332149, -1.299038105676657340 ) ) ;
#195020=CARTESIAN_POINT ( 'NONE',  ( 1.499999999999996891, 9.145833333333330373, -0.8660254037844378194 ) ) ;
#195114=CARTESIAN_POINT ( 'NONE',  ( 1.364683531249997417, 12.73437500034139980, 2.602085213965210642E-15 ) ) ;
#195238=DIRECTION ( 'NONE',  ( 0.000000000000000000, -1.000000000000000000, 0.000000000000000000 ) ) ;
#195251=EDGE_CURVE ( 'NONE', #47534, #29614, #107765, .T. ) ;
#195265=CARTESIAN_POINT ( 'NONE',  ( -1.364683531250014514, 12.15104166700806765, -0.7879004041258335089 ) ) ;
#195329=CARTESIAN_POINT ( 'NONE',  ( 0.6823417656249934904, 9.755208333674728394, 1.181850606188764807 ) ) ;
#195370=CARTESIAN_POINT ( 'NONE',  ( -0.7500000000000179856, 9.572916667349467446, 1.299038105676658228 ) ) ;
#195426=CARTESIAN_POINT ( 'NONE',  ( -0.5727075793229210454, 4.245792387587058236, -0.3118784721225407730 ) ) ;
#195458=ORIENTED_EDGE ( 'NONE', *, *, #141409, .T. ) ;
#195492=CARTESIAN_POINT ( 'NONE',  ( -1.494007359806937441, 3.367954574834560511, 0.1499524099051025572 ) ) ;
#195509=CARTESIAN_POINT ( 'NONE',  ( -8.012344526598182026E-15, 9.796875000341399797, -1.575800808251669460 ) ) ;
#195526=ORIENTED_EDGE ( 'NONE', *, *, #51634, .F. ) ;
#195556=VERTEX_POINT ( 'NONE', #193209 ) ;
#195584=CARTESIAN_POINT ( 'NONE',  ( 1.364683531250000303, 14.81770833367472839, -0.7879004041258355073 ) ) ;
#195741=CARTESIAN_POINT ( 'NONE',  ( -0.4019237886466837106, 12.94866454968462754, -1.500000000000000666 ) ) ;
#195768=CARTESIAN_POINT ( 'NONE',  ( 1.499999999999997113, 11.14583333333333215, -0.8660254037844378194 ) ) ;
#195773=CARTESIAN_POINT ( 'NONE',  ( -1.364683531250000748, 9.609375000341396245, 0.000000000000000000 ) ) ;
#195782=CARTESIAN_POINT ( 'NONE',  ( -0.5149768381150839902, 3.543642475881736864, -0.4000488691750889725 ) ) ;
#195805=VERTEX_POINT ( 'NONE', #183354 ) ;
#195810=CARTESIAN_POINT ( 'NONE',  ( 1.364683531250000748, 10.31770833367472839, -0.7879004041258355073 ) ) ;
#195811=ORIENTED_EDGE ( 'NONE', *, *, #162651, .T. ) ;
#195848=CARTESIAN_POINT ( 'NONE',  ( -1.500000000000015099, 9.979166666666671404, -0.8660254037844309360 ) ) ;
#195883=CARTESIAN_POINT ( 'NONE',  ( -1.500000000000001110, 13.55208333401613174, 0.8660254037844419273 ) ) ;
#195919=B_SPLINE_CURVE_WITH_KNOTS ( 'NONE', 3,
 ( #214390, #49807, #163575, #149442, #99626, #130080, #148389, #112752, #197119, #15158 ),
 .UNSPECIFIED., .F., .F.,
 ( 4, 2, 2, 2, 4 ),
 ( 2.539054641909564890E-15, 0.0005184205841295809816, 0.001036841168256622762, 0.001555261752383664759, 0.002073682336510707189 ),
 .UNSPECIFIED. ) ;
#195921=CARTESIAN_POINT ( 'NONE',  ( 0.6823417656249934904, 8.442708333674733723, 1.181850606188764807 ) ) ;
#195969=EDGE_LOOP ( 'NONE', ( #195006, #22289, #167828, #12059 ) ) ;
#195982=DIRECTION ( 'NONE',  ( 0.000000000000000000, 1.000000000000000000, 0.000000000000000000 ) ) ;
#196028=DIRECTION ( 'NONE',  ( 0.000000000000000000, 0.000000000000000000, -1.000000000000000000 ) ) ;
#196031=CARTESIAN_POINT ( 'NONE',  ( 1.364683531250000748, 12.25520833367473195, -0.7879004041258355073 ) ) ;
#196032=( BOUNDED_CURVE ( )  B_SPLINE_CURVE ( 2, ( #94527, #191975, #43642, #28434, #47918, #130283, #208231, #129233, #78245 ),
 .UNSPECIFIED., .F., .T. ) 
 B_SPLINE_CURVE_WITH_KNOTS ( ( 3, 2, 2, 2, 3 ),
 ( 0.7589285714285713969, 0.7619047619047618625, 0.7678571428571429047, 0.7738095238095238360, 0.7767857142857143016 ),
 .UNSPECIFIED. ) 
 CURVE ( )  GEOMETRIC_REPRESENTATION_ITEM ( )  RATIONAL_B_SPLINE_CURVE ( ( 0.9330127018922194093, 0.9330127018922194093, 1.000000000000000000, 0.8660254037844387076, 1.000000000000000000, 0.8660254037844387076, 1.000000000000000000, 0.9330127018922194093, 0.9330127018922194093 ) ) 
 REPRESENTATION_ITEM ( '' )  );
#196068=EDGE_CURVE ( 'NONE', #91043, #131458, #73177, .T. ) ;
#196075=CARTESIAN_POINT ( 'NONE',  ( -1.364683531250010295, 8.942708333674731946, 0.7879004041258445001 ) ) ;
#196081=CARTESIAN_POINT ( 'NONE',  ( -1.505691858957076246, 13.24428365067345403, -0.1501137743024005267 ) ) ;
#196101=CARTESIAN_POINT ( 'NONE',  ( 1.455305287003863635, 4.347738815597921302, -0.3947446046151246724 ) ) ;
#196127=CARTESIAN_POINT ( 'NONE',  ( 1.500000000000001332, 11.37499999999999645, 0.000000000000000000 ) ) ;
#196182=CARTESIAN_POINT ( 'NONE',  ( -1.364683531250010295, 12.63020833367473372, 0.7879004041258445001 ) ) ;
#196194=CARTESIAN_POINT ( 'NONE',  ( -1.464648953335778270, 4.228397023187225656, -0.3340396966001182300 ) ) ;
#196239=ORIENTED_EDGE ( 'NONE', *, *, #5890, .T. ) ;
#196329=CARTESIAN_POINT ( 'NONE',  ( -8.012344526598182026E-15, 12.35937500034139624, -1.575800808251669460 ) ) ;
#196393=CARTESIAN_POINT ( 'NONE',  ( -1.364683531250010295, 9.942708333674728394, 0.7879004041258445001 ) ) ;
#196434=CARTESIAN_POINT ( 'NONE',  ( 1.500000000000001332, 10.15625000068279249, 0.000000000000000000 ) ) ;
#196436=ORIENTED_EDGE ( 'NONE', *, *, #165975, .T. ) ;
#196487=CARTESIAN_POINT ( 'NONE',  ( -1.264911064067348656, 3.850000000000018296, 0.5000000000000064393 ) ) ;
#196503=CARTESIAN_POINT ( 'NONE',  ( 1.249999999999997558, -0.5000000000000004441, 1.734723475976807094E-15 ) ) ;
#196573=CARTESIAN_POINT ( 'NONE',  ( -8.012344526598182026E-15, 9.546875000341396245, -1.575800808251669460 ) ) ;
#196644=CARTESIAN_POINT ( 'NONE',  ( -0.6823417656250003738, 14.96354166700806410, 1.181850606188754593 ) ) ;
#196686=VERTEX_POINT ( 'NONE', #125134 ) ;
#196826=CARTESIAN_POINT ( 'NONE',  ( 0.7500000000000006661, 11.33333333333333393, 1.299038105676657340 ) ) ;
#196831=CARTESIAN_POINT ( 'NONE',  ( 1.364683531250000303, 9.005208333674731946, -0.7879004041258355073 ) ) ;
#196842=CARTESIAN_POINT ( 'NONE',  ( 0.000000000000000000, -2.500000000000002220, 0.000000000000000000 ) ) ;
#196867=CARTESIAN_POINT ( 'NONE',  ( 0.6823417656249934904, 11.00520833367472839, 1.181850606188764807 ) ) ;
#196894=DIRECTION ( 'NONE',  ( 0.000000000000000000, -1.000000000000000000, 0.000000000000000000 ) ) ;
#196939=CARTESIAN_POINT ( 'NONE',  ( -6.009258394948636914E-15, 12.46875000068279959, -1.732050807568875195 ) ) ;
#196973=CARTESIAN_POINT ( 'NONE',  ( 1.364683531250000303, 9.255208333674733723, -0.7879004041258355073 ) ) ;
#197031=( GEOMETRIC_REPRESENTATION_CONTEXT ( 3 ) GLOBAL_UNCERTAINTY_ASSIGNED_CONTEXT ( ( #139483 ) ) GLOBAL_UNIT_ASSIGNED_CONTEXT ( ( #111266, #210816, #113403 ) ) REPRESENTATION_CONTEXT ( 'NONE', 'WORKASPACE' ) );
#197088=ORIENTED_EDGE ( 'NONE', *, *, #60315, .F. ) ;
#197119=CARTESIAN_POINT ( 'NONE',  ( -0.9215813951549834959, 13.25030900364159336, -1.183391796694308828 ) ) ;
#197173=CARTESIAN_POINT ( 'NONE',  ( 1.220146605508150803E-14, 11.43749999999999822, -1.499999999999998446 ) ) ;
#197211=CARTESIAN_POINT ( 'NONE',  ( -2.788906526875773208E-15, 11.18749999999999822, -1.499999999999998446 ) ) ;
#197218=CARTESIAN_POINT ( 'NONE',  ( 0.5151702941667745117, 4.156692335018007611, 0.3998358608512675438 ) ) ;
#197227=CARTESIAN_POINT ( 'NONE',  ( -1.402160292154681736E-14, 12.92187500034139980, 1.575800808251682339 ) ) ;
#197291=CARTESIAN_POINT ( 'NONE',  ( -0.5773502691896261751, -4.295408888568413630, -0.9999999999999991118 ) ) ;
#197377=CARTESIAN_POINT ( 'NONE',  ( -0.6823417656250039265, 12.63020833367473017, -1.181850606188755259 ) ) ;
#197442=CARTESIAN_POINT ( 'NONE',  ( 1.364683531250000303, 10.06770833367473017, -0.7879004041258355073 ) ) ;
#197484=CARTESIAN_POINT ( 'NONE',  ( 1.499999999999993117, 9.385416667349465669, 0.8660254037844409281 ) ) ;
#197559=EDGE_LOOP ( 'NONE', ( #158796, #96512, #110531, #43846 ) ) ;
#197620=CARTESIAN_POINT ( 'NONE',  ( 1.364683531249996529, 9.963541667008064096, 0.7879004041258403923 ) ) ;
#197690=CARTESIAN_POINT ( 'NONE',  ( 1.364683531250000303, 14.56770833367473372, -0.7879004041258355073 ) ) ;
#197701=DIRECTION ( 'NONE',  ( 0.000000000000000000, -1.000000000000000000, 0.000000000000000000 ) ) ;
#197751=CARTESIAN_POINT ( 'NONE',  ( 3.834746474454188013E-15, 8.593750000682796042, 1.500000000000001554 ) ) ;
#197804=( BOUNDED_CURVE ( )  B_SPLINE_CURVE ( 2, ( #20917, #87012, #134729, #200736, #3596, #52386, #137916, #118514, #85952 ),
 .UNSPECIFIED., .F., .T. ) 
 B_SPLINE_CURVE_WITH_KNOTS ( ( 3, 2, 2, 2, 3 ),
 ( 0.6875000000000000000, 0.6904761904761904656, 0.6964285714285713969, 0.7023809523809523281, 0.7053571428571427937 ),
 .UNSPECIFIED. ) 
 CURVE ( )  GEOMETRIC_REPRESENTATION_ITEM ( )  RATIONAL_B_SPLINE_CURVE ( ( 0.9330127018922194093, 0.9330127018922194093, 1.000000000000000000, 0.8660254037844387076, 1.000000000000000000, 0.8660254037844387076, 1.000000000000000000, 0.9330127018922206306, 0.9330127018922194093 ) ) 
 REPRESENTATION_ITEM ( '' )  );
#197850=CARTESIAN_POINT ( 'NONE',  ( 3.834746474454188013E-15, 13.06250000000000178, 1.500000000000001554 ) ) ;
#197880=CARTESIAN_POINT ( 'NONE',  ( 1.499999999999993117, 11.60416666666666252, 0.8660254037844409281 ) ) ;
#197883=( BOUNDED_CURVE ( )  B_SPLINE_CURVE ( 2, ( #151273, #198916, #114569, #50562, #116683, #34303, #100376, #166446, #18038 ),
 .UNSPECIFIED., .F., .T. ) 
 B_SPLINE_CURVE_WITH_KNOTS ( ( 3, 2, 2, 2, 3 ),
 ( 0.2946428571428571508, 0.2976190476190476164, 0.3035714285714285476, 0.3095238095238095344, 0.3124999999999999445 ),
 .UNSPECIFIED. ) 
 CURVE ( )  GEOMETRIC_REPRESENTATION_ITEM ( )  RATIONAL_B_SPLINE_CURVE ( ( 0.9330127018922194093, 0.9330127018922194093, 1.000000000000000000, 0.8660254037844387076, 1.000000000000000000, 0.8660254037844387076, 1.000000000000000000, 0.9330127018922206306, 0.9330127018922194093 ) ) 
 REPRESENTATION_ITEM ( '' )  );
#197885=CARTESIAN_POINT ( 'NONE',  ( -1.402160292154681736E-14, 9.671875000341399797, 1.575800808251682339 ) ) ;
#197921=CARTESIAN_POINT ( 'NONE',  ( 1.364683531249997417, 10.04687500034139802, 2.602085213965210642E-15 ) ) ;
#197981=LINE ( 'NONE', #115734, #51668 ) ;
#197998=CARTESIAN_POINT ( 'NONE',  ( -1.500000000000015099, 12.26041666734946212, -0.8660254037844309360 ) ) ;
#198025=AXIS2_PLACEMENT_3D ( 'NONE', #52679, #153386, #170694 ) ;
#198065=EDGE_CURVE ( 'NONE', #177076, #96508, #214193, .T. ) ;
#198074=CARTESIAN_POINT ( 'NONE',  ( 1.378881877344245277, 3.612814789602863730, 0.5904953584335879135 ) ) ;
#198149=DIRECTION ( 'NONE',  ( 0.000000000000000000, 0.000000000000000000, 1.000000000000000000 ) ) ;
#198174=CARTESIAN_POINT ( 'NONE',  ( -1.364683531250014514, 8.651041667008065872, -0.7879004041258335089 ) ) ;
#198218=CARTESIAN_POINT ( 'NONE',  ( 0.4019237886466816012, 10.70758545099816672, -1.499999999999998668 ) ) ;
#198282=CARTESIAN_POINT ( 'NONE',  ( -1.402160292154681736E-14, 11.17187500034139802, 1.575800808251682339 ) ) ;
#198299=ORIENTED_EDGE ( 'NONE', *, *, #140470, .T. ) ;
#198431=CARTESIAN_POINT ( 'NONE',  ( -0.6823417656250039265, 12.13020833367473017, -1.181850606188755259 ) ) ;
#198482=CARTESIAN_POINT ( 'NONE',  ( -8.012344526598182026E-15, 13.29687500034139980, -1.575800808251669460 ) ) ;
#198487=CARTESIAN_POINT ( 'NONE',  ( 0.000000000000000000, 14.00000000000000533, 0.000000000000000000 ) ) ;
#198494=CARTESIAN_POINT ( 'NONE',  ( -1.364683531250014514, 10.40104166700806765, -0.7879004041258335089 ) ) ;
#198536=CARTESIAN_POINT ( 'NONE',  ( -1.500000000000015099, 10.01041666734946745, -0.8660254037844309360 ) ) ;
#198614=CARTESIAN_POINT ( 'NONE',  ( -1.500000000000008216, 12.78125000068279427, 3.469446951953614189E-15 ) ) ;
#198633=DIRECTION ( 'NONE',  ( 0.000000000000000000, 1.000000000000000000, 0.000000000000000000 ) ) ;
#198635=CARTESIAN_POINT ( 'NONE',  ( -0.4019237886467001974, 9.301335450315374231, 1.500000000000001998 ) ) ;
#198639=CARTESIAN_POINT ( 'NONE',  ( 0.7500000000000006661, 9.447916667349467446, -1.299038105676657340 ) ) ;
#198672=APPLICATION_CONTEXT ( 'automotive_design' ) ;
#198729=LINE ( 'NONE', #152144, #75586 ) ;
#198741=CARTESIAN_POINT ( 'NONE',  ( -1.364683531250010295, 13.94270833367473195, 0.7879004041258445001 ) ) ;
#198820=PRODUCT_CONTEXT ( 'NONE', #168032, 'mechanical' ) ;
#198852=CARTESIAN_POINT ( 'NONE',  ( -2.788906526875773208E-15, 12.96875000068279782, -1.499999999999998446 ) ) ;
#198916=CARTESIAN_POINT ( 'NONE',  ( 0.4019237886466816012, 13.20758545099816672, -1.499999999999998668 ) ) ;
#198928=CARTESIAN_POINT ( 'NONE',  ( -1.402160292154681736E-14, 10.81250000000000355, 1.732050807568881190 ) ) ;
#198934=CARTESIAN_POINT ( 'NONE',  ( 1.364683531250000303, 14.81770833367472839, -0.7879004041258355073 ) ) ;
#198974=CARTESIAN_POINT ( 'NONE',  ( -1.364683531250000748, 10.42187500034139802, 0.000000000000000000 ) ) ;
#199046=CARTESIAN_POINT ( 'NONE',  ( 1.499999999999997113, 12.92708333401612819, -0.8660254037844378194 ) ) ;
#199047=AXIS2_PLACEMENT_3D ( 'NONE', #25855, #10666, #192616 ) ;
#199049=ORIENTED_EDGE ( 'NONE', *, *, #46016, .F. ) ;
#199057=CARTESIAN_POINT ( 'NONE',  ( -0.4019237886466966447, 12.80133545031536890, 1.500000000000003997 ) ) ;
#199085=ORIENTED_EDGE ( 'NONE', *, *, #17820, .F. ) ;
#199137=CARTESIAN_POINT ( 'NONE',  ( 1.364683531250000303, 13.25520833367472839, -0.7879004041258355073 ) ) ;
#199190=CARTESIAN_POINT ( 'NONE',  ( -0.6823417656250039265, 12.06770833367473017, -1.181850606188755259 ) ) ;
#199200=EDGE_CURVE ( 'NONE', #137942, #78671, #37135, .T. ) ;
#199223=FACE_OUTER_BOUND ( 'NONE', #116061, .T. ) ;
#199334=CARTESIAN_POINT ( 'NONE',  ( 0.4153311931458959494, 3.850000000000006306, 0.5000000000000064393 ) ) ;
#199343=CARTESIAN_POINT ( 'NONE',  ( 1.364683531249996529, 11.21354166700806232, 0.7879004041258405033 ) ) ;
#199438=ORIENTED_EDGE ( 'NONE', *, *, #155474, .F. ) ;
#199495=CARTESIAN_POINT ( 'NONE',  ( 1.364683531249997417, 11.79687500034139802, 2.602085213965210642E-15 ) ) ;
#199528=EDGE_CURVE ( 'NONE', #111937, #29485, #9291, .T. ) ;
#199550=CARTESIAN_POINT ( 'NONE',  ( 1.364683531249997417, 13.23437500034139980, 2.602085213965210642E-15 ) ) ;
#199554=FACE_OUTER_BOUND ( 'NONE', #213892, .T. ) ;
#199564=CARTESIAN_POINT ( 'NONE',  ( -1.364683531250014514, 10.65104166700806942, -0.7879004041258335089 ) ) ;
#199606=CARTESIAN_POINT ( 'NONE',  ( -6.009258394948636914E-15, 8.968750000682799595, -1.732050807568875195 ) ) ;
#199670=DIRECTION ( 'NONE',  ( 0.000000000000000000, -1.000000000000000000, 0.000000000000000000 ) ) ;
#199746=CARTESIAN_POINT ( 'NONE',  ( -1.364683531250010740, 8.380208333674730170, 0.7879004041258445001 ) ) ;
#199816=CARTESIAN_POINT ( 'NONE',  ( -8.012344526598182026E-15, 13.85937500034139447, -1.575800808251669460 ) ) ;
#199899=VECTOR ( 'NONE', #40981, 1000.000000000000227 ) ;
#200001=CARTESIAN_POINT ( 'NONE',  ( -1.364683531250000748, 12.35937500034139980, 0.000000000000000000 ) ) ;
#200007=CARTESIAN_POINT ( 'NONE',  ( 0.7500000000000006661, 9.333333333333332149, 1.299038105676657340 ) ) ;
#200055=CARTESIAN_POINT ( 'NONE',  ( -1.364683531250014514, 9.651041667008064096, -0.7879004041258335089 ) ) ;
#200103=CARTESIAN_POINT ( 'NONE',  ( -1.115562610750309283E-14, 11.59375000068279604, 1.500000000000001554 ) ) ;
#200125=CARTESIAN_POINT ( 'NONE',  ( -0.7500000000000006661, 12.23958333401613174, -1.299038105676657340 ) ) ;
#200211=CARTESIAN_POINT ( 'NONE',  ( -0.6823417656250039265, 13.81770833367473195, -1.181850606188755259 ) ) ;
#200263=CARTESIAN_POINT ( 'NONE',  ( 0.6823417656249934904, 11.69270833367473017, 1.181850606188764807 ) ) ;
#200298=DIRECTION ( 'NONE',  ( 0.000000000000000000, -1.000000000000000000, 0.000000000000000000 ) ) ;
#200399=CARTESIAN_POINT ( 'NONE',  ( 0.5993518605652721210, 4.282474605821112057, -0.2595036419143193496 ) ) ;
#200406=( BOUNDED_CURVE ( )  B_SPLINE_CURVE ( 2, ( #188358, #23722, #134328, #71392, #102860, #152671, #135375, #137504, #168917 ),
 .UNSPECIFIED., .F., .T. ) 
 B_SPLINE_CURVE_WITH_KNOTS ( ( 3, 2, 2, 2, 3 ),
 ( 0.7410714285714286031, 0.7440476190476190688, 0.7500000000000000000, 0.7559523809523809312, 0.7589285714285713969 ),
 .UNSPECIFIED. ) 
 CURVE ( )  GEOMETRIC_REPRESENTATION_ITEM ( )  RATIONAL_B_SPLINE_CURVE ( ( 0.9330127018922194093, 0.9330127018922194093, 1.000000000000000000, 0.8660254037844387076, 1.000000000000000000, 0.8660254037844387076, 1.000000000000000000, 0.9330127018922194093, 0.9330127018922194093 ) ) 
 REPRESENTATION_ITEM ( '' )  );
#200407=AXIS2_PLACEMENT_3D ( 'NONE', #95216, #132002, #161266 ) ;
#200410=CARTESIAN_POINT ( 'NONE',  ( 1.364683531249996529, 11.71354166700806587, 0.7879004041258405033 ) ) ;
#200429=EDGE_LOOP ( 'NONE', ( #108680, #165176, #158535, #146874, #122543 ) ) ;
#200440=CARTESIAN_POINT ( 'NONE',  ( 1.371478227464764998, 13.33154996480476484, -0.3356224383821780899 ) ) ;
#200449=CARTESIAN_POINT ( 'NONE',  ( 0.5773502691896124084, -4.295408888568413630, -0.9999999999999991118 ) ) ;
#200557=CARTESIAN_POINT ( 'NONE',  ( 0.6823417656249969321, 11.58854166700806765, -1.181850606188757036 ) ) ;
#200623=CARTESIAN_POINT ( 'NONE',  ( 1.364683531249997417, 9.046875000341403350, 2.602085213965210642E-15 ) ) ;
#200663=CARTESIAN_POINT ( 'NONE',  ( 0.7500000000000006661, 8.697916667349467446, -1.299038105676657340 ) ) ;
#200728=DIRECTION ( 'NONE',  ( 0.000000000000000000, 0.000000000000000000, -1.000000000000000000 ) ) ;
#200736=CARTESIAN_POINT ( 'NONE',  ( 1.499999999999996891, 10.64583333333333037, -0.8660254037844378194 ) ) ;
#200851=DIRECTION ( 'NONE',  ( 0.000000000000000000, -1.000000000000000000, 0.000000000000000000 ) ) ;
#200854=CARTESIAN_POINT ( 'NONE',  ( -0.4019237886466933696, 8.801335450315374231, 1.500000000000005995 ) ) ;
#200869=CARTESIAN_POINT ( 'NONE',  ( 1.364683531249997417, 13.54687500034139980, 2.602085213965210642E-15 ) ) ;
#200943=SHAPE_DEFINITION_REPRESENTATION ( #142260, #137092 ) ;
#201057=CARTESIAN_POINT ( 'NONE',  ( -1.364683531250000748, 12.60937500034139980, 0.000000000000000000 ) ) ;
#201062=CARTESIAN_POINT ( 'NONE',  ( 1.500000000000001332, 9.125000000000001776, 0.000000000000000000 ) ) ;
#201111=CARTESIAN_POINT ( 'NONE',  ( 1.364683531249997417, 9.546875000341396245, 2.602085213965210642E-15 ) ) ;
#201128=CARTESIAN_POINT ( 'NONE',  ( -0.7500000000000179856, 12.57291666734946389, 1.299038105676658228 ) ) ;
#201173=CARTESIAN_POINT ( 'NONE',  ( -1.500000000000001110, 9.302083334016128191, 0.8660254037844418162 ) ) ;
#201186=CARTESIAN_POINT ( 'NONE',  ( -1.500000000000008216, 12.78125000068279427, 3.469446951953614189E-15 ) ) ;
#201234=CARTESIAN_POINT ( 'NONE',  ( -0.4019237886466802689, 11.22991455036742714, -1.500000000000002887 ) ) ;
#201258=CARTESIAN_POINT ( 'NONE',  ( 1.500085555261172932, 3.249813679204478056, -0.08157497973214339337 ) ) ;
#201260=DIRECTION ( 'NONE',  ( 0.000000000000000000, -1.000000000000000000, 0.000000000000000000 ) ) ;
#201274=CARTESIAN_POINT ( 'NONE',  ( -1.402160292154681736E-14, 13.17187500034139980, 1.575800808251682339 ) ) ;
#201285=EDGE_CURVE ( 'NONE', #39789, #60352, #147863, .T. ) ;
#201316=CARTESIAN_POINT ( 'NONE',  ( -1.500000000000001110, 14.02083333333333037, 0.8660254037844419273 ) ) ;
#201324=CARTESIAN_POINT ( 'NONE',  ( -0.6823417656250039265, 11.81770833367473017, -1.181850606188755259 ) ) ;
#201371=CARTESIAN_POINT ( 'NONE',  ( 1.364683531249997417, 13.29687500034139980, 2.602085213965210642E-15 ) ) ;
#201411=CARTESIAN_POINT ( 'NONE',  ( -1.500000000000015099, 11.47916666666666252, -0.8660254037844309360 ) ) ;
#201469=CARTESIAN_POINT ( 'NONE',  ( -8.012344526598182026E-15, 11.54687500034139980, -1.575800808251669460 ) ) ;
#201501=CARTESIAN_POINT ( 'NONE',  ( 0.4546835345321549871, 13.29443243002577191, 1.375797179799232106 ) ) ;
#201574=AXIS2_PLACEMENT_3D ( 'NONE', #174586, #190789, #210236 ) ;
#201611=( BOUNDED_CURVE ( )  B_SPLINE_CURVE ( 2, ( #202771, #133571, #68505, #69568, #38169, #117345, #292, #54421, #118414 ),
 .UNSPECIFIED., .F., .T. ) 
 B_SPLINE_CURVE_WITH_KNOTS ( ( 3, 2, 2, 2, 3 ),
 ( 0.7946428571428572063, 0.7976190476190476719, 0.8035714285714286031, 0.8095238095238095344, 0.8125000000000000000 ),
 .UNSPECIFIED. ) 
 CURVE ( )  GEOMETRIC_REPRESENTATION_ITEM ( )  RATIONAL_B_SPLINE_CURVE ( ( 0.9330127018922194093, 0.9330127018922206306, 1.000000000000000000, 0.8660254037844387076, 1.000000000000000000, 0.8660254037844387076, 1.000000000000000000, 0.9330127018922194093, 0.9330127018922194093 ) ) 
 REPRESENTATION_ITEM ( '' )  );
#201618=CARTESIAN_POINT ( 'NONE',  ( -1.402160292154681736E-14, 11.48437500034139980, 1.575800808251682339 ) ) ;
#201668=LINE ( 'NONE', #71671, #180686 ) ;
#201687=CARTESIAN_POINT ( 'NONE',  ( -8.012344526598182026E-15, 9.359375000341399797, -1.575800808251669460 ) ) ;
#201691=AXIS2_PLACEMENT_3D ( 'NONE', #32367, #63790, #46491 ) ;
#201692=AXIS2_PLACEMENT_3D ( 'NONE', #102650, #71182, #37643 ) ;
#201722=VECTOR ( 'NONE', #104789, 1000.000000000000000 ) ;
#201732=CARTESIAN_POINT ( 'NONE',  ( 1.499999999999997113, 8.427083334016133520, -0.8660254037844378194 ) ) ;
#201827=CARTESIAN_POINT ( 'NONE',  ( -2.788906526875773208E-15, 9.187500000000001776, -1.499999999999998446 ) ) ;
#201927=CARTESIAN_POINT ( 'NONE',  ( 0.6823417656249969321, 13.58854166700806942, -1.181850606188757036 ) ) ;
#201962=CARTESIAN_POINT ( 'NONE',  ( -5.000000000000009770, 3.850000000000006306, 6.071532165918824830E-15 ) ) ;
#202026=DIRECTION ( 'NONE',  ( 0.000000000000000000, -1.000000000000000000, 0.000000000000000000 ) ) ;
#202034=CARTESIAN_POINT ( 'NONE',  ( 0.7500000000000006661, 12.86458333401613352, 1.299038105676657340 ) ) ;
#202115=CARTESIAN_POINT ( 'NONE',  ( -0.6823417656250003738, 11.40104166700806765, 1.181850606188754593 ) ) ;
#202119=CARTESIAN_POINT ( 'NONE',  ( 0.4019237886466778820, 9.323664549684631098, 1.500000000000001554 ) ) ;
#202120=CARTESIAN_POINT ( 'NONE',  ( -0.7500000000000179856, 9.041666666666669627, 1.299038105676658228 ) ) ;
#202174=CARTESIAN_POINT ( 'NONE',  ( 1.364683531250000748, 9.317708333674731946, -0.7879004041258355073 ) ) ;
#202250=CARTESIAN_POINT ( 'NONE',  ( 1.499999999999993117, 10.88541666734946389, 0.8660254037844409281 ) ) ;
#202298=CARTESIAN_POINT ( 'NONE',  ( -1.500000000000015099, 11.26041666734946567, -0.8660254037844309360 ) ) ;
#202302=VECTOR ( 'NONE', #72797, 1000.000000000000000 ) ;
#202324=CARTESIAN_POINT ( 'NONE',  ( 1.493132593725484458, 3.264523918964489457, -0.1629718138060145538 ) ) ;
#202336=CARTESIAN_POINT ( 'NONE',  ( 0.6823417656249934904, 13.19270833367473195, 1.181850606188764807 ) ) ;
#202384=CARTESIAN_POINT ( 'NONE',  ( -1.402160292154681736E-14, 13.31250000000000000, 1.732050807568881190 ) ) ;
#202390=CARTESIAN_POINT ( 'NONE',  ( -1.364683531250000748, 12.10937500034139980, 0.000000000000000000 ) ) ;
#202435=CARTESIAN_POINT ( 'NONE',  ( -1.364683531250000748, 13.17187500034139980, 0.000000000000000000 ) ) ;
#202536=CARTESIAN_POINT ( 'NONE',  ( -1.402160292154681736E-14, 11.42187500034140157, 1.575800808251682339 ) ) ;
#202544=DIRECTION ( 'NONE',  ( 0.000000000000000000, -1.000000000000000000, 0.000000000000000000 ) ) ;
#202692=CARTESIAN_POINT ( 'NONE',  ( 1.364683531249997417, 10.79687500034139802, 2.602085213965210642E-15 ) ) ;
#202706=VERTEX_POINT ( 'NONE', #158325 ) ;
#202724=CARTESIAN_POINT ( 'NONE',  ( 0.000000000000000000, 13.49999999999999822, 0.000000000000000000 ) ) ;
#202755=CARTESIAN_POINT ( 'NONE',  ( -8.012344526598182026E-15, 8.609375000341403350, -1.575800808251669460 ) ) ;
#202771=CARTESIAN_POINT ( 'NONE',  ( 1.220146605508150803E-14, 9.718750000682797818, -1.499999999999998446 ) ) ;
#202801=CARTESIAN_POINT ( 'NONE',  ( -0.7500000000000006661, 8.989583334016129967, -1.299038105676657340 ) ) ;
#202803=ORIENTED_EDGE ( 'NONE', *, *, #154706, .F. ) ;
#202874=EDGE_LOOP ( 'NONE', ( #76006, #27704, #138508, #168928 ) ) ;
#202899=( BOUNDED_CURVE ( )  B_SPLINE_CURVE ( 2, ( #36466, #3941, #153435, #1809, #150240, #54865, #168604, #166473, #20206 ),
 .UNSPECIFIED., .F., .T. ) 
 B_SPLINE_CURVE_WITH_KNOTS ( ( 3, 2, 2, 2, 3 ),
 ( 0.8303571428571429047, 0.8333333333333333703, 0.8392857142857143016, 0.8452380952380952328, 0.8482142857142856984 ),
 .UNSPECIFIED. ) 
 CURVE ( )  GEOMETRIC_REPRESENTATION_ITEM ( )  RATIONAL_B_SPLINE_CURVE ( ( 0.9330127018922194093, 0.9330127018922206306, 1.000000000000000000, 0.8660254037844387076, 1.000000000000000000, 0.8660254037844387076, 1.000000000000000000, 0.9330127018922194093, 0.9330127018922194093 ) ) 
 REPRESENTATION_ITEM ( '' )  );
#202938=CARTESIAN_POINT ( 'NONE',  ( -0.6823417656250039265, 8.567708333674733723, -1.181850606188755259 ) ) ;
#202944=CARTESIAN_POINT ( 'NONE',  ( 1.364683531250000303, 15.31770833367473017, -0.7879004041258355073 ) ) ;
#202955=( BOUNDED_CURVE ( )  B_SPLINE_CURVE ( 2, ( #56952, #173935, #91616, #124178, #137145, #120966, #25507, #186937, #157666 ),
 .UNSPECIFIED., .F., .T. ) 
 B_SPLINE_CURVE_WITH_KNOTS ( ( 3, 2, 2, 2, 3 ),
 ( 0.9017857142857143016, 0.9047619047619047672, 0.9107142857142856984, 0.9166666666666666297, 0.9196428571428570953 ),
 .UNSPECIFIED. ) 
 CURVE ( )  GEOMETRIC_REPRESENTATION_ITEM ( )  RATIONAL_B_SPLINE_CURVE ( ( 0.9330127018922194093, 0.9330127018922194093, 1.000000000000000000, 0.8660254037844387076, 1.000000000000000000, 0.8660254037844387076, 1.000000000000000000, 0.9330127018922206306, 0.9330127018922194093 ) ) 
 REPRESENTATION_ITEM ( '' )  );
#203007=CARTESIAN_POINT ( 'NONE',  ( -1.364683531250010295, 12.44270833367473372, 0.7879004041258445001 ) ) ;
#203089=CARTESIAN_POINT ( 'NONE',  ( -0.7500000000000006661, 10.98958333401613174, -1.299038105676657340 ) ) ;
#203126=AXIS2_PLACEMENT_3D ( 'NONE', #55229, #75741, #189489 ) ;
#203171=CARTESIAN_POINT ( 'NONE',  ( -1.378881877344243945, 4.087185210397143109, 0.5904953584335903560 ) ) ;
#203174=EDGE_CURVE ( 'NONE', #139889, #210054, #48833, .T. ) ;
#203196=CARTESIAN_POINT ( 'NONE',  ( -0.6823417656250003738, 11.65104166700806765, 1.181850606188754593 ) ) ;
#203201=CARTESIAN_POINT ( 'NONE',  ( -1.500000000000001110, 10.27083333333332860, 0.8660254037844419273 ) ) ;
#203252=CARTESIAN_POINT ( 'NONE',  ( 1.364683531249997417, 9.046875000341403350, 2.602085213965210642E-15 ) ) ;
#203258=CARTESIAN_POINT ( 'NONE',  ( -0.4019237886466871523, 10.22991455036742714, -1.499999999999998668 ) ) ;
#203307=CARTESIAN_POINT ( 'NONE',  ( 1.499999999999996891, 12.39583333333333037, -0.8660254037844378194 ) ) ;
#203309=CARTESIAN_POINT ( 'NONE',  ( -1.500000000000001110, 9.802083334016129967, 0.8660254037844418162 ) ) ;
#203313=CARTESIAN_POINT ( 'NONE',  ( -1.115562610750309283E-14, 8.343750000682796042, 1.500000000000001554 ) ) ;
#203317=ADVANCED_FACE ( 'NONE', ( #165775 ), #85892, .T. ) ;
#203373=AXIS2_PLACEMENT_3D ( 'NONE', #38700, #156730, #106957 ) ;
#203388=ORIENTED_EDGE ( 'NONE', *, *, #19860, .F. ) ;
#203404=CARTESIAN_POINT ( 'NONE',  ( -1.364683531250000748, 13.85937500034140157, 0.000000000000000000 ) ) ;
#203449=CARTESIAN_POINT ( 'NONE',  ( 1.500000000000001332, 13.62499999999999822, 0.000000000000000000 ) ) ;
#203455=CARTESIAN_POINT ( 'NONE',  ( -1.364683531250014514, 11.58854166700806410, -0.7879004041258335089 ) ) ;
#203501=CARTESIAN_POINT ( 'NONE',  ( 0.6823417656249934904, 13.25520833367473195, 1.181850606188764807 ) ) ;
#203603=CARTESIAN_POINT ( 'NONE',  ( -1.364683531250014514, 10.33854166700806765, -0.7879004041258335089 ) ) ;
#203634=CARTESIAN_POINT ( 'NONE',  ( 0.1851935683049925341, 13.36182424988519912, -1.369245237587793040 ) ) ;
#203733=ORIENTED_EDGE ( 'NONE', *, *, #191341, .T. ) ;
#203755=CARTESIAN_POINT ( 'NONE',  ( -1.364683531250014514, 11.15104166700806232, -0.7879004041258335089 ) ) ;
#203764=CARTESIAN_POINT ( 'NONE',  ( -1.104620755056546555, 13.37576698399828246, -0.8213461108120255760 ) ) ;
#203781=CARTESIAN_POINT ( 'NONE',  ( -1.364683531250014514, 14.83854166700806410, -0.7879004041258335089 ) ) ;
#203822=CARTESIAN_POINT ( 'NONE',  ( 0.6823417656249934904, 8.505208333674733723, 1.181850606188764807 ) ) ;
#203868=CARTESIAN_POINT ( 'NONE',  ( -1.364683531250000748, 13.85937500034140157, 0.000000000000000000 ) ) ;
#203880=CARTESIAN_POINT ( 'NONE',  ( -1.435158330144267635, 4.071532573434739177, -0.4529249069356953150 ) ) ;
#203897=ADVANCED_FACE ( 'NONE', ( #1912 ), #137302, .F. ) ;
#203903=CARTESIAN_POINT ( 'NONE',  ( 1.109591582173274693, -4.250299932362443300, -0.07813100402512697384 ) ) ;
#203960=CARTESIAN_POINT ( 'NONE',  ( 1.499999999999996891, 8.427083334016131744, -0.8660254037844378194 ) ) ;
#204002=CARTESIAN_POINT ( 'NONE',  ( -1.402160292154681736E-14, 14.48437500034139980, 1.575800808251682339 ) ) ;
#204061=CARTESIAN_POINT ( 'NONE',  ( -1.364683531250000748, 13.42187500034139980, 0.000000000000000000 ) ) ;
#204091=DIRECTION ( 'NONE',  ( 0.000000000000000000, -1.000000000000000000, 0.000000000000000000 ) ) ;
#204109=CARTESIAN_POINT ( 'NONE',  ( -1.109591582173425461, -4.250299932362596067, 0.07813100402492727248 ) ) ;
#204152=( BOUNDED_CURVE ( )  B_SPLINE_CURVE ( 2, ( #86024, #37272, #124749, #109555, #22051, #42370, #71879, #19938, #140952 ),
 .UNSPECIFIED., .F., .T. ) 
 B_SPLINE_CURVE_WITH_KNOTS ( ( 3, 2, 2, 2, 3 ),
 ( 0.6696428571428570953, 0.6726190476190476719, 0.6785714285714286031, 0.6845238095238095344, 0.6875000000000000000 ),
 .UNSPECIFIED. ) 
 CURVE ( )  GEOMETRIC_REPRESENTATION_ITEM ( )  RATIONAL_B_SPLINE_CURVE ( ( 0.9330127018922194093, 0.9330127018922180770, 1.000000000000000000, 0.8660254037844387076, 1.000000000000000000, 0.8660254037844387076, 1.000000000000000000, 0.9330127018922194093, 0.9330127018922194093 ) ) 
 REPRESENTATION_ITEM ( '' )  );
#204205=AXIS2_PLACEMENT_3D ( 'NONE', #202724, #74891, #120514 ) ;
#204252=CARTESIAN_POINT ( 'NONE',  ( 1.364683531249997417, 10.48437500034139802, 2.602085213965210642E-15 ) ) ;
#204259=CARTESIAN_POINT ( 'NONE',  ( 0.7500000000000006661, 9.666666666666671404, -1.299038105676657340 ) ) ;
#204278=CARTESIAN_POINT ( 'NONE',  ( -1.500000000000008216, 8.531250000682797818, 3.469446951953614189E-15 ) ) ;
#204309=CARTESIAN_POINT ( 'NONE',  ( 0.6823417656249969321, 8.838541667008065872, -1.181850606188757036 ) ) ;
#204367=CARTESIAN_POINT ( 'NONE',  ( -0.4019237886466871523, 9.229914550367427140, -1.499999999999998668 ) ) ;
#204460=CARTESIAN_POINT ( 'NONE',  ( 0.7500000000000006661, 12.69791666734946389, -1.299038105676657340 ) ) ;
#204484=CARTESIAN_POINT ( 'NONE',  ( 1.499999999999996891, 12.17708333401613352, -0.8660254037844378194 ) ) ;
#204519=CARTESIAN_POINT ( 'NONE',  ( 0.7500000000000006661, 13.41666666666666785, -1.299038105676657340 ) ) ;
#204525=CARTESIAN_POINT ( 'NONE',  ( 1.364683531249997417, 10.98437500034139802, 2.602085213965210642E-15 ) ) ;
#204646=CYLINDRICAL_SURFACE ( 'NONE', #206549, 1.500000000000000222 ) ;
#204672=CARTESIAN_POINT ( 'NONE',  ( 0.6823417656249934904, 10.94270833367473550, 1.181850606188764807 ) ) ;
#204767=DIRECTION ( 'NONE',  ( 0.000000000000000000, -1.000000000000000000, 0.000000000000000000 ) ) ;
#204819=CARTESIAN_POINT ( 'NONE',  ( 1.364683531249997417, 10.54687500034139802, 2.602085213965210642E-15 ) ) ;
#204831=CARTESIAN_POINT ( 'NONE',  ( -1.500000000000001110, 10.77083333333333037, 0.8660254037844418162 ) ) ;
#204841=CARTESIAN_POINT ( 'NONE',  ( 0.5150272702496164756, 3.543562648825416161, 0.3999758201171684791 ) ) ;
#204845=CARTESIAN_POINT ( 'NONE',  ( -8.012344526598182026E-15, 14.79687500034140157, -1.575800808251669460 ) ) ;
#204860=CARTESIAN_POINT ( 'NONE',  ( 1.500000000000001332, 9.906250000682799595, 0.000000000000000000 ) ) ;
#204889=CARTESIAN_POINT ( 'NONE',  ( -1.364683531250000748, 8.421875000341403350, 0.000000000000000000 ) ) ;
#204899=EDGE_LOOP ( 'NONE', ( #193159, #45573 ) ) ;
#204937=CARTESIAN_POINT ( 'NONE',  ( -0.6823417656250003738, 14.15104166700806232, 1.181850606188754593 ) ) ;
#204946=CARTESIAN_POINT ( 'NONE',  ( -1.423138914311270709, 3.789383647063556904, -0.4995195405159393309 ) ) ;
#205060=CARTESIAN_POINT ( 'NONE',  ( 1.286813488861813459, 4.047007041464545374, -0.4595522011843575783 ) ) ;
#205083=CARTESIAN_POINT ( 'NONE',  ( -1.364683531250000748, 15.17187500034139447, 0.000000000000000000 ) ) ;
#205142=CARTESIAN_POINT ( 'NONE',  ( -1.364683531250000748, 12.42187500034139980, 0.000000000000000000 ) ) ;
#205179=CARTESIAN_POINT ( 'NONE',  ( -1.115562610750309283E-14, 11.31249999999999822, 1.500000000000001554 ) ) ;
#205229=CARTESIAN_POINT ( 'NONE',  ( -1.115562610750309283E-14, 9.593750000682799595, 1.500000000000001554 ) ) ;
#205336=CARTESIAN_POINT ( 'NONE',  ( -0.6823417656250003738, 10.90104166700806765, 1.181850606188754593 ) ) ;
#205395=CARTESIAN_POINT ( 'NONE',  ( 0.6823417656249934904, 8.505208333674733723, 1.181850606188764807 ) ) ;
#205435=CYLINDRICAL_SURFACE ( 'NONE', #171553, 0.5000000000000003331 ) ;
#205442=ORIENTED_EDGE ( 'NONE', *, *, #116111, .T. ) ;
#205543=VERTEX_POINT ( 'NONE', #730 ) ;
#205551=CARTESIAN_POINT ( 'NONE',  ( -2.788906526875773208E-15, 12.43750000000000000, -1.499999999999998446 ) ) ;
#205565=CARTESIAN_POINT ( 'NONE',  ( 0.4019237886466816012, 12.20758545099816672, -1.499999999999998668 ) ) ;
#205600=CARTESIAN_POINT ( 'NONE',  ( -1.500000000000001110, 14.27083333333333215, 0.8660254037844419273 ) ) ;
#205605=CARTESIAN_POINT ( 'NONE',  ( -0.6823417656250039265, 10.31770833367473550, -1.181850606188755259 ) ) ;
#205650=CARTESIAN_POINT ( 'NONE',  ( -1.402160292154681736E-14, 12.48437500034139802, 1.575800808251682339 ) ) ;
#205656=DIRECTION ( 'NONE',  ( 0.000000000000000000, -1.000000000000000000, 0.000000000000000000 ) ) ;
#205677=CARTESIAN_POINT ( 'NONE',  ( -1.364683531250000748, 13.35937500034139980, 0.000000000000000000 ) ) ;
#205681=ORIENTED_EDGE ( 'NONE', *, *, #122569, .T. ) ;
#205717=CARTESIAN_POINT ( 'NONE',  ( 0.7500000000000006661, 15.19791666734946567, -1.299038105676657340 ) ) ;
#205752=CARTESIAN_POINT ( 'NONE',  ( 0.6823417656249934904, 10.19270833367473550, 1.181850606188764807 ) ) ;
#205786=CARTESIAN_POINT ( 'NONE',  ( 0.4572639771135831865, 13.35664422513058547, -1.309345794938320928 ) ) ;
#205853=DIRECTION ( 'NONE',  ( 0.000000000000000000, 1.000000000000000000, 0.000000000000000000 ) ) ;
#205905=CARTESIAN_POINT ( 'NONE',  ( -1.364683531250014514, 9.151041667008060543, -0.7879004041258335089 ) ) ;
#205912=CARTESIAN_POINT ( 'NONE',  ( -1.320903661431851450, 13.37576698399828956, 0.3874755904549384566 ) ) ;
#205914=DIRECTION ( 'NONE',  ( 0.000000000000000000, 0.000000000000000000, 1.000000000000000000 ) ) ;
#205930=CARTESIAN_POINT ( 'NONE',  ( -0.6823417656250039265, 14.81770833367473195, -1.181850606188755259 ) ) ;
#205953=ORIENTED_EDGE ( 'NONE', *, *, #24366, .T. ) ;
#205973=CARTESIAN_POINT ( 'NONE',  ( -1.500000000000015099, 15.47916666666666430, -0.8660254037844309360 ) ) ;
#205978=CARTESIAN_POINT ( 'NONE',  ( -1.493132593725482682, 4.435476081035520046, -0.1629718138060227417 ) ) ;
#206016=CARTESIAN_POINT ( 'NONE',  ( 1.364683531249996529, 13.71354166700806765, 0.7879004041258405033 ) ) ;
#206027=CARTESIAN_POINT ( 'NONE',  ( 1.836970198721030181E-16, 13.49999999999999822, 1.500000000000000222 ) ) ;
#206115=CARTESIAN_POINT ( 'NONE',  ( -1.500095892183268109, 3.249791167484341159, 0.08036760724049506199 ) ) ;
#206161=CARTESIAN_POINT ( 'NONE',  ( -1.364683531250000748, 14.42187500034139447, 0.000000000000000000 ) ) ;
#206223=CARTESIAN_POINT ( 'NONE',  ( -8.012344526598182026E-15, 11.60937500034140157, -1.575800808251669460 ) ) ;
#206265=CARTESIAN_POINT ( 'NONE',  ( -6.009258394948636914E-15, 11.71875000068279604, -1.732050807568875195 ) ) ;
#206276=ADVANCED_FACE ( 'NONE', ( #119751 ), #137014, .F. ) ;
#206370=CARTESIAN_POINT ( 'NONE',  ( -0.7807912181424305764, 13.24045051524828942, -1.280767376876722041 ) ) ;
#206411=CARTESIAN_POINT ( 'NONE',  ( -0.6823417656250039265, 11.06770833367473550, -1.181850606188755259 ) ) ;
#206416=CARTESIAN_POINT ( 'NONE',  ( 1.499999999999993117, 9.354166666666667851, 0.8660254037844408170 ) ) ;
#206469=CARTESIAN_POINT ( 'NONE',  ( -1.364683531250010740, 8.442708333674730170, 0.7879004041258445001 ) ) ;
#206549=AXIS2_PLACEMENT_3D ( 'NONE', #74678, #23777, #87723 ) ;
#206615=VECTOR ( 'NONE', #140764, 1000.000000000000000 ) ;
#206671=CARTESIAN_POINT ( 'NONE',  ( -0.7500000000000006661, 12.20833333333333570, -1.299038105676657340 ) ) ;
#206677=CARTESIAN_POINT ( 'NONE',  ( -0.6823417656250003738, 10.65104166700806765, 1.181850606188754593 ) ) ;
#206721=CARTESIAN_POINT ( 'NONE',  ( -1.402160292154681736E-14, 11.48437500034139980, 1.575800808251682339 ) ) ;
#206819=CARTESIAN_POINT ( 'NONE',  ( -1.402160292154681736E-14, 10.92187500034139802, 1.575800808251682339 ) ) ;
#206851=CARTESIAN_POINT ( 'NONE',  ( 0.09321446940366702461, 13.36358420534790703, -1.376866309900354413 ) ) ;
#206890=EDGE_LOOP ( 'NONE', ( #162559, #89513, #137925, #34357 ) ) ;
#206908=( BOUNDED_CURVE ( )  B_SPLINE_CURVE ( 2, ( #118381, #102072, #168137, #106392, #21846, #186511, #155096, #41366, #91180 ),
 .UNSPECIFIED., .F., .T. ) 
 B_SPLINE_CURVE_WITH_KNOTS ( ( 3, 2, 2, 2, 3 ),
 ( 0.5089285714285713969, 0.5119047619047618625, 0.5178571428571429047, 0.5238095238095238360, 0.5267857142857143016 ),
 .UNSPECIFIED. ) 
 CURVE ( )  GEOMETRIC_REPRESENTATION_ITEM ( )  RATIONAL_B_SPLINE_CURVE ( ( 0.9330127018922194093, 0.9330127018922194093, 1.000000000000000000, 0.8660254037844387076, 1.000000000000000000, 0.8660254037844387076, 1.000000000000000000, 0.9330127018922194093, 0.9330127018922194093 ) ) 
 REPRESENTATION_ITEM ( '' )  );
#206917=ADVANCED_FACE ( 'NONE', ( #122990 ), #41666, .T. ) ;
#206950=AXIS2_PLACEMENT_3D ( 'NONE', #134372, #19499, #152714 ) ;
#206957=CARTESIAN_POINT ( 'NONE',  ( 0.4019237886466847653, 10.35491455036742714, 1.499999999999997113 ) ) ;
#206971=CARTESIAN_POINT ( 'NONE',  ( -1.402160292154681736E-14, 9.484375000341398021, 1.575800808251682339 ) ) ;
#206978=CARTESIAN_POINT ( 'NONE',  ( -0.5368768833858145184, 13.37576698399828246, -1.254641125003840507 ) ) ;
#206993=CIRCLE ( 'NONE', #155063, 1.500000000000000222 ) ;
#206995=CARTESIAN_POINT ( 'NONE',  ( -8.012344526598182026E-15, 14.29687500034139802, -1.575800808251669460 ) ) ;
#207013=CARTESIAN_POINT ( 'NONE',  ( 0.4019237886466778820, 9.854914550367428916, 1.500000000000001554 ) ) ;
#207019=CARTESIAN_POINT ( 'NONE',  ( -1.115562610750309283E-14, 11.81250000000000000, 1.500000000000001554 ) ) ;
#207040=CARTESIAN_POINT ( 'NONE',  ( -1.500000000000008216, 14.49999999999999822, 3.469446951953614189E-15 ) ) ;
#207043=EDGE_CURVE ( 'NONE', #29614, #162002, #56746, .T. ) ;
#207083=CARTESIAN_POINT ( 'NONE',  ( -1.364683531250014514, 14.83854166700806410, -0.7879004041258335089 ) ) ;
#207096=CARTESIAN_POINT ( 'NONE',  ( -1.425126390603233428, 3.734596776778838390, -0.4909503797920832247 ) ) ;
#207102=ORIENTED_EDGE ( 'NONE', *, *, #17820, .T. ) ;
#207231=CARTESIAN_POINT ( 'NONE',  ( -1.364683531250014514, 13.65104166700806765, -0.7879004041258335089 ) ) ;
#207295=CARTESIAN_POINT ( 'NONE',  ( -1.364683531250000748, 11.67187500034139802, 0.000000000000000000 ) ) ;
#207340=CARTESIAN_POINT ( 'NONE',  ( -1.402160292154681736E-14, 10.59375000068279782, 1.732050807568881190 ) ) ;
#207358=EDGE_CURVE ( 'NONE', #86318, #170765, #80064, .T. ) ;
#207459=DIRECTION ( 'NONE',  ( 0.000000000000000000, -1.000000000000000000, 0.000000000000000000 ) ) ;
#207462=CARTESIAN_POINT ( 'NONE',  ( 1.499999999999993117, 8.854166666666666075, 0.8660254037844408170 ) ) ;
#207478=CARTESIAN_POINT ( 'NONE',  ( 0.6823417656249969321, 10.77604166700806765, -1.181850606188757036 ) ) ;
#207485=CARTESIAN_POINT ( 'NONE',  ( -1.402160292154681736E-14, 8.812500000000003553, 1.732050807568881190 ) ) ;
#207549=CARTESIAN_POINT ( 'NONE',  ( 0.6823417656249969321, 15.08854166700806410, -1.181850606188757036 ) ) ;
#207616=EDGE_CURVE ( 'NONE', #183713, #151085, #41585, .T. ) ;
#207739=CARTESIAN_POINT ( 'NONE',  ( 1.499999999999997113, 12.64583333333333215, -0.8660254037844378194 ) ) ;
#207744=CARTESIAN_POINT ( 'NONE',  ( -1.364683531250000748, 10.35937500034139802, 0.000000000000000000 ) ) ;
#207782=CARTESIAN_POINT ( 'NONE',  ( -1.402160292154681736E-14, 11.98437500034140335, 1.575800808251682339 ) ) ;
#207851=CARTESIAN_POINT ( 'NONE',  ( -1.500000000000001110, 14.05208333401613530, 0.8660254037844419273 ) ) ;
#207885=CARTESIAN_POINT ( 'NONE',  ( -0.6823417656250039265, 9.817708333674735499, -1.181850606188755259 ) ) ;
#207902=ADVANCED_FACE ( 'NONE', ( #93566 ), #108795, .T. ) ;
#207998=AXIS2_PLACEMENT_3D ( 'NONE', #208309, #126094, #187796 ) ;
#208007=EDGE_CURVE ( 'NONE', #180121, #143111, #94636, .T. ) ;
#208012=DIRECTION ( 'NONE',  ( 0.000000000000000000, 0.000000000000000000, 1.000000000000000000 ) ) ;
#208013=DIRECTION ( 'NONE',  ( 0.000000000000000000, 0.000000000000000000, -1.000000000000000000 ) ) ;
#208021=CARTESIAN_POINT ( 'NONE',  ( 1.500000000000001332, 10.40625000068279249, 0.000000000000000000 ) ) ;
#208035=CARTESIAN_POINT ( 'NONE',  ( -0.6823417656250039265, 9.880208333674728394, -1.181850606188755259 ) ) ;
#208041=CARTESIAN_POINT ( 'NONE',  ( -0.4486483537597074078, 13.27801534917682780, 1.409698628028286382 ) ) ;
#208046=CARTESIAN_POINT ( 'NONE',  ( 1.264911064067342217, 3.850000000000006306, -0.4999999999999987232 ) ) ;
#208047=B_SPLINE_CURVE_WITH_KNOTS ( 'NONE', 3,
 ( #159356, #8835, #155100, #75976 ),
 .UNSPECIFIED., .F., .F.,
 ( 4, 4 ),
 ( 0.001673025196799804177, 0.002270020235895683393 ),
 .UNSPECIFIED. ) ;
#208053=CARTESIAN_POINT ( 'NONE',  ( 0.5997958527293488773, 3.416913062369157483, -0.2585301179639583613 ) ) ;
#208076=CARTESIAN_POINT ( 'NONE',  ( 0.7500000000000006661, 9.864583334016129967, 1.299038105676657340 ) ) ;
#208104=CARTESIAN_POINT ( 'NONE',  ( -1.402160292154681736E-14, 15.06250000000000000, 1.732050807568881190 ) ) ;
#208112=ORIENTED_EDGE ( 'NONE', *, *, #122569, .F. ) ;
#208146=CARTESIAN_POINT ( 'NONE',  ( -1.364683531250000748, 14.85937500034140157, 0.000000000000000000 ) ) ;
#208187=CARTESIAN_POINT ( 'NONE',  ( -1.266901613973837604, 3.917879858053340048, 0.4965463943947248104 ) ) ;
#208231=CARTESIAN_POINT ( 'NONE',  ( 0.7500000000000006661, 10.08333333333333215, 1.299038105676657340 ) ) ;
#208262=CARTESIAN_POINT ( 'NONE',  ( 1.354873262373950116, 3.776319345677265460, -0.6436764175676652489 ) ) ;
#208285=CARTESIAN_POINT ( 'NONE',  ( 0.6823417656249969321, 13.58854166700806942, -1.181850606188757036 ) ) ;
#208309=CARTESIAN_POINT ( 'NONE',  ( 0.000000000000000000, 13.49999999999999822, 0.000000000000000000 ) ) ;
#208352=CARTESIAN_POINT ( 'NONE',  ( -1.364683531250000748, 12.17187500034139980, 0.000000000000000000 ) ) ;
#208393=CARTESIAN_POINT ( 'NONE',  ( 1.499999999999993117, 11.13541666734946567, 0.8660254037844409281 ) ) ;
#208491=CARTESIAN_POINT ( 'NONE',  ( 1.286813488861813459, 4.047007041464545374, -0.4595522011843575783 ) ) ;
#208512=CARTESIAN_POINT ( 'NONE',  ( -1.297698954646265834, 3.601166593375767278, 0.4386024987755252624 ) ) ;
#208529=CARTESIAN_POINT ( 'NONE',  ( -1.364683531250014514, 10.08854166700806410, -0.7879004041258335089 ) ) ;
#208604=CARTESIAN_POINT ( 'NONE',  ( -1.364683531250010295, 15.19270833367472839, 0.7879004041258445001 ) ) ;
#208686=CARTESIAN_POINT ( 'NONE',  ( -1.115562610750309283E-14, 9.593750000682799595, 1.500000000000001554 ) ) ;
#208796=CARTESIAN_POINT ( 'NONE',  ( -0.7500000000000179856, 12.29166666666666607, 1.299038105676658228 ) ) ;
#208802=CARTESIAN_POINT ( 'NONE',  ( 0.6823417656249934904, 10.44270833367473550, 1.181850606188764807 ) ) ;
#208840=CARTESIAN_POINT ( 'NONE',  ( -1.364683531250014514, 12.65104166700806232, -0.7879004041258335089 ) ) ;
#208892=FACE_OUTER_BOUND ( 'NONE', #125356, .T. ) ;
#208907=CARTESIAN_POINT ( 'NONE',  ( 1.499999999999993117, 14.13541666734946389, 0.8660254037844409281 ) ) ;
#208940=CARTESIAN_POINT ( 'NONE',  ( -0.6823417656250039265, 9.567708333674735499, -1.181850606188755259 ) ) ;
#208948=CARTESIAN_POINT ( 'NONE',  ( 1.499999999999996891, 11.17708333401612819, -0.8660254037844378194 ) ) ;
#209000=ORIENTED_EDGE ( 'NONE', *, *, #18978, .F. ) ;
#209072=CARTESIAN_POINT ( 'NONE',  ( 1.499999999999996891, 10.42708333401613352, -0.8660254037844378194 ) ) ;
#209089=CARTESIAN_POINT ( 'NONE',  ( 0.6823417656249934904, 9.505208333674728394, 1.181850606188764807 ) ) ;
#209161=CARTESIAN_POINT ( 'NONE',  ( -1.500000000000015099, 14.97916666666666252, -0.8660254037844309360 ) ) ;
#209165=FACE_OUTER_BOUND ( 'NONE', #118317, .T. ) ;
#209203=CARTESIAN_POINT ( 'NONE',  ( -0.6823417656250003738, 13.40104166700806232, 1.181850606188754593 ) ) ;
#209206=CARTESIAN_POINT ( 'NONE',  ( 1.836970198721030181E-16, 13.49999999999999822, 1.500000000000000222 ) ) ;
#209213=CARTESIAN_POINT ( 'NONE',  ( -1.378881877344206197, 4.087185210396952151, 0.5904953584336783967 ) ) ;
#209298=CARTESIAN_POINT ( 'NONE',  ( -1.408835580989212355, 3.462626791720190944, 0.5203893312692456918 ) ) ;
#209318=CARTESIAN_POINT ( 'NONE',  ( 1.390311220213875876, 3.551797531149446296, -0.5641062960582096109 ) ) ;
#209321=ORIENTED_EDGE ( 'NONE', *, *, #91462, .F. ) ;
#209343=CARTESIAN_POINT ( 'NONE',  ( 1.364683531249996529, 13.77604166700806765, 0.7879004041258405033 ) ) ;
#209407=CARTESIAN_POINT ( 'NONE',  ( -0.6823417656250003738, 12.21354166700806765, 1.181850606188754593 ) ) ;
#209431=( BOUNDED_CURVE ( )  B_SPLINE_CURVE ( 2, ( #64994, #180890, #131148, #195020, #163595, #149462, #30400, #147344, #150542 ),
 .UNSPECIFIED., .F., .T. ) 
 B_SPLINE_CURVE_WITH_KNOTS ( ( 3, 2, 2, 2, 3 ),
 ( 0.9017857142857143016, 0.9047619047619047672, 0.9107142857142856984, 0.9166666666666666297, 0.9196428571428570953 ),
 .UNSPECIFIED. ) 
 CURVE ( )  GEOMETRIC_REPRESENTATION_ITEM ( )  RATIONAL_B_SPLINE_CURVE ( ( 0.9330127018922194093, 0.9330127018922194093, 1.000000000000000000, 0.8660254037844387076, 1.000000000000000000, 0.8660254037844387076, 1.000000000000000000, 0.9330127018922206306, 0.9330127018922194093 ) ) 
 REPRESENTATION_ITEM ( '' )  );
#209453=CARTESIAN_POINT ( 'NONE',  ( -1.500000000000001110, 10.80208333401613352, 0.8660254037844419273 ) ) ;
#209493=VERTEX_POINT ( 'NONE', #106394 ) ;
#209506=LINE ( 'NONE', #95810, #98900 ) ;
#209510=CARTESIAN_POINT ( 'NONE',  ( 0.9657642407454472000, -4.140281660848636136, 0.3272472668956626918 ) ) ;
#209526=EDGE_CURVE ( 'NONE', #183272, #12932, #208047, .T. ) ;
#209555=CARTESIAN_POINT ( 'NONE',  ( 1.422919657202426968, 3.901887307304316987, 0.5004438751493111015 ) ) ;
#209574=CARTESIAN_POINT ( 'NONE',  ( -1.494964465105841578, 3.364977991896605847, -0.1399972980471414497 ) ) ;
#209592=CARTESIAN_POINT ( 'NONE',  ( 1.364683531250000748, 9.255208333674733723, -0.7879004041258355073 ) ) ;
#209657=DIRECTION ( 'NONE',  ( 0.000000000000000000, -1.000000000000000000, 0.000000000000000000 ) ) ;
#209778=CARTESIAN_POINT ( 'NONE',  ( 0.7500000000000006661, 11.91666666666666607, -1.299038105676657340 ) ) ;
#209793=FACE_OUTER_BOUND ( 'NONE', #137214, .T. ) ;
#209858=CARTESIAN_POINT ( 'NONE',  ( -1.402160292154681736E-14, 12.31250000000000355, 1.732050807568881190 ) ) ;
#209860=( BOUNDED_CURVE ( )  B_SPLINE_CURVE ( 2, ( #150996, #2563, #198639, #99044, #50287, #119612, #182396, #106286, #166159 ),
 .UNSPECIFIED., .F., .T. ) 
 B_SPLINE_CURVE_WITH_KNOTS ( ( 3, 2, 2, 2, 3 ),
 ( 0.8303571428571429047, 0.8333333333333333703, 0.8392857142857143016, 0.8452380952380952328, 0.8482142857142856984 ),
 .UNSPECIFIED. ) 
 CURVE ( )  GEOMETRIC_REPRESENTATION_ITEM ( )  RATIONAL_B_SPLINE_CURVE ( ( 0.9330127018922194093, 0.9330127018922206306, 1.000000000000000000, 0.8660254037844387076, 1.000000000000000000, 0.8660254037844387076, 1.000000000000000000, 0.9330127018922194093, 0.9330127018922194093 ) ) 
 REPRESENTATION_ITEM ( '' )  );
#209864=CARTESIAN_POINT ( 'NONE',  ( 1.364683531249996529, 8.713541667008067648, 0.7879004041258405033 ) ) ;
#209902=CARTESIAN_POINT ( 'NONE',  ( 0.6823417656249969321, 11.33854166700806765, -1.181850606188757036 ) ) ;
#209932=DIRECTION ( 'NONE',  ( 0.000000000000000000, -1.000000000000000000, 0.000000000000000000 ) ) ;
#209971=CARTESIAN_POINT ( 'NONE',  ( -0.7500000000000179856, 13.32291666734946389, 1.299038105676658228 ) ) ;
#210007=CARTESIAN_POINT ( 'NONE',  ( 0.6823417656249969321, 9.026041667008065872, -1.181850606188757036 ) ) ;
#210010=ORIENTED_EDGE ( 'NONE', *, *, #29537, .T. ) ;
#210019=CARTESIAN_POINT ( 'NONE',  ( 0.4019237886466778820, 10.85491455036742714, 1.500000000000001554 ) ) ;
#210054=VERTEX_POINT ( 'NONE', #29366 ) ;
#210114=PLANE ( 'NONE',  #37584 ) ;
#210160=CARTESIAN_POINT ( 'NONE',  ( -8.012344526598182026E-15, 10.10937500034140157, -1.575800808251669460 ) ) ;
#210202=CARTESIAN_POINT ( 'NONE',  ( -0.7500000000000006661, 9.989583334016129967, -1.299038105676657340 ) ) ;
#210236=DIRECTION ( 'NONE',  ( 0.000000000000000000, 0.000000000000000000, -1.000000000000000000 ) ) ;
#210258=CARTESIAN_POINT ( 'NONE',  ( -0.4019237886467001974, 9.801335450315370679, 1.500000000000001998 ) ) ;
#210277=CARTESIAN_POINT ( 'NONE',  ( -1.364683531250014514, 12.33854166700806054, -0.7879004041258335089 ) ) ;
#210402=CARTESIAN_POINT ( 'NONE',  ( 1.300105796840295813, 3.592889250479052610, 0.4336863642760066528 ) ) ;
#210413=ORIENTED_EDGE ( 'NONE', *, *, #91968, .F. ) ;
#210425=CARTESIAN_POINT ( 'NONE',  ( 0.6823417656249934904, 13.50520833367473195, 1.181850606188764807 ) ) ;
#210448=FACE_OUTER_BOUND ( 'NONE', #85929, .T. ) ;
#210466=ORIENTED_EDGE ( 'NONE', *, *, #41782, .F. ) ;
#210491=CARTESIAN_POINT ( 'NONE',  ( -1.364683531250000748, 11.17187500034139802, 0.000000000000000000 ) ) ;
#210537=CARTESIAN_POINT ( 'NONE',  ( -1.500000000000008216, 10.28125000068279249, 3.469446951953614189E-15 ) ) ;
#210641=CARTESIAN_POINT ( 'NONE',  ( 1.364708430267706829, 3.684592235245700564, 0.6235921627254619182 ) ) ;
#210661=CARTESIAN_POINT ( 'NONE',  ( -1.399654745096419406, 3.350671350837230555, 0.07090406488317851919 ) ) ;
#210678=CARTESIAN_POINT ( 'NONE',  ( -1.364683531250014514, 8.838541667008069425, -0.7879004041258335089 ) ) ;
#210699=VERTEX_POINT ( 'NONE', #52007 ) ;
#210719=( BOUNDED_CURVE ( )  B_SPLINE_CURVE ( 2, ( #46641, #15170, #1036, #96476, #213365, #150535, #195007, #163588, #17293 ),
 .UNSPECIFIED., .F., .T. ) 
 B_SPLINE_CURVE_WITH_KNOTS ( ( 3, 2, 2, 2, 3 ),
 ( 0.8482142857142856984, 0.8511904761904761640, 0.8571428571428570953, 0.8630952380952381375, 0.8660714285714286031 ),
 .UNSPECIFIED. ) 
 CURVE ( )  GEOMETRIC_REPRESENTATION_ITEM ( )  RATIONAL_B_SPLINE_CURVE ( ( 0.9330127018922194093, 0.9330127018922194093, 1.000000000000000000, 0.8660254037844387076, 1.000000000000000000, 0.8660254037844387076, 1.000000000000000000, 0.9330127018922194093, 0.9330127018922194093 ) ) 
 REPRESENTATION_ITEM ( '' )  );
#210816=( NAMED_UNIT ( * ) PLANE_ANGLE_UNIT ( ) SI_UNIT ( $, .RADIAN. ) );
#210930=CARTESIAN_POINT ( 'NONE',  ( -0.7500000000000179856, 12.04166666666666607, 1.299038105676658228 ) ) ;
#210936=CARTESIAN_POINT ( 'NONE',  ( 0.6823417656249934904, 9.942708333674735499, 1.181850606188764807 ) ) ;
#210969=CARTESIAN_POINT ( 'NONE',  ( 1.364683531249997417, 10.54687500034139802, 2.602085213965210642E-15 ) ) ;
#211025=CARTESIAN_POINT ( 'NONE',  ( 1.836970198721030181E-16, 13.49999999999999822, 1.500000000000000222 ) ) ;
#211039=CARTESIAN_POINT ( 'NONE',  ( 1.499999999999993117, 13.88541666734946034, 0.8660254037844409281 ) ) ;
#211076=CARTESIAN_POINT ( 'NONE',  ( 0.6823417656249934904, 8.942708333674733723, 1.181850606188764807 ) ) ;
#211098=ORIENTED_EDGE ( 'NONE', *, *, #209526, .F. ) ;
#211116=CARTESIAN_POINT ( 'NONE',  ( 1.886507792743700940E-16, 13.20000000000000284, 1.540450515248283025 ) ) ;
#211137=CARTESIAN_POINT ( 'NONE',  ( 0.000000000000000000, 13.49999999999999822, 0.000000000000000000 ) ) ;
#211324=CARTESIAN_POINT ( 'NONE',  ( 1.499999999999993117, 11.10416666666666785, 0.8660254037844408170 ) ) ;
#211344=CARTESIAN_POINT ( 'NONE',  ( -1.402160292154681736E-14, 13.17187500034139980, 1.575800808251682339 ) ) ;
#211357=CARTESIAN_POINT ( 'NONE',  ( -1.499708767979548218, 4.349101188573495591, -0.07854769233531130879 ) ) ;
#211382=ORIENTED_EDGE ( 'NONE', *, *, #193016, .F. ) ;
#211395=VERTEX_POINT ( 'NONE', #125615 ) ;
#211414=CARTESIAN_POINT ( 'NONE',  ( 0.000000000000000000, -2.500000000000002220, 0.000000000000000000 ) ) ;
#211438=CARTESIAN_POINT ( 'NONE',  ( -1.500000000000001110, 12.27083333333333925, 0.8660254037844418162 ) ) ;
#211439=CARTESIAN_POINT ( 'NONE',  ( 0.000000000000000000, 6.161115872820241535, 0.000000000000000000 ) ) ;
#211464=CARTESIAN_POINT ( 'NONE',  ( 1.423138914311261827, 3.910616352936421958, -0.4995195405159349455 ) ) ;
#211488=CARTESIAN_POINT ( 'NONE',  ( -8.012344526598182026E-15, 12.85937500034139802, -1.575800808251669460 ) ) ;
#211552=CARTESIAN_POINT ( 'NONE',  ( 0.6823417656249934904, 10.50520833367472839, 1.181850606188764807 ) ) ;
#211592=CARTESIAN_POINT ( 'NONE',  ( -6.009258394948636914E-15, 10.21875000068279604, -1.732050807568875195 ) ) ;
#211696=DIRECTION ( 'NONE',  ( 0.000000000000000000, -1.000000000000000000, 0.000000000000000000 ) ) ;
#211697=CARTESIAN_POINT ( 'NONE',  ( 1.350460993223239425, 4.246634823808397741, 0.3113056364346962757 ) ) ;
#211716=CARTESIAN_POINT ( 'NONE',  ( -1.390391755498394444, 3.551399914175640937, 0.5639175007713631560 ) ) ;
#211735=CARTESIAN_POINT ( 'NONE',  ( -8.012344526598182026E-15, 9.046875000341405126, -1.575800808251669460 ) ) ;
#211749=CARTESIAN_POINT ( 'NONE',  ( -1.432341765625004593, 8.320312500512100584, 8.673617379884035472E-16 ) ) ;
#211807=CARTESIAN_POINT ( 'NONE',  ( 1.364683531250000303, 15.31770833367473017, -0.7879004041258355073 ) ) ;
#211895=AXIS2_PLACEMENT_3D ( 'NONE', #129850, #163339, #49574 ) ;
#211963=CARTESIAN_POINT ( 'NONE',  ( -0.4019237886466933696, 13.05133545031537246, 1.500000000000005995 ) ) ;
#211992=CARTESIAN_POINT ( 'NONE',  ( 1.499999999999997113, 10.39583333333332860, -0.8660254037844378194 ) ) ;
#211998=CARTESIAN_POINT ( 'NONE',  ( -1.402160292154681736E-14, 9.171875000341396245, 1.575800808251682339 ) ) ;
#212032=CARTESIAN_POINT ( 'NONE',  ( 1.364683531249996529, 11.27604166700806410, 0.7879004041258403923 ) ) ;
#212045=CIRCLE ( 'NONE', #201691, 0.09999999999999982514 ) ;
#212047=CIRCLE ( 'NONE', #201692, 2.000000000000000000 ) ;
#212061=CARTESIAN_POINT ( 'NONE',  ( -0.5773502691896470473, -2.500000000000002220, 0.9999999999999991118 ) ) ;
#212088=DIRECTION ( 'NONE',  ( 0.000000000000000000, -1.000000000000000000, 0.000000000000000000 ) ) ;
#212103=CARTESIAN_POINT ( 'NONE',  ( -0.7500000000000006661, 13.98958333401613352, -1.299038105676657340 ) ) ;
#212138=CARTESIAN_POINT ( 'NONE',  ( -1.364683531250000748, 9.109375000341396245, 0.000000000000000000 ) ) ;
#212152=CARTESIAN_POINT ( 'NONE',  ( 0.7500000000000006661, 10.94791666734946212, -1.299038105676657340 ) ) ;
#212216=EDGE_CURVE ( 'NONE', #78562, #185232, #18113, .T. ) ;
#212292=CARTESIAN_POINT ( 'NONE',  ( -0.6823417656250003738, 8.713541667008065872, 1.181850606188754593 ) ) ;
#212385=CARTESIAN_POINT ( 'NONE',  ( -0.4019237886466802689, 9.698664549684631098, -1.500000000000002887 ) ) ;
#212402=CARTESIAN_POINT ( 'NONE',  ( 1.364683531250000303, 13.50520833367472839, -0.7879004041258355073 ) ) ;
#212409=EDGE_CURVE ( 'NONE', #132613, #1738, #120590, .T. ) ;
#212455=ORIENTED_EDGE ( 'NONE', *, *, #18034, .F. ) ;
#212463=B_SPLINE_CURVE_WITH_KNOTS ( 'NONE', 3,
 ( #7653, #188550, #90010, #174465, #106295, #23905, #54296, #120434, #186409, #38046 ),
 .UNSPECIFIED., .F., .F.,
 ( 4, 2, 2, 2, 4 ),
 ( 0.0002061898317416328299, 0.0005587239135660436798, 0.0009112579953904544755, 0.001263792077214865271, 0.001616326159039276067 ),
 .UNSPECIFIED. ) ;
#212560=CARTESIAN_POINT ( 'NONE',  ( 1.364683531249997417, 12.54687500034139980, 2.602085213965210642E-15 ) ) ;
#212584=CARTESIAN_POINT ( 'NONE',  ( -0.7500000000000179856, 12.04166666666666607, 1.299038105676658228 ) ) ;
#212598=EDGE_LOOP ( 'NONE', ( #119935, #160106, #15457, #100334, #32277, #155610, #78568, #154798, #120500, #64210, #55474, #110635, #58055, #158105, #9233, #91420, #42577, #44030, #166157, #1837, #186503, #187126, #199438, #209321, #33260, #31195, #118621, #108244, #172525, #169951, #176085, #126799, #22874, #79665, #87382, #92334, #175832, #94998, #177351, #191827, #171173, #109395, #15320, #103172 ) ) ;
#212619=CARTESIAN_POINT ( 'NONE',  ( -1.364683531250000748, 10.42187500034139802, 0.000000000000000000 ) ) ;
#212621=DIRECTION ( 'NONE',  ( 0.000000000000000000, 0.000000000000000000, -1.000000000000000000 ) ) ;
#212659=CARTESIAN_POINT ( 'NONE',  ( -1.402160292154681736E-14, 10.09375000068279604, 1.732050807568881190 ) ) ;
#212766=CARTESIAN_POINT ( 'NONE',  ( 1.412038856124948838, 4.223545038993179901, -0.5099368981155084635 ) ) ;
#212783=CARTESIAN_POINT ( 'NONE',  ( -1.354875605471922873, 3.776832748260927630, 0.6436714776511484049 ) ) ;
#212801=CARTESIAN_POINT ( 'NONE',  ( -1.364683531250014514, 9.838541667008064096, -0.7879004041258335089 ) ) ;
#212875=CARTESIAN_POINT ( 'NONE',  ( 1.364683531249997417, 14.29687500034140157, 2.602085213965210642E-15 ) ) ;
#212939=ADVANCED_FACE ( 'NONE', ( #113369 ), #158849, .T. ) ;
#212981=( BOUNDED_CURVE ( )  B_SPLINE_CURVE ( 2, ( #203313, #47795, #179904, #31527, #97601 ),
 .UNSPECIFIED., .F., .T. ) 
 B_SPLINE_CURVE_WITH_KNOTS ( ( 3, 2, 3 ),
 ( 0.9910714285714286031, 0.9940476190476190688, 1.000000000000000000 ),
 .UNSPECIFIED. ) 
 CURVE ( )  GEOMETRIC_REPRESENTATION_ITEM ( )  RATIONAL_B_SPLINE_CURVE ( ( 0.9330127018922194093, 0.9330127018922194093, 1.000000000000000000, 0.8660254037844387076, 1.000000000000000000 ) ) 
 REPRESENTATION_ITEM ( '' )  );
#212987=ADVANCED_FACE ( 'NONE', ( #93875 ), #96004, .T. ) ;
#213032=AXIS2_PLACEMENT_3D ( 'NONE', #48520, #163330, #14910 ) ;
#213059=CARTESIAN_POINT ( 'NONE',  ( 1.499999999999997113, 11.39583333333333393, -0.8660254037844378194 ) ) ;
#213064=CARTESIAN_POINT ( 'NONE',  ( -1.364683531250010295, 9.380208333674735499, 0.7879004041258445001 ) ) ;
#213073=DIRECTION ( 'NONE',  ( -0.000000000000000000, 1.000000000000000000, -0.000000000000000000 ) ) ;
#213081=CARTESIAN_POINT ( 'NONE',  ( -1.274519002043997595, 3.715789678311091748, -0.4828173461639007069 ) ) ;
#213099=CARTESIAN_POINT ( 'NONE',  ( 1.364683531249996529, 10.52604166700806765, 0.7879004041258403923 ) ) ;
#213140=CARTESIAN_POINT ( 'NONE',  ( -0.4019237886467001974, 10.05133545031537246, 1.500000000000001998 ) ) ;
#213173=CARTESIAN_POINT ( 'NONE',  ( 0.7500000000000006661, 12.19791666734946389, -1.299038105676657340 ) ) ;
#213207=CARTESIAN_POINT ( 'NONE',  ( -1.402160292154681736E-14, 8.421875000341403350, 1.575800808251682339 ) ) ;
#213247=( BOUNDED_CURVE ( )  B_SPLINE_CURVE ( 2, ( #197173, #179874, #29359, #31499, #196127, #112805, #47765, #83415, #178818 ),
 .UNSPECIFIED., .F., .T. ) 
 B_SPLINE_CURVE_WITH_KNOTS ( ( 3, 2, 2, 2, 3 ),
 ( 0.5803571428571429047, 0.5833333333333333703, 0.5892857142857143016, 0.5952380952380952328, 0.5982142857142856984 ),
 .UNSPECIFIED. ) 
 CURVE ( )  GEOMETRIC_REPRESENTATION_ITEM ( )  RATIONAL_B_SPLINE_CURVE ( ( 0.9330127018922194093, 0.9330127018922206306, 1.000000000000000000, 0.8660254037844387076, 1.000000000000000000, 0.8660254037844387076, 1.000000000000000000, 0.9330127018922194093, 0.9330127018922194093 ) ) 
 REPRESENTATION_ITEM ( '' )  );
#213248=CARTESIAN_POINT ( 'NONE',  ( 1.195384358724066508E-16, -4.140708350189171938, 1.000000000000004441 ) ) ;
#213351=B_SPLINE_CURVE_WITH_KNOTS ( 'NONE', 3,
 ( #186126, #52935, #151521, #73447, #135280, #106015, #87580, #20424, #55081, #4158 ),
 .UNSPECIFIED., .F., .F.,
 ( 4, 2, 2, 2, 4 ),
 ( 0.001822879634083278844, 0.002175306537177320101, 0.002527733440271360925, 0.002880160343365402182, 0.003232587246459443439 ),
 .UNSPECIFIED. ) ;
#213354=CARTESIAN_POINT ( 'NONE',  ( -1.402160292154681736E-14, 8.734375000341403350, 1.575800808251682339 ) ) ;
#213365=CARTESIAN_POINT ( 'NONE',  ( -1.500000000000008216, 9.500000000000001776, 3.469446951953614189E-15 ) ) ;
#213412=CARTESIAN_POINT ( 'NONE',  ( -0.3670591950586384877, 13.37245467069800497, -1.330911102734550822 ) ) ;
#213460=CARTESIAN_POINT ( 'NONE',  ( 1.364683531249997417, 12.48437500034139980, 2.602085213965210642E-15 ) ) ;
#213472=CARTESIAN_POINT ( 'NONE',  ( -1.491588839496432062, 4.432142968562463814, -0.1769418395740521011 ) ) ;
#213528=VERTEX_POINT ( 'NONE', #172712 ) ;
#213604=CARTESIAN_POINT ( 'NONE',  ( -1.364683531250000748, 12.92187500034139980, 0.000000000000000000 ) ) ;
#213667=CARTESIAN_POINT ( 'NONE',  ( -8.012344526598182026E-15, 10.60937500034139624, -1.575800808251669460 ) ) ;
#213710=CARTESIAN_POINT ( 'NONE',  ( -6.009258394948636914E-15, 9.968750000682796042, -1.732050807568875195 ) ) ;
#213787=CARTESIAN_POINT ( 'NONE',  ( -0.7500000000000006661, 12.73958333401613352, -1.299038105676657340 ) ) ;
#213821=CIRCLE ( 'NONE', #23506, 0.6500000000000000222 ) ;
#213851=CARTESIAN_POINT ( 'NONE',  ( 0.6823417656249969321, 8.776041667008065872, -1.181850606188757036 ) ) ;
#213892=EDGE_LOOP ( 'NONE', ( #140177, #87718, #79362, #177920 ) ) ;
#213920=CARTESIAN_POINT ( 'NONE',  ( -1.364683531250014514, 14.15104166700806765, -0.7879004041258335089 ) ) ;
#214096=CARTESIAN_POINT ( 'NONE',  ( -0.7500000000000006661, 10.70833333333333393, -1.299038105676657340 ) ) ;
#214100=CARTESIAN_POINT ( 'NONE',  ( -0.6823417656250039265, 9.067708333674733723, -1.181850606188755259 ) ) ;
#214111=CARTESIAN_POINT ( 'NONE',  ( -0.5151702941667783975, 3.543307664981999228, 0.3998358608512623813 ) ) ;
#214138=CARTESIAN_POINT ( 'NONE',  ( -0.6823417656250039265, 10.13020833367472839, -1.181850606188755259 ) ) ;
#214176=CARTESIAN_POINT ( 'NONE',  ( -0.7500000000000179856, 10.04166666666667140, 1.299038105676658228 ) ) ;
#214193=LINE ( 'NONE', #96252, #92433 ) ;
#214211=CARTESIAN_POINT ( 'NONE',  ( 1.499999999999993117, 12.88541666734946389, 0.8660254037844409281 ) ) ;
#214278=CARTESIAN_POINT ( 'NONE',  ( 1.678041975860264342E-16, 13.49999999999999822, 1.240450515248286534 ) ) ;
#214390=CARTESIAN_POINT ( 'NONE',  ( -1.247849810309911600, 13.37576698399836594, 0.5524780460566154350 ) ) ;
#214397=CARTESIAN_POINT ( 'NONE',  ( -1.500000000000008216, 12.03125000068279427, 3.469446951953614189E-15 ) ) ;
ENDSEC;
END-ISO-10303-21;
